ISO-10303-21;
HEADER;
/* Generated by software containing ST-Developer
 * from STEP Tools, Inc. (www.steptools.com) 
 */

FILE_DESCRIPTION(
/* description */ ('Independent bearing-supported roller-ramp one-way clutch. Six logarit
hmic ramps with plain solid rollers, sprung guided plungers, native Co
il variants, removable shared keepers, rounded parallel key, shaft wit
h complete retaining lips, bronze journal/thrust support and bolted co
vers. Native rotor, roller planar/spin and plunger joints permit manua
l geometric engaged/released inspection. Automatic frictional torque s
witching/contact dynamics are not simulated; no capacity, hardness, fi
t, lubrication, speed, force or life rating. External input driver/cou
pling/anchors outside assembly.'),
/* implementation_level */ '2;1');

FILE_NAME(
/* name */ 'Socket head cap screw M4x12.step',
/* time_stamp */ '2026-11-08T07:04:38-08:00',
/* author */ (''),
/* organization */ (''),
/* preprocessor_version */ 'ST-DEVELOPER v20.2',
/* originating_system */ 'Autodesk Translation Framework v15.17.0.0',
/* authorisation */ '');

FILE_SCHEMA (('AUTOMOTIVE_DESIGN { 1 0 10303 214 3 1 1 }'));
ENDSEC;

DATA;
#10=MECHANICAL_DESIGN_GEOMETRIC_PRESENTATION_REPRESENTATION('',(#314),#99526);
#253=CONICAL_SURFACE('',#19682,1.5,0.785398163397449);
#282=SHAPE_REPRESENTATION_RELATIONSHIP('SRR','None',#99639,#298);
#298=ADVANCED_BREP_SHAPE_REPRESENTATION('',(#330),#99524);
#314=STYLED_ITEM('',(#99722),#330);
#330=MANIFOLD_SOLID_BREP('Body1',#18284);
#437=FACE_BOUND('',#2739,.T.);
#438=FACE_BOUND('',#2742,.T.);
#594=PLANE('',#19688);
#595=PLANE('',#19689);
#596=PLANE('',#19690);
#597=PLANE('',#19691);
#598=PLANE('',#19692);
#599=PLANE('',#19693);
#600=PLANE('',#19694);
#601=PLANE('',#19695);
#602=PLANE('',#19699);
#603=PLANE('',#19700);
#671=B_SPLINE_SURFACE_WITH_KNOTS('',3,3,((#96718,#96719,#96720,#96721,#96722,
#96723,#96724,#96725,#96726,#96727,#96728,#96729,#96730,#96731,#96732,#96733,
#96734,#96735,#96736,#96737,#96738,#96739,#96740,#96741,#96742,#96743,#96744,
#96745,#96746,#96747,#96748,#96749,#96750,#96751,#96752,#96753,#96754,#96755,
#96756,#96757,#96758,#96759,#96760,#96761,#96762,#96763,#96764,#96765,#96766,
#96767,#96768,#96769,#96770,#96771,#96772,#96773,#96774,#96775,#96776,#96777,
#96778,#96779,#96780,#96781,#96782,#96783,#96784,#96785,#96786,#96787,#96788,
#96789,#96790,#96791,#96792,#96793,#96794,#96795,#96796,#96797,#96798,#96799,
#96800,#96801,#96802,#96803,#96804,#96805,#96806,#96807,#96808,#96809,#96810,
#96811,#96812,#96813,#96814,#96815,#96816,#96817,#96818,#96819,#96820,#96821,
#96822,#96823),(#96824,#96825,#96826,#96827,#96828,#96829,#96830,#96831,
#96832,#96833,#96834,#96835,#96836,#96837,#96838,#96839,#96840,#96841,#96842,
#96843,#96844,#96845,#96846,#96847,#96848,#96849,#96850,#96851,#96852,#96853,
#96854,#96855,#96856,#96857,#96858,#96859,#96860,#96861,#96862,#96863,#96864,
#96865,#96866,#96867,#96868,#96869,#96870,#96871,#96872,#96873,#96874,#96875,
#96876,#96877,#96878,#96879,#96880,#96881,#96882,#96883,#96884,#96885,#96886,
#96887,#96888,#96889,#96890,#96891,#96892,#96893,#96894,#96895,#96896,#96897,
#96898,#96899,#96900,#96901,#96902,#96903,#96904,#96905,#96906,#96907,#96908,
#96909,#96910,#96911,#96912,#96913,#96914,#96915,#96916,#96917,#96918,#96919,
#96920,#96921,#96922,#96923,#96924,#96925,#96926,#96927,#96928,#96929),
(#96930,#96931,#96932,#96933,#96934,#96935,#96936,#96937,#96938,#96939,
#96940,#96941,#96942,#96943,#96944,#96945,#96946,#96947,#96948,#96949,#96950,
#96951,#96952,#96953,#96954,#96955,#96956,#96957,#96958,#96959,#96960,#96961,
#96962,#96963,#96964,#96965,#96966,#96967,#96968,#96969,#96970,#96971,#96972,
#96973,#96974,#96975,#96976,#96977,#96978,#96979,#96980,#96981,#96982,#96983,
#96984,#96985,#96986,#96987,#96988,#96989,#96990,#96991,#96992,#96993,#96994,
#96995,#96996,#96997,#96998,#96999,#97000,#97001,#97002,#97003,#97004,#97005,
#97006,#97007,#97008,#97009,#97010,#97011,#97012,#97013,#97014,#97015,#97016,
#97017,#97018,#97019,#97020,#97021,#97022,#97023,#97024,#97025,#97026,#97027,
#97028,#97029,#97030,#97031,#97032,#97033,#97034,#97035),(#97036,#97037,
#97038,#97039,#97040,#97041,#97042,#97043,#97044,#97045,#97046,#97047,#97048,
#97049,#97050,#97051,#97052,#97053,#97054,#97055,#97056,#97057,#97058,#97059,
#97060,#97061,#97062,#97063,#97064,#97065,#97066,#97067,#97068,#97069,#97070,
#97071,#97072,#97073,#97074,#97075,#97076,#97077,#97078,#97079,#97080,#97081,
#97082,#97083,#97084,#97085,#97086,#97087,#97088,#97089,#97090,#97091,#97092,
#97093,#97094,#97095,#97096,#97097,#97098,#97099,#97100,#97101,#97102,#97103,
#97104,#97105,#97106,#97107,#97108,#97109,#97110,#97111,#97112,#97113,#97114,
#97115,#97116,#97117,#97118,#97119,#97120,#97121,#97122,#97123,#97124,#97125,
#97126,#97127,#97128,#97129,#97130,#97131,#97132,#97133,#97134,#97135,#97136,
#97137,#97138,#97139,#97140,#97141)),.UNSPECIFIED.,.F.,.F.,.F.,(4,4),(4,
1,1,1,1,1,1,1,1,1,1,1,1,1,1,1,1,1,1,1,1,1,1,1,1,1,1,1,1,1,1,1,1,1,1,1,1,
1,1,1,1,1,1,1,1,1,1,1,1,1,1,1,1,1,1,1,1,1,1,1,1,1,1,1,1,1,1,1,1,1,1,1,1,
1,1,1,1,1,1,1,1,1,1,1,1,1,1,1,1,1,1,1,1,1,1,1,1,1,1,1,1,1,1,4),(0.,0.0460148164544132),
(11.6154215191105,12.6127573616628,13.610093204215,14.6074290467673,15.6047648893195,
16.6021007318718,17.599436574424,18.5967724169762,19.5941082595285,20.5914441020807,
21.588779944633,22.5861157871852,23.5834516297375,24.5807874722897,25.5781233148419,
26.5754591573942,27.5727949999464,28.5701308424987,29.5674666850509,30.5648025276032,
31.5621383701554,32.5594742127077,33.5568100552599,34.5541458978121,35.5514817403644,
36.5488175829166,37.5461534254689,38.5434892680211,39.5408251105734,40.5381609531256,
41.5354967956779,42.5328326382301,43.5301684807823,44.5275043233346,45.5248401658868,
46.5221760084391,47.5195118509913,48.5168476935436,49.5141835360958,50.5115193786481,
51.5088552212003,52.5061910637525,53.5035269063048,54.500862748857,55.4981985914093,
56.4955344339615,57.4928702765138,58.490206119066,59.4875419616182,60.4848778041705,
61.4822136467227,62.479549489275,63.4768853318272,64.4742211743795,65.4715570169317,
66.468892859484,67.4662287020362,68.4635645445884,69.4609003871407,70.4582362296929,
71.4555720722452,72.4529079147974,73.4502437573497,74.4475795999019,75.4449154424541,
76.4422512850064,77.4395871275586,78.4369229701109,79.4342588126631,80.4315946552154,
81.4289304977676,82.4262663403199,83.4236021828721,84.4209380254243,85.4182738679766,
86.4156097105288,87.4129455530811,88.4102813956333,89.4076172381856,90.4049530807378,
91.4022889232901,92.3996247658423,93.3969606083945,94.3942964509468,95.391632293499,
96.3889681360513,97.3863039786035,98.3836398211558,99.380975663708,100.37831150626,
101.375647348812,102.372983191365,103.370319033917,104.367654876469,105.364990719021,
106.362326561574,107.359662404126,108.356998246678,109.35433408923,110.351669931783,
111.349005774335,112.346341616887,113.343677459439,114.341013301992),
 .UNSPECIFIED.);
#672=B_SPLINE_SURFACE_WITH_KNOTS('',3,3,((#97261,#97262,#97263,#97264,#97265,
#97266,#97267,#97268,#97269,#97270,#97271,#97272,#97273,#97274,#97275,#97276,
#97277,#97278,#97279,#97280,#97281,#97282,#97283,#97284,#97285,#97286,#97287,
#97288,#97289,#97290,#97291,#97292,#97293,#97294,#97295,#97296,#97297,#97298,
#97299,#97300,#97301,#97302,#97303,#97304,#97305,#97306,#97307,#97308,#97309,
#97310,#97311,#97312,#97313,#97314,#97315,#97316,#97317,#97318,#97319,#97320,
#97321,#97322,#97323,#97324,#97325,#97326,#97327,#97328,#97329,#97330,#97331,
#97332,#97333,#97334,#97335,#97336,#97337,#97338,#97339,#97340,#97341,#97342,
#97343,#97344,#97345,#97346,#97347,#97348,#97349,#97350,#97351,#97352,#97353,
#97354,#97355,#97356,#97357,#97358,#97359,#97360,#97361,#97362,#97363,#97364,
#97365,#97366,#97367,#97368),(#97369,#97370,#97371,#97372,#97373,#97374,
#97375,#97376,#97377,#97378,#97379,#97380,#97381,#97382,#97383,#97384,#97385,
#97386,#97387,#97388,#97389,#97390,#97391,#97392,#97393,#97394,#97395,#97396,
#97397,#97398,#97399,#97400,#97401,#97402,#97403,#97404,#97405,#97406,#97407,
#97408,#97409,#97410,#97411,#97412,#97413,#97414,#97415,#97416,#97417,#97418,
#97419,#97420,#97421,#97422,#97423,#97424,#97425,#97426,#97427,#97428,#97429,
#97430,#97431,#97432,#97433,#97434,#97435,#97436,#97437,#97438,#97439,#97440,
#97441,#97442,#97443,#97444,#97445,#97446,#97447,#97448,#97449,#97450,#97451,
#97452,#97453,#97454,#97455,#97456,#97457,#97458,#97459,#97460,#97461,#97462,
#97463,#97464,#97465,#97466,#97467,#97468,#97469,#97470,#97471,#97472,#97473,
#97474,#97475,#97476),(#97477,#97478,#97479,#97480,#97481,#97482,#97483,
#97484,#97485,#97486,#97487,#97488,#97489,#97490,#97491,#97492,#97493,#97494,
#97495,#97496,#97497,#97498,#97499,#97500,#97501,#97502,#97503,#97504,#97505,
#97506,#97507,#97508,#97509,#97510,#97511,#97512,#97513,#97514,#97515,#97516,
#97517,#97518,#97519,#97520,#97521,#97522,#97523,#97524,#97525,#97526,#97527,
#97528,#97529,#97530,#97531,#97532,#97533,#97534,#97535,#97536,#97537,#97538,
#97539,#97540,#97541,#97542,#97543,#97544,#97545,#97546,#97547,#97548,#97549,
#97550,#97551,#97552,#97553,#97554,#97555,#97556,#97557,#97558,#97559,#97560,
#97561,#97562,#97563,#97564,#97565,#97566,#97567,#97568,#97569,#97570,#97571,
#97572,#97573,#97574,#97575,#97576,#97577,#97578,#97579,#97580,#97581,#97582,
#97583,#97584),(#97585,#97586,#97587,#97588,#97589,#97590,#97591,#97592,
#97593,#97594,#97595,#97596,#97597,#97598,#97599,#97600,#97601,#97602,#97603,
#97604,#97605,#97606,#97607,#97608,#97609,#97610,#97611,#97612,#97613,#97614,
#97615,#97616,#97617,#97618,#97619,#97620,#97621,#97622,#97623,#97624,#97625,
#97626,#97627,#97628,#97629,#97630,#97631,#97632,#97633,#97634,#97635,#97636,
#97637,#97638,#97639,#97640,#97641,#97642,#97643,#97644,#97645,#97646,#97647,
#97648,#97649,#97650,#97651,#97652,#97653,#97654,#97655,#97656,#97657,#97658,
#97659,#97660,#97661,#97662,#97663,#97664,#97665,#97666,#97667,#97668,#97669,
#97670,#97671,#97672,#97673,#97674,#97675,#97676,#97677,#97678,#97679,#97680,
#97681,#97682,#97683,#97684,#97685,#97686,#97687,#97688,#97689,#97690,#97691,
#97692)),.UNSPECIFIED.,.F.,.F.,.F.,(4,4),(4,1,1,1,1,1,1,1,1,1,1,1,1,1,1,
1,1,1,1,1,1,1,1,1,1,1,1,1,1,1,1,1,1,1,1,1,1,1,1,1,1,1,1,1,1,1,1,1,1,1,1,
1,1,1,1,1,1,1,1,1,1,1,1,1,1,1,1,1,1,1,1,1,1,1,1,1,1,1,1,1,1,1,1,1,1,1,1,
1,1,1,1,1,1,1,1,1,1,1,1,1,1,1,1,1,1,4),(0.,0.0460148164544132),(8.31058692273969,
9.30859389336977,10.3066008639999,11.30460783463,12.30261480526,13.3006217758901,
14.2986287465202,15.2966357171503,16.2946426877804,17.2926496584105,18.2906566290406,
19.2886635996707,20.2866705703008,21.2846775409308,22.2826845115609,23.280691482191,
24.2786984528211,25.2767054234512,26.2747123940813,27.2727193647114,28.2707263353415,
29.2687333059716,30.2667402766016,31.2647472472317,32.2627542178618,33.2607611884919,
34.258768159122,35.2567751297521,36.2547821003822,37.2527890710123,38.2507960416424,
39.2488030122724,40.2468099829025,41.2448169535326,42.2428239241627,43.2408308947928,
44.2388378654229,45.236844836053,46.2348518066831,47.2328587773132,48.2308657479432,
49.2288727185733,50.2268796892034,51.2248866598335,52.2228936304636,53.2209006010937,
54.2189075717238,55.2169145423539,56.214921512984,57.212928483614,58.2109354542441,
59.2089424248742,60.2069493955043,61.2049563661344,62.2029633367645,63.2009703073946,
64.1989772780247,65.1969842486548,66.1949912192848,67.1929981899149,68.191005160545,
69.1890121311751,70.1870191018052,71.1850260724353,72.1830330430654,73.1810400136955,
74.1790469843256,75.1770539549557,76.1750609255857,77.1730678962158,78.1710748668459,
79.169081837476,80.1670888081061,81.1650957787362,82.1631027493663,83.1611097199964,
84.1591166906264,85.1571236612565,86.1551306318866,87.1531376025167,88.1511445731468,
89.1491515437769,90.147158514407,91.1451654850371,92.1431724556672,93.1411794262973,
94.1391863969273,95.1371933675574,96.1352003381875,97.1332073088176,98.1312142794477,
99.1292212500778,100.127228220708,101.125235191338,102.123242161968,103.121249132598,
104.119256103228,105.117263073858,106.115270044488,107.113277015118,108.111283985749,
109.109290956379,110.107297927009,111.105304897639,112.103311868269,113.101318838899),
 .UNSPECIFIED.);
#1592=FACE_OUTER_BOUND('',#2694,.T.);
#1593=FACE_OUTER_BOUND('',#2695,.T.);
#1594=FACE_OUTER_BOUND('',#2696,.T.);
#1595=FACE_OUTER_BOUND('',#2697,.T.);
#1596=FACE_OUTER_BOUND('',#2698,.T.);
#1597=FACE_OUTER_BOUND('',#2699,.T.);
#1598=FACE_OUTER_BOUND('',#2700,.T.);
#1599=FACE_OUTER_BOUND('',#2701,.T.);
#1600=FACE_OUTER_BOUND('',#2702,.T.);
#1601=FACE_OUTER_BOUND('',#2703,.T.);
#1602=FACE_OUTER_BOUND('',#2704,.T.);
#1603=FACE_OUTER_BOUND('',#2705,.T.);
#1604=FACE_OUTER_BOUND('',#2706,.T.);
#1605=FACE_OUTER_BOUND('',#2707,.T.);
#1606=FACE_OUTER_BOUND('',#2708,.T.);
#1607=FACE_OUTER_BOUND('',#2709,.T.);
#1608=FACE_OUTER_BOUND('',#2710,.T.);
#1609=FACE_OUTER_BOUND('',#2711,.T.);
#1610=FACE_OUTER_BOUND('',#2712,.T.);
#1611=FACE_OUTER_BOUND('',#2713,.T.);
#1612=FACE_OUTER_BOUND('',#2714,.T.);
#1613=FACE_OUTER_BOUND('',#2715,.T.);
#1614=FACE_OUTER_BOUND('',#2716,.T.);
#1615=FACE_OUTER_BOUND('',#2717,.T.);
#1616=FACE_OUTER_BOUND('',#2718,.T.);
#1617=FACE_OUTER_BOUND('',#2719,.T.);
#1618=FACE_OUTER_BOUND('',#2720,.T.);
#1619=FACE_OUTER_BOUND('',#2721,.T.);
#1620=FACE_OUTER_BOUND('',#2722,.T.);
#1621=FACE_OUTER_BOUND('',#2723,.T.);
#1622=FACE_OUTER_BOUND('',#2724,.T.);
#1623=FACE_OUTER_BOUND('',#2725,.T.);
#1624=FACE_OUTER_BOUND('',#2726,.T.);
#1625=FACE_OUTER_BOUND('',#2727,.T.);
#1626=FACE_OUTER_BOUND('',#2728,.T.);
#1627=FACE_OUTER_BOUND('',#2729,.T.);
#1628=FACE_OUTER_BOUND('',#2730,.T.);
#1629=FACE_OUTER_BOUND('',#2731,.T.);
#1630=FACE_OUTER_BOUND('',#2732,.T.);
#1631=FACE_OUTER_BOUND('',#2733,.T.);
#1632=FACE_OUTER_BOUND('',#2734,.T.);
#1633=FACE_OUTER_BOUND('',#2735,.T.);
#1634=FACE_OUTER_BOUND('',#2736,.T.);
#1635=FACE_OUTER_BOUND('',#2737,.T.);
#1636=FACE_OUTER_BOUND('',#2738,.T.);
#1637=FACE_OUTER_BOUND('',#2740,.T.);
#1638=FACE_OUTER_BOUND('',#2741,.T.);
#1639=FACE_OUTER_BOUND('',#2743,.T.);
#2694=EDGE_LOOP('',(#16098,#16099,#16100,#16101));
#2695=EDGE_LOOP('',(#16102,#16103,#16104,#16105));
#2696=EDGE_LOOP('',(#16106,#16107,#16108,#16109));
#2697=EDGE_LOOP('',(#16110,#16111,#16112,#16113));
#2698=EDGE_LOOP('',(#16114,#16115,#16116,#16117));
#2699=EDGE_LOOP('',(#16118,#16119,#16120,#16121));
#2700=EDGE_LOOP('',(#16122,#16123,#16124,#16125));
#2701=EDGE_LOOP('',(#16126,#16127,#16128,#16129));
#2702=EDGE_LOOP('',(#16130,#16131,#16132,#16133));
#2703=EDGE_LOOP('',(#16134,#16135,#16136,#16137));
#2704=EDGE_LOOP('',(#16138,#16139,#16140,#16141));
#2705=EDGE_LOOP('',(#16142,#16143,#16144,#16145));
#2706=EDGE_LOOP('',(#16146,#16147,#16148,#16149));
#2707=EDGE_LOOP('',(#16150,#16151,#16152,#16153));
#2708=EDGE_LOOP('',(#16154,#16155,#16156,#16157));
#2709=EDGE_LOOP('',(#16158,#16159,#16160,#16161));
#2710=EDGE_LOOP('',(#16162,#16163,#16164,#16165));
#2711=EDGE_LOOP('',(#16166,#16167,#16168,#16169));
#2712=EDGE_LOOP('',(#16170,#16171,#16172,#16173));
#2713=EDGE_LOOP('',(#16174,#16175,#16176,#16177));
#2714=EDGE_LOOP('',(#16178,#16179,#16180,#16181));
#2715=EDGE_LOOP('',(#16182,#16183,#16184,#16185));
#2716=EDGE_LOOP('',(#16186,#16187,#16188,#16189));
#2717=EDGE_LOOP('',(#16190,#16191,#16192,#16193));
#2718=EDGE_LOOP('',(#16194,#16195,#16196,#16197));
#2719=EDGE_LOOP('',(#16198,#16199,#16200,#16201));
#2720=EDGE_LOOP('',(#16202,#16203,#16204,#16205));
#2721=EDGE_LOOP('',(#16206,#16207,#16208,#16209));
#2722=EDGE_LOOP('',(#16210,#16211,#16212,#16213));
#2723=EDGE_LOOP('',(#16214,#16215,#16216,#16217));
#2724=EDGE_LOOP('',(#16218,#16219,#16220,#16221));
#2725=EDGE_LOOP('',(#16222,#16223,#16224,#16225));
#2726=EDGE_LOOP('',(#16226,#16227,#16228,#16229,#16230,#16231,#16232,#16233));
#2727=EDGE_LOOP('',(#16234,#16235,#16236,#16237,#16238,#16239,#16240,#16241,
#16242,#16243,#16244,#16245,#16246,#16247,#16248,#16249,#16250,#16251,#16252,
#16253,#16254,#16255,#16256,#16257,#16258,#16259,#16260,#16261,#16262,#16263,
#16264,#16265,#16266,#16267,#16268,#16269));
#2728=EDGE_LOOP('',(#16270,#16271,#16272,#16273));
#2729=EDGE_LOOP('',(#16274,#16275,#16276,#16277,#16278,#16279,#16280,#16281,
#16282,#16283,#16284,#16285,#16286,#16287,#16288,#16289,#16290,#16291,#16292,
#16293,#16294,#16295,#16296,#16297,#16298,#16299,#16300,#16301,#16302,#16303,
#16304,#16305,#16306,#16307,#16308,#16309,#16310));
#2730=EDGE_LOOP('',(#16311,#16312,#16313,#16314));
#2731=EDGE_LOOP('',(#16315,#16316,#16317,#16318));
#2732=EDGE_LOOP('',(#16319,#16320,#16321,#16322));
#2733=EDGE_LOOP('',(#16323,#16324,#16325,#16326));
#2734=EDGE_LOOP('',(#16327,#16328,#16329,#16330));
#2735=EDGE_LOOP('',(#16331,#16332,#16333,#16334));
#2736=EDGE_LOOP('',(#16335,#16336,#16337,#16338));
#2737=EDGE_LOOP('',(#16339,#16340,#16341,#16342,#16343,#16344));
#2738=EDGE_LOOP('',(#16345));
#2739=EDGE_LOOP('',(#16346,#16347,#16348,#16349));
#2740=EDGE_LOOP('',(#16350,#16351,#16352,#16353));
#2741=EDGE_LOOP('',(#16354));
#2742=EDGE_LOOP('',(#16355,#16356,#16357,#16358,#16359,#16360));
#2743=EDGE_LOOP('',(#16361));
#3098=CIRCLE('',#19649,1.954);
#3099=CIRCLE('',#19666,1.5555);
#3100=CIRCLE('',#19683,1.954);
#3101=CIRCLE('',#19684,1.);
#3102=CIRCLE('',#19686,1.5555);
#3103=CIRCLE('',#19696,3.5);
#3104=CIRCLE('',#19698,3.5);
#4516=B_SPLINE_CURVE_WITH_KNOTS('',3,(#95269,#95270,#95271,#95272,#95273,
#95274,#95275,#95276,#95277,#95278),.UNSPECIFIED.,.F.,.F.,(4,3,3,4),(-4.09254174883833,
-3.98934337020898,-2.99200752765673,-2.06514013327813),.UNSPECIFIED.);
#4517=B_SPLINE_CURVE_WITH_KNOTS('',3,(#95281,#95282,#95283,#95284,#95285,
#95286,#95287),.UNSPECIFIED.,.F.,.F.,(4,3,4),(0.,0.998006970630082,1.11419103802948),
 .UNSPECIFIED.);
#4518=B_SPLINE_CURVE_WITH_KNOTS('',3,(#95292,#95293,#95294,#95295,#95296,
#95297,#95298,#95299,#95300,#95301,#95302,#95303,#95304,#95305,#95306,#95307,
#95308,#95309,#95310,#95311,#95312,#95313),.UNSPECIFIED.,.F.,.F.,(4,3,3,
3,3,3,3,4),(-10.3757270560179,-9.97335842552244,-8.9760225829702,-7.97868674041795,
-6.9813508978657,-5.98401505531347,-4.98667921276122,-4.09254174883833),
 .UNSPECIFIED.);
#4519=B_SPLINE_CURVE_WITH_KNOTS('',3,(#95314,#95315,#95316,#95317,#95318,
#95319,#95320,#95321,#95322,#95323,#95324,#95325,#95326,#95327,#95328,#95329,
#95330,#95331,#95332,#95333,#95334,#95335),.UNSPECIFIED.,.F.,.F.,(4,3,3,
3,3,3,3,4),(1.11419103802948,1.99601394126018,2.99402091189026,3.99202788252035,
4.99003485315045,5.98804182378054,6.98604879441062,7.39737634520907),
 .UNSPECIFIED.);
#4520=B_SPLINE_CURVE_WITH_KNOTS('',3,(#95340,#95341,#95342,#95343,#95344,
#95345,#95346,#95347,#95348,#95349,#95350,#95351,#95352,#95353,#95354,#95355,
#95356,#95357,#95358,#95359,#95360,#95361),.UNSPECIFIED.,.F.,.F.,(4,3,3,
3,3,3,3,4),(-16.6589123631975,-15.9573734808359,-14.9600376382837,-13.9627017957314,
-12.9653659531792,-11.9680301106269,-10.9706942680747,-10.3757270560179),
 .UNSPECIFIED.);
#4521=B_SPLINE_CURVE_WITH_KNOTS('',3,(#95362,#95363,#95364,#95365,#95366,
#95367,#95368,#95369,#95370,#95371,#95372,#95373,#95374,#95375,#95376,#95377,
#95378,#95379,#95380,#95381,#95382,#95383),.UNSPECIFIED.,.F.,.F.,(4,3,3,
3,3,3,3,4),(7.39737634520907,7.98405576504071,8.9820627356708,9.98006970630089,
10.978076676931,11.9760836475611,12.9740906181912,13.6805616523887),
 .UNSPECIFIED.);
#4522=B_SPLINE_CURVE_WITH_KNOTS('',3,(#95388,#95389,#95390,#95391,#95392,
#95393,#95394,#95395,#95396,#95397,#95398,#95399,#95400,#95401,#95402,#95403,
#95404,#95405,#95406,#95407,#95408,#95409,#95410,#95411,#95412),
 .UNSPECIFIED.,.F.,.F.,(4,3,3,3,3,3,3,3,4),(-22.9420976703771,-22.9387243787016,
-21.9413885361494,-20.9440526935971,-19.9467168510449,-18.9493810084926,
-17.9520451659404,-16.9547093233881,-16.6589123631975),.UNSPECIFIED.);
#4523=B_SPLINE_CURVE_WITH_KNOTS('',3,(#95413,#95414,#95415,#95416,#95417,
#95418,#95419,#95420,#95421,#95422,#95423,#95424,#95425,#95426,#95427,#95428,
#95429,#95430,#95431,#95432,#95433,#95434,#95435,#95436,#95437),
 .UNSPECIFIED.,.F.,.F.,(4,3,3,3,3,3,3,3,4),(13.6805616523887,13.9720975888212,
14.9701045594513,15.9681115300814,16.9661185007115,17.9641254713416,18.9621324419717,
19.9601394126018,19.9637469595682),.UNSPECIFIED.);
#4524=B_SPLINE_CURVE_WITH_KNOTS('',3,(#95442,#95443,#95444,#95445,#95446,
#95447,#95448,#95449,#95450,#95451,#95452,#95453,#95454,#95455,#95456,#95457,
#95458,#95459,#95460,#95461,#95462,#95463),.UNSPECIFIED.,.F.,.F.,(4,3,3,
3,3,3,3,4),(-29.2252829775567,-28.9227394340151,-27.9254035914628,-26.9280677489106,
-25.9307319063583,-24.9333960638061,-23.9360602212539,-22.9420976703771),
 .UNSPECIFIED.);
#4525=B_SPLINE_CURVE_WITH_KNOTS('',3,(#95464,#95465,#95466,#95467,#95468,
#95469,#95470,#95471,#95472,#95473,#95474,#95475,#95476,#95477,#95478,#95479,
#95480,#95481,#95482,#95483,#95484,#95485),.UNSPECIFIED.,.F.,.F.,(4,3,3,
3,3,3,3,4),(19.9637469595682,20.9581463832319,21.956153353862,22.954160324492,
23.9521672951221,24.9501742657522,25.9481812363823,26.2469322667478),
 .UNSPECIFIED.);
#4526=B_SPLINE_CURVE_WITH_KNOTS('',3,(#95490,#95491,#95492,#95493,#95494,
#95495,#95496,#95497,#95498,#95499,#95500,#95501,#95502,#95503,#95504,#95505,
#95506,#95507,#95508,#95509,#95510,#95511),.UNSPECIFIED.,.F.,.F.,(4,3,3,
3,3,3,3,4),(-35.5084682847363,-34.9067544893285,-33.9094186467763,-32.9120828042241,
-31.9147469616718,-30.9174111191196,-29.9200752765673,-29.2252829775567),
 .UNSPECIFIED.);
#4527=B_SPLINE_CURVE_WITH_KNOTS('',3,(#95512,#95513,#95514,#95515,#95516,
#95517,#95518,#95519,#95520,#95521,#95522,#95523,#95524,#95525,#95526,#95527,
#95528,#95529,#95530,#95531,#95532,#95533),.UNSPECIFIED.,.F.,.F.,(4,3,3,
3,3,3,3,4),(26.2469322667478,26.9461882070124,27.9441951776425,28.9422021482726,
29.9402091189027,30.9382160895327,31.9362230601628,32.5301175739274),
 .UNSPECIFIED.);
#4528=B_SPLINE_CURVE_WITH_KNOTS('',3,(#95538,#95539,#95540,#95541,#95542,
#95543,#95544,#95545,#95546,#95547,#95548,#95549,#95550,#95551,#95552,#95553,
#95554,#95555,#95556,#95557,#95558,#95559),.UNSPECIFIED.,.F.,.F.,(4,3,3,
3,3,3,3,4),(-41.7916535919159,-40.890769544642,-39.8934337020898,-38.8960978595375,
-37.8987620169853,-36.901426174433,-35.9040903318808,-35.5084682847363),
 .UNSPECIFIED.);
#4529=B_SPLINE_CURVE_WITH_KNOTS('',3,(#95560,#95561,#95562,#95563,#95564,
#95565,#95566,#95567,#95568,#95569,#95570,#95571,#95572,#95573,#95574,#95575,
#95576,#95577,#95578,#95579,#95580,#95581),.UNSPECIFIED.,.F.,.F.,(4,3,3,
3,3,3,3,4),(32.5301175739274,32.9342300307929,33.932237001423,34.9302439720531,
35.9282509426832,36.9262579133133,37.9242648839434,38.813302881107),
 .UNSPECIFIED.);
#4530=B_SPLINE_CURVE_WITH_KNOTS('',3,(#95586,#95587,#95588,#95589,#95590,
#95591,#95592,#95593,#95594,#95595,#95596,#95597,#95598,#95599,#95600,#95601,
#95602,#95603,#95604,#95605,#95606,#95607,#95608,#95609,#95610),
 .UNSPECIFIED.,.F.,.F.,(4,3,3,3,3,3,3,3,4),(-48.0748388990955,-47.8721204425077,
-46.8747845999555,-45.8774487574032,-44.880112914851,-43.8827770722987,
-42.8854412297465,-41.8881053871943,-41.7916535919159),.UNSPECIFIED.);
#4531=B_SPLINE_CURVE_WITH_KNOTS('',3,(#95611,#95612,#95613,#95614,#95615,
#95616,#95617,#95618,#95619,#95620,#95621,#95622,#95623,#95624,#95625,#95626,
#95627,#95628,#95629,#95630,#95631,#95632,#95633,#95634,#95635),
 .UNSPECIFIED.,.F.,.F.,(4,3,3,3,3,3,3,3,4),(38.813302881107,38.9222718545735,
39.9202788252036,40.9182857958337,41.9162927664637,42.9142997370938,43.9123067077239,
44.910313678354,45.0964881882866),.UNSPECIFIED.);
#4532=B_SPLINE_CURVE_WITH_KNOTS('',3,(#95640,#95641,#95642,#95643,#95644,
#95645,#95646,#95647,#95648,#95649,#95650,#95651,#95652,#95653,#95654,#95655,
#95656,#95657,#95658,#95659,#95660,#95661),.UNSPECIFIED.,.F.,.F.,(4,3,3,
3,3,3,3,4),(-54.3580242062751,-53.8561354978212,-52.8587996552689,-51.8614638127167,
-50.8641279701645,-49.8667921276122,-48.86945628506,-48.0748388990955),
 .UNSPECIFIED.);
#4533=B_SPLINE_CURVE_WITH_KNOTS('',3,(#95662,#95663,#95664,#95665,#95666,
#95667,#95668,#95669,#95670,#95671,#95672,#95673,#95674,#95675,#95676,#95677,
#95678,#95679,#95680,#95681,#95682,#95683),.UNSPECIFIED.,.F.,.F.,(4,3,3,
3,3,3,3,4),(45.0964881882866,45.9083206489841,46.9063276196142,47.9043345902443,
48.9023415608744,49.9003485315045,50.8983555021345,51.3796734954662),
 .UNSPECIFIED.);
#4534=B_SPLINE_CURVE_WITH_KNOTS('',3,(#95688,#95689,#95690,#95691,#95692,
#95693,#95694,#95695,#95696,#95697,#95698,#95699,#95700,#95701,#95702,#95703,
#95704,#95705,#95706,#95707,#95708,#95709),.UNSPECIFIED.,.F.,.F.,(4,3,3,
3,3,3,3,4),(-60.6412095134546,-59.8401505531347,-58.8428147105824,-57.8454788680302,
-56.8481430254779,-55.8508071829257,-54.8534713403734,-54.3580242062751),
 .UNSPECIFIED.);
#4535=B_SPLINE_CURVE_WITH_KNOTS('',3,(#95710,#95711,#95712,#95713,#95714,
#95715,#95716,#95717,#95718,#95719,#95720,#95721,#95722,#95723,#95724,#95725,
#95726,#95727,#95728,#95729,#95730,#95731),.UNSPECIFIED.,.F.,.F.,(4,3,3,
3,3,3,3,4),(51.3796734954662,51.8963624727646,52.8943694433947,53.8923764140248,
54.8903833846549,55.888390355285,56.8863973259151,57.6628588026458),
 .UNSPECIFIED.);
#4536=B_SPLINE_CURVE_WITH_KNOTS('',3,(#95736,#95737,#95738,#95739,#95740,
#95741,#95742,#95743,#95744,#95745,#95746,#95747,#95748,#95749,#95750,#95751,
#95752,#95753,#95754,#95755,#95756,#95757,#95758,#95759,#95760),
 .UNSPECIFIED.,.F.,.F.,(4,3,3,3,3,3,3,3,4),(-66.9243948206342,-66.8215014510004,
-65.8241656084481,-64.8268297658959,-63.8294939233436,-62.8321580807914,
-61.8348222382391,-60.8374863956869,-60.6412095134546),.UNSPECIFIED.);
#4537=B_SPLINE_CURVE_WITH_KNOTS('',3,(#95761,#95762,#95763,#95764,#95765,
#95766,#95767,#95768,#95769,#95770,#95771,#95772,#95773,#95774,#95775,#95776,
#95777,#95778,#95779,#95780,#95781,#95782,#95783,#95784,#95785),
 .UNSPECIFIED.,.F.,.F.,(4,3,3,3,3,3,3,3,4),(57.6628588026458,57.8844042965452,
58.8824112671752,59.8804182378054,60.8784252084354,61.8764321790655,62.8744391496956,
63.8724461203257,63.9460441098254),.UNSPECIFIED.);
#4538=B_SPLINE_CURVE_WITH_KNOTS('',3,(#95790,#95791,#95792,#95793,#95794,
#95795,#95796,#95797,#95798,#95799,#95800,#95801,#95802,#95803,#95804,#95805,
#95806,#95807,#95808,#95809,#95810,#95811),.UNSPECIFIED.,.F.,.F.,(4,3,3,
3,3,3,3,4),(-73.2075801278138,-72.8055165063138,-71.8081806637616,-70.8108448212093,
-69.8135089786571,-68.8161731361048,-67.8188372935526,-66.9243948206342),
 .UNSPECIFIED.);
#4539=B_SPLINE_CURVE_WITH_KNOTS('',3,(#95812,#95813,#95814,#95815,#95816,
#95817,#95818,#95819,#95820,#95821,#95822,#95823,#95824,#95825,#95826,#95827,
#95828,#95829,#95830,#95831,#95832,#95833),.UNSPECIFIED.,.F.,.F.,(4,3,3,
3,3,3,3,4),(63.9460441098254,64.8704530909558,65.8684600615859,66.866467032216,
67.8644740028461,68.8624809734761,69.8604879441062,70.229229417005),
 .UNSPECIFIED.);
#4540=B_SPLINE_CURVE_WITH_KNOTS('',3,(#95838,#95839,#95840,#95841,#95842,
#95843,#95844,#95845,#95846,#95847,#95848,#95849,#95850,#95851,#95852,#95853,
#95854,#95855,#95856,#95857,#95858,#95859),.UNSPECIFIED.,.F.,.F.,(4,3,3,
3,3,3,3,4),(-79.4907654349934,-78.7895315616273,-77.792195719075,-76.7948598765228,
-75.7975240339705,-74.8001881914183,-73.802852348866,-73.2075801278138),
 .UNSPECIFIED.);
#4541=B_SPLINE_CURVE_WITH_KNOTS('',3,(#95860,#95861,#95862,#95863,#95864,
#95865,#95866,#95867,#95868,#95869,#95870,#95871,#95872,#95873,#95874,#95875,
#95876,#95877,#95878,#95879,#95880,#95881),.UNSPECIFIED.,.F.,.F.,(4,3,3,
3,3,3,3,4),(70.229229417005,70.8584949147363,71.8565018853664,72.8545088559965,
73.8525158266266,74.8505227972567,75.8485297678868,76.5124147241846),
 .UNSPECIFIED.);
#4542=B_SPLINE_CURVE_WITH_KNOTS('',3,(#95886,#95887,#95888,#95889,#95890,
#95891,#95892,#95893,#95894,#95895,#95896,#95897,#95898,#95899,#95900,#95901,
#95902,#95903,#95904,#95905,#95906,#95907,#95908,#95909,#95910),
 .UNSPECIFIED.,.F.,.F.,(4,3,3,3,3,3,3,3,4),(-85.773950742173,-85.770882459493,
-84.7735466169407,-83.7762107743885,-82.7788749318363,-81.781539089284,
-80.7842032467318,-79.7868674041795,-79.4907654349934),.UNSPECIFIED.);
#4543=B_SPLINE_CURVE_WITH_KNOTS('',3,(#95911,#95912,#95913,#95914,#95915,
#95916,#95917,#95918,#95919,#95920,#95921,#95922,#95923,#95924,#95925,#95926,
#95927,#95928,#95929,#95930,#95931,#95932),.UNSPECIFIED.,.F.,.F.,(4,3,3,
3,3,3,3,4),(76.5124147241846,76.8465367385169,77.8445437091469,78.842550679777,
79.8405576504071,80.8385646210372,81.8365715916673,82.7956000313642),
 .UNSPECIFIED.);
#4544=B_SPLINE_CURVE_WITH_KNOTS('',3,(#95937,#95938,#95939,#95940,#95941,
#95942,#95943,#95944,#95945,#95946,#95947,#95948,#95949,#95950,#95951,#95952,
#95953,#95954,#95955,#95956,#95957,#95958),.UNSPECIFIED.,.F.,.F.,(4,3,3,
3,3,3,3,4),(-92.0571360493526,-91.7548975148065,-90.7575616722542,-89.760225829702,
-88.7628899871497,-87.7655541445975,-86.7682183020452,-85.773950742173),
 .UNSPECIFIED.);
#4545=B_SPLINE_CURVE_WITH_KNOTS('',3,(#95959,#95960,#95961,#95962,#95963,
#95964,#95965,#95966,#95967,#95968,#95969,#95970,#95971,#95972,#95973,#95974,
#95975,#95976,#95977,#95978,#95979,#95980,#95981,#95982,#95983),
 .UNSPECIFIED.,.F.,.F.,(4,3,3,3,3,3,3,3,4),(82.7956000313642,82.8345785622974,
83.8325855329275,84.8305925035576,85.8285994741877,86.8266064448178,87.8246134154479,
88.822620386078,89.0787853385438),.UNSPECIFIED.);
#4546=B_SPLINE_CURVE_WITH_KNOTS('',3,(#95988,#95989,#95990,#95991,#95992,
#95993,#95994,#95995,#95996,#95997,#95998,#95999,#96000,#96001,#96002,#96003,
#96004,#96005,#96006,#96007,#96008,#96009),.UNSPECIFIED.,.F.,.F.,(4,3,3,
3,3,3,3,4),(-98.3403213565322,-97.7389125701199,-96.7415767275677,-95.7442408850154,
-94.7469050424632,-93.7495691999109,-92.7522333573587,-92.0571360493526),
 .UNSPECIFIED.);
#4547=B_SPLINE_CURVE_WITH_KNOTS('',3,(#96010,#96011,#96012,#96013,#96014,
#96015,#96016,#96017,#96018,#96019,#96020,#96021,#96022,#96023,#96024,#96025,
#96026,#96027,#96028,#96029,#96030,#96031),.UNSPECIFIED.,.F.,.F.,(4,3,3,
3,3,3,3,4),(89.0787853385438,89.820627356708,90.8186343273381,91.8166412979682,
92.8146482685983,93.8126552392284,94.8106622098585,95.3619706457233),
 .UNSPECIFIED.);
#4548=B_SPLINE_CURVE_WITH_KNOTS('',3,(#96037,#96038,#96039,#96040,#96041,
#96042,#96043,#96044),.UNSPECIFIED.,.F.,.F.,(4,1,1,1,1,4),(109.955742875643,
110.351669931783,111.349005774335,112.346341616887,113.343677459439,114.341013301992),
 .UNSPECIFIED.);
#4549=B_SPLINE_CURVE_WITH_KNOTS('',3,(#96047,#96048,#96049,#96050,#96051,
#96052,#96053),.UNSPECIFIED.,.F.,.F.,(4,1,1,1,4),(109.955742875643,110.107297927009,
111.105304897639,112.103311868269,113.101318838899),.UNSPECIFIED.);
#4550=B_SPLINE_CURVE_WITH_KNOTS('',3,(#96058,#96059,#96060,#96061,#96062,
#96063,#96064,#96065,#96066,#96067),.UNSPECIFIED.,.F.,.F.,(4,1,1,1,1,1,
1,4),(103.672557568463,104.367654876469,105.364990719021,106.362326561574,
107.359662404126,108.356998246678,109.35433408923,109.955742875643),
 .UNSPECIFIED.);
#4551=B_SPLINE_CURVE_WITH_KNOTS('',3,(#96068,#96069,#96070,#96071,#96072,
#96073,#96074,#96075,#96076,#96077),.UNSPECIFIED.,.F.,.F.,(4,1,1,1,1,1,
1,4),(103.672557568463,104.119256103228,105.117263073858,106.115270044488,
107.113277015118,108.111283985749,109.109290956379,109.955742875643),
 .UNSPECIFIED.);
#4552=B_SPLINE_CURVE_WITH_KNOTS('',3,(#96082,#96083,#96084,#96085,#96086,
#96087,#96088,#96089,#96090,#96091),.UNSPECIFIED.,.F.,.F.,(4,1,1,1,1,1,
1,4),(97.3893722612836,98.3836398211558,99.380975663708,100.37831150626,
101.375647348812,102.372983191365,103.370319033917,103.672557568463),
 .UNSPECIFIED.);
#4553=B_SPLINE_CURVE_WITH_KNOTS('',3,(#96092,#96093,#96094,#96095,#96096,
#96097,#96098,#96099,#96100,#96101),.UNSPECIFIED.,.F.,.F.,(4,1,1,1,1,1,
1,4),(97.3893722612836,98.1312142794477,99.1292212500778,100.127228220708,
101.125235191338,102.123242161968,103.121249132598,103.672557568463),
 .UNSPECIFIED.);
#4554=B_SPLINE_CURVE_WITH_KNOTS('',3,(#96106,#96107,#96108,#96109,#96110,
#96111,#96112,#96113,#96114,#96115,#96116),.UNSPECIFIED.,.F.,.F.,(4,1,1,
1,1,1,1,1,4),(91.106186954104,91.4022889232901,92.3996247658423,93.3969606083945,
94.3942964509468,95.391632293499,96.3889681360513,97.3863039786035,97.3893722612836),
 .UNSPECIFIED.);
#4555=B_SPLINE_CURVE_WITH_KNOTS('',3,(#96117,#96118,#96119,#96120,#96121,
#96122,#96123,#96124,#96125,#96126,#96127),.UNSPECIFIED.,.F.,.F.,(4,1,1,
1,1,1,1,1,4),(91.106186954104,91.1451654850371,92.1431724556672,93.1411794262973,
94.1391863969273,95.1371933675574,96.1352003381875,97.1332073088176,97.3893722612836),
 .UNSPECIFIED.);
#4556=B_SPLINE_CURVE_WITH_KNOTS('',3,(#96132,#96133,#96134,#96135,#96136,
#96137,#96138,#96139,#96140,#96141),.UNSPECIFIED.,.F.,.F.,(4,1,1,1,1,1,
1,4),(84.8230016469244,85.4182738679766,86.4156097105288,87.4129455530811,
88.4102813956333,89.4076172381856,90.4049530807378,91.106186954104),
 .UNSPECIFIED.);
#4557=B_SPLINE_CURVE_WITH_KNOTS('',3,(#96142,#96143,#96144,#96145,#96146,
#96147,#96148,#96149,#96150,#96151),.UNSPECIFIED.,.F.,.F.,(4,1,1,1,1,1,
1,4),(84.8230016469244,85.1571236612565,86.1551306318866,87.1531376025167,
88.1511445731468,89.1491515437769,90.147158514407,91.106186954104),
 .UNSPECIFIED.);
#4558=B_SPLINE_CURVE_WITH_KNOTS('',3,(#96156,#96157,#96158,#96159,#96160,
#96161,#96162,#96163,#96164,#96165),.UNSPECIFIED.,.F.,.F.,(4,1,1,1,1,1,
1,4),(78.5398163397448,79.4342588126631,80.4315946552154,81.4289304977676,
82.4262663403199,83.4236021828721,84.4209380254243,84.8230016469244),
 .UNSPECIFIED.);
#4559=B_SPLINE_CURVE_WITH_KNOTS('',3,(#96166,#96167,#96168,#96169,#96170,
#96171,#96172,#96173,#96174,#96175),.UNSPECIFIED.,.F.,.F.,(4,1,1,1,1,1,
1,4),(78.5398163397448,79.169081837476,80.1670888081061,81.1650957787362,
82.1631027493663,83.1611097199964,84.1591166906264,84.8230016469244),
 .UNSPECIFIED.);
#4560=B_SPLINE_CURVE_WITH_KNOTS('',3,(#96180,#96181,#96182,#96183,#96184,
#96185,#96186,#96187,#96188,#96189,#96190),.UNSPECIFIED.,.F.,.F.,(4,1,1,
1,1,1,1,1,4),(72.2566310325652,72.4529079147974,73.4502437573497,74.4475795999019,
75.4449154424541,76.4422512850064,77.4395871275586,78.4369229701109,78.5398163397448),
 .UNSPECIFIED.);
#4561=B_SPLINE_CURVE_WITH_KNOTS('',3,(#96191,#96192,#96193,#96194,#96195,
#96196,#96197,#96198,#96199,#96200),.UNSPECIFIED.,.F.,.F.,(4,1,1,1,1,1,
1,4),(72.2566310325652,73.1810400136955,74.1790469843256,75.1770539549557,
76.1750609255857,77.1730678962158,78.1710748668459,78.5398163397448),
 .UNSPECIFIED.);
#4562=B_SPLINE_CURVE_WITH_KNOTS('',3,(#96205,#96206,#96207,#96208,#96209,
#96210,#96211,#96212,#96213,#96214),.UNSPECIFIED.,.F.,.F.,(4,1,1,1,1,1,
1,4),(65.9734457253856,66.468892859484,67.4662287020362,68.4635645445884,
69.4609003871407,70.4582362296929,71.4555720722452,72.2566310325652),
 .UNSPECIFIED.);
#4563=B_SPLINE_CURVE_WITH_KNOTS('',3,(#96215,#96216,#96217,#96218,#96219,
#96220,#96221,#96222,#96223,#96224,#96225),.UNSPECIFIED.,.F.,.F.,(4,1,1,
1,1,1,1,1,4),(65.9734457253856,66.1949912192848,67.1929981899149,68.191005160545,
69.1890121311751,70.1870191018052,71.1850260724353,72.1830330430654,72.2566310325652),
 .UNSPECIFIED.);
#4564=B_SPLINE_CURVE_WITH_KNOTS('',3,(#96230,#96231,#96232,#96233,#96234,
#96235,#96236,#96237,#96238,#96239),.UNSPECIFIED.,.F.,.F.,(4,1,1,1,1,1,
1,4),(59.690260418206,60.4848778041705,61.4822136467227,62.479549489275,
63.4768853318272,64.4742211743795,65.4715570169317,65.9734457253856),
 .UNSPECIFIED.);
#4565=B_SPLINE_CURVE_WITH_KNOTS('',3,(#96240,#96241,#96242,#96243,#96244,
#96245,#96246,#96247,#96248,#96249),.UNSPECIFIED.,.F.,.F.,(4,1,1,1,1,1,
1,4),(59.690260418206,60.2069493955043,61.2049563661344,62.2029633367645,
63.2009703073946,64.1989772780247,65.1969842486548,65.9734457253856),
 .UNSPECIFIED.);
#4566=B_SPLINE_CURVE_WITH_KNOTS('',3,(#96254,#96255,#96256,#96257,#96258,
#96259,#96260,#96261,#96262,#96263,#96264),.UNSPECIFIED.,.F.,.F.,(4,1,1,
1,1,1,1,1,4),(53.4070751110265,53.5035269063048,54.500862748857,55.4981985914093,
56.4955344339615,57.4928702765138,58.490206119066,59.4875419616182,59.690260418206),
 .UNSPECIFIED.);
#4567=B_SPLINE_CURVE_WITH_KNOTS('',3,(#96265,#96266,#96267,#96268,#96269,
#96270,#96271,#96272,#96273,#96274),.UNSPECIFIED.,.F.,.F.,(4,1,1,1,1,1,
1,4),(53.4070751110264,54.2189075717238,55.2169145423539,56.214921512984,
57.212928483614,58.2109354542441,59.2089424248742,59.690260418206),
 .UNSPECIFIED.);
#4568=B_SPLINE_CURVE_WITH_KNOTS('',3,(#96279,#96280,#96281,#96282,#96283,
#96284,#96285,#96286,#96287,#96288),.UNSPECIFIED.,.F.,.F.,(4,1,1,1,1,1,
1,4),(47.1238898038469,47.5195118509913,48.5168476935436,49.5141835360958,
50.5115193786481,51.5088552212003,52.5061910637525,53.4070751110265),
 .UNSPECIFIED.);
#4569=B_SPLINE_CURVE_WITH_KNOTS('',3,(#96289,#96290,#96291,#96292,#96293,
#96294,#96295,#96296,#96297,#96298,#96299),.UNSPECIFIED.,.F.,.F.,(4,1,1,
1,1,1,1,1,4),(47.1238898038468,47.2328587773132,48.2308657479432,49.2288727185733,
50.2268796892034,51.2248866598335,52.2228936304636,53.2209006010937,53.4070751110264),
 .UNSPECIFIED.);
#4570=B_SPLINE_CURVE_WITH_KNOTS('',3,(#96304,#96305,#96306,#96307,#96308,
#96309,#96310,#96311,#96312,#96313),.UNSPECIFIED.,.F.,.F.,(4,1,1,1,1,1,
1,4),(40.8407044966673,41.5354967956779,42.5328326382301,43.5301684807823,
44.5275043233346,45.5248401658868,46.5221760084391,47.1238898038469),
 .UNSPECIFIED.);
#4571=B_SPLINE_CURVE_WITH_KNOTS('',3,(#96314,#96315,#96316,#96317,#96318,
#96319,#96320,#96321,#96322,#96323),.UNSPECIFIED.,.F.,.F.,(4,1,1,1,1,1,
1,4),(40.8407044966672,41.2448169535326,42.2428239241627,43.2408308947928,
44.2388378654229,45.236844836053,46.2348518066831,47.1238898038468),
 .UNSPECIFIED.);
#4572=B_SPLINE_CURVE_WITH_KNOTS('',3,(#96328,#96329,#96330,#96331,#96332,
#96333,#96334,#96335,#96336,#96337),.UNSPECIFIED.,.F.,.F.,(4,1,1,1,1,1,
1,4),(34.5575191894877,35.5514817403644,36.5488175829166,37.5461534254689,
38.5434892680211,39.5408251105734,40.5381609531256,40.8407044966673),
 .UNSPECIFIED.);
#4573=B_SPLINE_CURVE_WITH_KNOTS('',3,(#96338,#96339,#96340,#96341,#96342,
#96343,#96344,#96345,#96346,#96347),.UNSPECIFIED.,.F.,.F.,(4,1,1,1,1,1,
1,4),(34.5575191894876,35.2567751297521,36.2547821003822,37.2527890710123,
38.2507960416424,39.2488030122724,40.2468099829025,40.8407044966672),
 .UNSPECIFIED.);
#4574=B_SPLINE_CURVE_WITH_KNOTS('',3,(#96352,#96353,#96354,#96355,#96356,
#96357,#96358,#96359,#96360,#96361,#96362),.UNSPECIFIED.,.F.,.F.,(4,1,1,
1,1,1,1,1,4),(28.2743338823081,28.5701308424987,29.5674666850509,30.5648025276032,
31.5621383701554,32.5594742127077,33.5568100552599,34.5541458978121,34.5575191894877),
 .UNSPECIFIED.);
#4575=B_SPLINE_CURVE_WITH_KNOTS('',3,(#96363,#96364,#96365,#96366,#96367,
#96368,#96369,#96370,#96371,#96372),.UNSPECIFIED.,.F.,.F.,(4,1,1,1,1,1,
1,4),(28.274333882308,29.2687333059716,30.2667402766016,31.2647472472317,
32.2627542178618,33.2607611884919,34.258768159122,34.5575191894876),
 .UNSPECIFIED.);
#4576=B_SPLINE_CURVE_WITH_KNOTS('',3,(#96377,#96378,#96379,#96380,#96381,
#96382,#96383,#96384,#96385,#96386),.UNSPECIFIED.,.F.,.F.,(4,1,1,1,1,1,
1,4),(21.9911485751285,22.5861157871852,23.5834516297375,24.5807874722897,
25.5781233148419,26.5754591573942,27.5727949999464,28.2743338823081),
 .UNSPECIFIED.);
#4577=B_SPLINE_CURVE_WITH_KNOTS('',3,(#96387,#96388,#96389,#96390,#96391,
#96392,#96393,#96394,#96395,#96396,#96397),.UNSPECIFIED.,.F.,.F.,(4,1,1,
1,1,1,1,1,4),(21.9911485751285,22.2826845115609,23.280691482191,24.2786984528211,
25.2767054234512,26.2747123940813,27.2727193647114,28.2707263353415,28.274333882308),
 .UNSPECIFIED.);
#4578=B_SPLINE_CURVE_WITH_KNOTS('',3,(#96402,#96403,#96404,#96405,#96406,
#96407,#96408,#96409,#96410,#96411),.UNSPECIFIED.,.F.,.F.,(4,1,1,1,1,1,
1,4),(15.7079632679489,16.6021007318718,17.599436574424,18.5967724169762,
19.5941082595285,20.5914441020807,21.588779944633,21.9911485751285),
 .UNSPECIFIED.);
#4579=B_SPLINE_CURVE_WITH_KNOTS('',3,(#96412,#96413,#96414,#96415,#96416,
#96417,#96418,#96419,#96420,#96421),.UNSPECIFIED.,.F.,.F.,(4,1,1,1,1,1,
1,4),(15.7079632679489,16.2946426877804,17.2926496584105,18.2906566290406,
19.2886635996707,20.2866705703008,21.2846775409308,21.9911485751285),
 .UNSPECIFIED.);
#4580=B_SPLINE_CURVE_WITH_KNOTS('',3,(#96424,#96425,#96426,#96427,#96428,
#96429,#96430,#96431,#96432,#96433,#96434,#96435,#96436,#96437,#96438,#96439,
#96440,#96441,#96442,#96443,#96444,#96445,#96446,#96447,#96448,#96449,#96450,
#96451,#96452,#96453,#96454,#96455,#96456,#96457,#96458,#96459,#96460,#96461,
#96462,#96463,#96464,#96465,#96466,#96467,#96468,#96469,#96470,#96471,#96472,
#96473,#96474,#96475,#96476,#96477,#96478,#96479,#96480,#96481,#96482,#96483,
#96484,#96485,#96486,#96487,#96488,#96489,#96490,#96491,#96492,#96493,#96494,
#96495,#96496,#96497,#96498,#96499,#96500,#96501,#96502,#96503,#96504,#96505,
#96506,#96507,#96508,#96509,#96510,#96511,#96512,#96513,#96514,#96515,#96516,
#96517,#96518,#96519,#96520,#96521,#96522,#96523,#96524,#96525,#96526,#96527,
#96528,#96529,#96530,#96531,#96532,#96533,#96534,#96535,#96536,#96537,#96538,
#96539,#96540,#96541,#96542,#96543,#96544,#96545,#96546,#96547,#96548,#96549,
#96550),.UNSPECIFIED.,.F.,.F.,(4,3,3,3,3,3,3,3,3,3,3,3,3,3,3,3,3,3,3,3,
3,3,3,3,3,3,3,3,3,3,3,3,3,3,3,3,3,3,3,3,3,3,4),(-0.996917990983956,-0.978871588953361,
-0.96111138213616,-0.951572166884024,-0.94788730271085,-0.928958746515757,
-0.909876465942473,-0.904936500084987,-0.901848009849201,-0.882541837721487,
-0.863353532865677,-0.850071733640713,-0.842096384739765,-0.838733342910066,
-0.836789934415749,-0.818254783653573,-0.798902591036692,-0.782735584954257,
-0.778204258927876,-0.774298497031817,-0.75473106557298,-0.734923369072796,
-0.7185841623989,-0.712646708603056,-0.709110058221935,-0.689189804001172,
-0.669566542377212,-0.649891129487148,-0.644972000047888,-0.641670824784499,
-0.621885476350888,-0.601705353300825,-0.588427767916722,-0.579820295317846,
-0.575107459303169,-0.554609906499435,-0.53420632583291,-0.514845498030454,
-0.510394870356688,-0.506773348856668,-0.495484670227998,-0.475532816008266,
-0.468408511919796),.UNSPECIFIED.);
#4581=B_SPLINE_CURVE_WITH_KNOTS('',3,(#96552,#96553,#96554,#96555,#96556,
#96557,#96558,#96559,#96560,#96561,#96562,#96563,#96564,#96565,#96566,#96567,
#96568,#96569,#96570,#96571,#96572,#96573,#96574,#96575,#96576,#96577,#96578,
#96579,#96580,#96581,#96582,#96583,#96584,#96585,#96586,#96587,#96588,#96589,
#96590,#96591,#96592,#96593,#96594,#96595,#96596,#96597,#96598,#96599,#96600,
#96601,#96602,#96603,#96604,#96605,#96606,#96607,#96608,#96609),
 .UNSPECIFIED.,.F.,.F.,(4,3,3,3,3,3,3,3,3,3,3,3,3,3,3,3,3,3,3,4),(-0.271362855059921,
-0.249815156703991,-0.228817954605844,-0.214757059032555,-0.202695986178297,
-0.199258382274391,-0.179079040584676,-0.172574372312687,-0.151002575773601,
-0.132127253801901,-0.128545223737615,-0.108660382312346,-0.0889046320299183,
-0.0695673553379917,-0.0643976613730527,-0.0611873083345303,-0.0424332578302701,
-0.0240014673407122,-0.00610701619818059,0.),.UNSPECIFIED.);
#4582=B_SPLINE_CURVE_WITH_KNOTS('',3,(#96612,#96613,#96614,#96615,#96616,
#96617,#96618,#96619,#96620,#96621,#96622,#96623,#96624,#96625,#96626,#96627,
#96628,#96629,#96630,#96631,#96632,#96633,#96634,#96635,#96636,#96637,#96638,
#96639,#96640,#96641,#96642,#96643,#96644,#96645,#96646,#96647,#96648,#96649,
#96650,#96651,#96652,#96653,#96654,#96655,#96656,#96657,#96658,#96659,#96660,
#96661,#96662,#96663,#96664,#96665,#96666,#96667,#96668,#96669,#96670,#96671,
#96672,#96673,#96674,#96675,#96676,#96677,#96678,#96679,#96680,#96681,#96682,
#96683,#96684,#96685,#96686,#96687,#96688,#96689,#96690,#96691,#96692,#96693,
#96694,#96695,#96696,#96697,#96698,#96699,#96700,#96701,#96702,#96703,#96704,
#96705,#96706,#96707,#96708,#96709,#96710,#96711,#96712,#96713,#96714),
 .UNSPECIFIED.,.F.,.F.,(4,3,3,3,3,3,3,3,3,3,3,3,3,3,3,3,3,3,3,3,3,3,3,3,
3,3,3,3,3,3,3,3,3,3,4),(-0.468408511919796,-0.449159592277506,-0.442679572366002,
-0.439139523917826,-0.418501747794262,-0.397540534942074,-0.376759689901926,
-0.369408338867191,-0.366188435771172,-0.344993296658329,-0.324164935680159,
-0.314417154781481,-0.302674036643168,-0.298303152413865,-0.294792657786698,
-0.273759483634418,-0.252453791079512,-0.23671297526563,-0.228622459040654,
-0.22484613779528,-0.221071692886511,-0.199520974492535,-0.177947952659577,
-0.156760757052952,-0.151824997028116,-0.148277425274246,-0.12652726456846,
-0.105236270462937,-0.0835127492652271,-0.0784406535722348,-0.0733870619889256,
-0.0516031153801045,-0.029512914496819,-0.0074997402847098,0.),
 .UNSPECIFIED.);
#4583=B_SPLINE_CURVE_WITH_KNOTS('',3,(#97143,#97144,#97145,#97146,#97147,
#97148,#97149,#97150),.UNSPECIFIED.,.F.,.F.,(4,1,1,1,1,4),(11.6154215191105,
12.6127573616628,13.610093204215,14.6074290467673,15.6047648893195,15.7079632679489),
 .UNSPECIFIED.);
#4584=B_SPLINE_CURVE_WITH_KNOTS('',3,(#97151,#97152,#97153,#97154,#97155,
#97156,#97157,#97158,#97159,#97160,#97161,#97162,#97163,#97164,#97165,#97166,
#97167,#97168,#97169,#97170,#97171,#97172,#97173,#97174,#97175,#97176,#97177,
#97178,#97179,#97180,#97181,#97182,#97183,#97184,#97185,#97186,#97187,#97188,
#97189,#97190,#97191,#97192,#97193,#97194,#97195,#97196,#97197,#97198,#97199,
#97200,#97201,#97202,#97203,#97204,#97205,#97206,#97207,#97208,#97209,#97210,
#97211,#97212,#97213,#97214,#97215,#97216,#97217,#97218,#97219,#97220,#97221,
#97222,#97223,#97224,#97225,#97226,#97227,#97228,#97229,#97230,#97231,#97232,
#97233,#97234,#97235),.UNSPECIFIED.,.F.,.F.,(4,3,3,3,3,3,3,3,3,3,3,3,3,
3,3,3,3,3,3,3,3,3,3,3,3,3,3,3,4),(-0.364629307890661,-0.350885759085945,
-0.329296488089375,-0.318978386270927,-0.313741431878983,-0.309365163672801,
-0.288042901568511,-0.272809238661881,-0.264006177467146,-0.26029818106468,
-0.239567096461013,-0.219346880276472,-0.206053559786221,-0.194876880502573,
-0.191399047668888,-0.171813366976952,-0.166173598315468,-0.145401898526034,
-0.126706873608775,-0.123379860192083,-0.103925496661725,-0.0845481894111439,
-0.065567586070534,-0.0621782887363481,-0.05894467115978,-0.0403543924373443,
-0.0220984153978596,-0.00442511140790438,0.),.UNSPECIFIED.);
#4585=B_SPLINE_CURVE_WITH_KNOTS('',3,(#97236,#97237,#97238,#97239,#97240,
#97241,#97242,#97243,#97244,#97245,#97246,#97247,#97248),.UNSPECIFIED.,
 .F.,.F.,(4,3,3,3,4),(-101.213804280572,-100.730920097777,-99.7335842552244,
-98.7362484126722,-98.3403213565322),.UNSPECIFIED.);
#4586=B_SPLINE_CURVE_WITH_KNOTS('',3,(#97251,#97252,#97253,#97254,#97255,
#97256,#97257,#97258,#97259),.UNSPECIFIED.,.F.,.F.,(4,1,1,1,1,1,4),(10.3757270560178,
11.30460783463,12.30261480526,13.3006217758901,14.2986287465202,15.2966357171503,
15.7079632679489),.UNSPECIFIED.);
#4587=B_SPLINE_CURVE_WITH_KNOTS('',3,(#97693,#97694,#97695,#97696,#97697,
#97698,#97699,#97700,#97701,#97702,#97703,#97704,#97705,#97706,#97707,#97708),
 .UNSPECIFIED.,.F.,.F.,(4,3,3,3,3,4),(95.3619706457233,95.8086691804886,
96.8066761511186,97.8046831217487,98.8026900923788,99.1486641472938),
 .UNSPECIFIED.);
#4588=B_SPLINE_CURVE_WITH_KNOTS('',3,(#97709,#97710,#97711,#97712,#97713,
#97714,#97715,#97716,#97717,#97718,#97719,#97720,#97721,#97722,#97723,#97724,
#97725,#97726,#97727,#97728,#97729,#97730,#97731,#97732,#97733,#97734,#97735,
#97736,#97737,#97738,#97739,#97740,#97741,#97742,#97743,#97744,#97745,#97746,
#97747,#97748,#97749,#97750,#97751,#97752,#97753,#97754,#97755,#97756,#97757,
#97758,#97759,#97760,#97761,#97762,#97763,#97764,#97765,#97766,#97767,#97768,
#97769,#97770,#97771,#97772,#97773,#97774,#97775,#97776,#97777,#97778,#97779,
#97780,#97781,#97782,#97783,#97784,#97785,#97786,#97787,#97788,#97789,#97790,
#97791,#97792,#97793),.UNSPECIFIED.,.F.,.F.,(4,3,3,3,3,3,3,3,3,3,3,3,3,
3,3,3,3,3,3,3,3,3,3,3,3,3,3,3,4),(-0.366397579005845,-0.355461226466819,
-0.337490969642209,-0.327214164040339,-0.321649482146298,-0.302840833811487,
-0.288386907394637,-0.281257238921911,-0.277593927902022,-0.258153123971634,
-0.238335729520815,-0.225554152759783,-0.218411056976172,-0.214856426708649,
-0.194426531587897,-0.187209422476688,-0.167504451243421,-0.156894426252658,
-0.149523127563347,-0.145921626399787,-0.125494957624892,-0.104619107174947,
-0.0835512936559854,-0.0752831225832569,-0.0721648689176682,-0.0505208253811386,
-0.028827309118007,-0.00759789023731293,0.),.UNSPECIFIED.);
#5446=LINE('',#95267,#6350);
#5447=LINE('',#95291,#6351);
#5448=LINE('',#95339,#6352);
#5449=LINE('',#95387,#6353);
#5450=LINE('',#95441,#6354);
#5451=LINE('',#95489,#6355);
#5452=LINE('',#95537,#6356);
#5453=LINE('',#95585,#6357);
#5454=LINE('',#95639,#6358);
#5455=LINE('',#95687,#6359);
#5456=LINE('',#95735,#6360);
#5457=LINE('',#95789,#6361);
#5458=LINE('',#95837,#6362);
#5459=LINE('',#95885,#6363);
#5460=LINE('',#95936,#6364);
#5461=LINE('',#95987,#6365);
#5462=LINE('',#96035,#6366);
#5463=LINE('',#96057,#6367);
#5464=LINE('',#96081,#6368);
#5465=LINE('',#96105,#6369);
#5466=LINE('',#96131,#6370);
#5467=LINE('',#96155,#6371);
#5468=LINE('',#96179,#6372);
#5469=LINE('',#96204,#6373);
#5470=LINE('',#96229,#6374);
#5471=LINE('',#96253,#6375);
#5472=LINE('',#96278,#6376);
#5473=LINE('',#96303,#6377);
#5474=LINE('',#96327,#6378);
#5475=LINE('',#96351,#6379);
#5476=LINE('',#96376,#6380);
#5477=LINE('',#96401,#6381);
#5478=LINE('',#96716,#6382);
#5479=LINE('',#97798,#6383);
#5480=LINE('',#97800,#6384);
#5481=LINE('',#97802,#6385);
#5482=LINE('',#97803,#6386);
#5483=LINE('',#97806,#6387);
#5484=LINE('',#97808,#6388);
#5485=LINE('',#97809,#6389);
#5486=LINE('',#97812,#6390);
#5487=LINE('',#97814,#6391);
#5488=LINE('',#97815,#6392);
#5489=LINE('',#97818,#6393);
#5490=LINE('',#97820,#6394);
#5491=LINE('',#97821,#6395);
#5492=LINE('',#97824,#6396);
#5493=LINE('',#97826,#6397);
#5494=LINE('',#97827,#6398);
#5495=LINE('',#97829,#6399);
#5496=LINE('',#97830,#6400);
#5497=LINE('',#97837,#6401);
#6350=VECTOR('',#22987,2.);
#6351=VECTOR('',#22992,2.);
#6352=VECTOR('',#22995,2.);
#6353=VECTOR('',#22998,2.);
#6354=VECTOR('',#23001,2.);
#6355=VECTOR('',#23004,2.);
#6356=VECTOR('',#23007,2.);
#6357=VECTOR('',#23010,2.);
#6358=VECTOR('',#23013,2.);
#6359=VECTOR('',#23016,2.);
#6360=VECTOR('',#23019,2.);
#6361=VECTOR('',#23022,2.);
#6362=VECTOR('',#23025,2.);
#6363=VECTOR('',#23028,2.);
#6364=VECTOR('',#23031,2.);
#6365=VECTOR('',#23034,2.);
#6366=VECTOR('',#23037,1.5555);
#6367=VECTOR('',#23042,1.5555);
#6368=VECTOR('',#23045,1.5555);
#6369=VECTOR('',#23048,1.5555);
#6370=VECTOR('',#23051,1.5555);
#6371=VECTOR('',#23054,1.5555);
#6372=VECTOR('',#23057,1.5555);
#6373=VECTOR('',#23060,1.5555);
#6374=VECTOR('',#23063,1.5555);
#6375=VECTOR('',#23066,1.5555);
#6376=VECTOR('',#23069,1.5555);
#6377=VECTOR('',#23072,1.5555);
#6378=VECTOR('',#23075,1.5555);
#6379=VECTOR('',#23078,1.5555);
#6380=VECTOR('',#23081,1.5555);
#6381=VECTOR('',#23084,1.5555);
#6382=VECTOR('',#23089,1.5);
#6383=VECTOR('',#23100,10.);
#6384=VECTOR('',#23101,10.);
#6385=VECTOR('',#23102,10.);
#6386=VECTOR('',#23103,10.);
#6387=VECTOR('',#23106,10.);
#6388=VECTOR('',#23107,10.);
#6389=VECTOR('',#23108,10.);
#6390=VECTOR('',#23111,10.);
#6391=VECTOR('',#23112,10.);
#6392=VECTOR('',#23113,10.);
#6393=VECTOR('',#23116,10.);
#6394=VECTOR('',#23117,10.);
#6395=VECTOR('',#23118,10.);
#6396=VECTOR('',#23121,10.);
#6397=VECTOR('',#23122,10.);
#6398=VECTOR('',#23123,10.);
#6399=VECTOR('',#23126,10.);
#6400=VECTOR('',#23127,10.);
#6401=VECTOR('',#23136,3.5);
#8117=VERTEX_POINT('',#95265);
#8118=VERTEX_POINT('',#95266);
#8119=VERTEX_POINT('',#95268);
#8120=VERTEX_POINT('',#95279);
#8121=VERTEX_POINT('',#95289);
#8122=VERTEX_POINT('',#95290);
#8123=VERTEX_POINT('',#95337);
#8124=VERTEX_POINT('',#95338);
#8125=VERTEX_POINT('',#95385);
#8126=VERTEX_POINT('',#95386);
#8127=VERTEX_POINT('',#95439);
#8128=VERTEX_POINT('',#95440);
#8129=VERTEX_POINT('',#95487);
#8130=VERTEX_POINT('',#95488);
#8131=VERTEX_POINT('',#95535);
#8132=VERTEX_POINT('',#95536);
#8133=VERTEX_POINT('',#95583);
#8134=VERTEX_POINT('',#95584);
#8135=VERTEX_POINT('',#95637);
#8136=VERTEX_POINT('',#95638);
#8137=VERTEX_POINT('',#95685);
#8138=VERTEX_POINT('',#95686);
#8139=VERTEX_POINT('',#95733);
#8140=VERTEX_POINT('',#95734);
#8141=VERTEX_POINT('',#95787);
#8142=VERTEX_POINT('',#95788);
#8143=VERTEX_POINT('',#95835);
#8144=VERTEX_POINT('',#95836);
#8145=VERTEX_POINT('',#95883);
#8146=VERTEX_POINT('',#95884);
#8147=VERTEX_POINT('',#95934);
#8148=VERTEX_POINT('',#95935);
#8149=VERTEX_POINT('',#95985);
#8150=VERTEX_POINT('',#95986);
#8151=VERTEX_POINT('',#96033);
#8152=VERTEX_POINT('',#96034);
#8153=VERTEX_POINT('',#96036);
#8154=VERTEX_POINT('',#96045);
#8155=VERTEX_POINT('',#96055);
#8156=VERTEX_POINT('',#96056);
#8157=VERTEX_POINT('',#96079);
#8158=VERTEX_POINT('',#96080);
#8159=VERTEX_POINT('',#96103);
#8160=VERTEX_POINT('',#96104);
#8161=VERTEX_POINT('',#96129);
#8162=VERTEX_POINT('',#96130);
#8163=VERTEX_POINT('',#96153);
#8164=VERTEX_POINT('',#96154);
#8165=VERTEX_POINT('',#96177);
#8166=VERTEX_POINT('',#96178);
#8167=VERTEX_POINT('',#96202);
#8168=VERTEX_POINT('',#96203);
#8169=VERTEX_POINT('',#96227);
#8170=VERTEX_POINT('',#96228);
#8171=VERTEX_POINT('',#96251);
#8172=VERTEX_POINT('',#96252);
#8173=VERTEX_POINT('',#96276);
#8174=VERTEX_POINT('',#96277);
#8175=VERTEX_POINT('',#96301);
#8176=VERTEX_POINT('',#96302);
#8177=VERTEX_POINT('',#96325);
#8178=VERTEX_POINT('',#96326);
#8179=VERTEX_POINT('',#96349);
#8180=VERTEX_POINT('',#96350);
#8181=VERTEX_POINT('',#96374);
#8182=VERTEX_POINT('',#96375);
#8183=VERTEX_POINT('',#96399);
#8184=VERTEX_POINT('',#96400);
#8185=VERTEX_POINT('',#96423);
#8186=VERTEX_POINT('',#96551);
#8187=VERTEX_POINT('',#96610);
#8188=VERTEX_POINT('',#96715);
#8189=VERTEX_POINT('',#97142);
#8190=VERTEX_POINT('',#97250);
#8191=VERTEX_POINT('',#97796);
#8192=VERTEX_POINT('',#97797);
#8193=VERTEX_POINT('',#97799);
#8194=VERTEX_POINT('',#97801);
#8195=VERTEX_POINT('',#97805);
#8196=VERTEX_POINT('',#97807);
#8197=VERTEX_POINT('',#97811);
#8198=VERTEX_POINT('',#97813);
#8199=VERTEX_POINT('',#97817);
#8200=VERTEX_POINT('',#97819);
#8201=VERTEX_POINT('',#97823);
#8202=VERTEX_POINT('',#97825);
#8203=VERTEX_POINT('',#97833);
#8204=VERTEX_POINT('',#97836);
#10801=EDGE_CURVE('',#8117,#8118,#5446,.T.);
#10802=EDGE_CURVE('',#8117,#8119,#4516,.T.);
#10803=EDGE_CURVE('',#8119,#8120,#3098,.F.);
#10804=EDGE_CURVE('',#8120,#8118,#4517,.T.);
#10805=EDGE_CURVE('',#8121,#8122,#5447,.T.);
#10806=EDGE_CURVE('',#8121,#8117,#4518,.T.);
#10807=EDGE_CURVE('',#8118,#8122,#4519,.T.);
#10808=EDGE_CURVE('',#8123,#8124,#5448,.T.);
#10809=EDGE_CURVE('',#8123,#8121,#4520,.T.);
#10810=EDGE_CURVE('',#8122,#8124,#4521,.T.);
#10811=EDGE_CURVE('',#8125,#8126,#5449,.T.);
#10812=EDGE_CURVE('',#8125,#8123,#4522,.T.);
#10813=EDGE_CURVE('',#8124,#8126,#4523,.T.);
#10814=EDGE_CURVE('',#8127,#8128,#5450,.T.);
#10815=EDGE_CURVE('',#8127,#8125,#4524,.T.);
#10816=EDGE_CURVE('',#8126,#8128,#4525,.T.);
#10817=EDGE_CURVE('',#8129,#8130,#5451,.T.);
#10818=EDGE_CURVE('',#8129,#8127,#4526,.T.);
#10819=EDGE_CURVE('',#8128,#8130,#4527,.T.);
#10820=EDGE_CURVE('',#8131,#8132,#5452,.T.);
#10821=EDGE_CURVE('',#8131,#8129,#4528,.T.);
#10822=EDGE_CURVE('',#8130,#8132,#4529,.T.);
#10823=EDGE_CURVE('',#8133,#8134,#5453,.T.);
#10824=EDGE_CURVE('',#8133,#8131,#4530,.T.);
#10825=EDGE_CURVE('',#8132,#8134,#4531,.T.);
#10826=EDGE_CURVE('',#8135,#8136,#5454,.T.);
#10827=EDGE_CURVE('',#8135,#8133,#4532,.T.);
#10828=EDGE_CURVE('',#8134,#8136,#4533,.T.);
#10829=EDGE_CURVE('',#8137,#8138,#5455,.T.);
#10830=EDGE_CURVE('',#8137,#8135,#4534,.T.);
#10831=EDGE_CURVE('',#8136,#8138,#4535,.T.);
#10832=EDGE_CURVE('',#8139,#8140,#5456,.T.);
#10833=EDGE_CURVE('',#8139,#8137,#4536,.T.);
#10834=EDGE_CURVE('',#8138,#8140,#4537,.T.);
#10835=EDGE_CURVE('',#8141,#8142,#5457,.T.);
#10836=EDGE_CURVE('',#8141,#8139,#4538,.T.);
#10837=EDGE_CURVE('',#8140,#8142,#4539,.T.);
#10838=EDGE_CURVE('',#8143,#8144,#5458,.T.);
#10839=EDGE_CURVE('',#8143,#8141,#4540,.T.);
#10840=EDGE_CURVE('',#8142,#8144,#4541,.T.);
#10841=EDGE_CURVE('',#8145,#8146,#5459,.T.);
#10842=EDGE_CURVE('',#8145,#8143,#4542,.T.);
#10843=EDGE_CURVE('',#8144,#8146,#4543,.T.);
#10844=EDGE_CURVE('',#8147,#8148,#5460,.T.);
#10845=EDGE_CURVE('',#8147,#8145,#4544,.T.);
#10846=EDGE_CURVE('',#8146,#8148,#4545,.T.);
#10847=EDGE_CURVE('',#8149,#8150,#5461,.T.);
#10848=EDGE_CURVE('',#8149,#8147,#4546,.T.);
#10849=EDGE_CURVE('',#8148,#8150,#4547,.T.);
#10850=EDGE_CURVE('',#8151,#8152,#5462,.T.);
#10851=EDGE_CURVE('',#8151,#8153,#4548,.T.);
#10852=EDGE_CURVE('',#8153,#8154,#3099,.T.);
#10853=EDGE_CURVE('',#8152,#8154,#4549,.T.);
#10854=EDGE_CURVE('',#8155,#8156,#5463,.T.);
#10855=EDGE_CURVE('',#8155,#8151,#4550,.T.);
#10856=EDGE_CURVE('',#8156,#8152,#4551,.T.);
#10857=EDGE_CURVE('',#8157,#8158,#5464,.T.);
#10858=EDGE_CURVE('',#8157,#8155,#4552,.T.);
#10859=EDGE_CURVE('',#8158,#8156,#4553,.T.);
#10860=EDGE_CURVE('',#8159,#8160,#5465,.T.);
#10861=EDGE_CURVE('',#8159,#8157,#4554,.T.);
#10862=EDGE_CURVE('',#8160,#8158,#4555,.T.);
#10863=EDGE_CURVE('',#8161,#8162,#5466,.T.);
#10864=EDGE_CURVE('',#8161,#8159,#4556,.T.);
#10865=EDGE_CURVE('',#8162,#8160,#4557,.T.);
#10866=EDGE_CURVE('',#8163,#8164,#5467,.T.);
#10867=EDGE_CURVE('',#8163,#8161,#4558,.T.);
#10868=EDGE_CURVE('',#8164,#8162,#4559,.T.);
#10869=EDGE_CURVE('',#8165,#8166,#5468,.T.);
#10870=EDGE_CURVE('',#8165,#8163,#4560,.T.);
#10871=EDGE_CURVE('',#8166,#8164,#4561,.T.);
#10872=EDGE_CURVE('',#8167,#8168,#5469,.T.);
#10873=EDGE_CURVE('',#8167,#8165,#4562,.T.);
#10874=EDGE_CURVE('',#8168,#8166,#4563,.T.);
#10875=EDGE_CURVE('',#8169,#8170,#5470,.T.);
#10876=EDGE_CURVE('',#8169,#8167,#4564,.T.);
#10877=EDGE_CURVE('',#8170,#8168,#4565,.T.);
#10878=EDGE_CURVE('',#8171,#8172,#5471,.T.);
#10879=EDGE_CURVE('',#8171,#8169,#4566,.T.);
#10880=EDGE_CURVE('',#8172,#8170,#4567,.T.);
#10881=EDGE_CURVE('',#8173,#8174,#5472,.T.);
#10882=EDGE_CURVE('',#8173,#8171,#4568,.T.);
#10883=EDGE_CURVE('',#8174,#8172,#4569,.T.);
#10884=EDGE_CURVE('',#8175,#8176,#5473,.T.);
#10885=EDGE_CURVE('',#8175,#8173,#4570,.T.);
#10886=EDGE_CURVE('',#8176,#8174,#4571,.T.);
#10887=EDGE_CURVE('',#8177,#8178,#5474,.T.);
#10888=EDGE_CURVE('',#8177,#8175,#4572,.T.);
#10889=EDGE_CURVE('',#8178,#8176,#4573,.T.);
#10890=EDGE_CURVE('',#8179,#8180,#5475,.T.);
#10891=EDGE_CURVE('',#8179,#8177,#4574,.T.);
#10892=EDGE_CURVE('',#8180,#8178,#4575,.T.);
#10893=EDGE_CURVE('',#8181,#8182,#5476,.T.);
#10894=EDGE_CURVE('',#8181,#8179,#4576,.T.);
#10895=EDGE_CURVE('',#8182,#8180,#4577,.T.);
#10896=EDGE_CURVE('',#8183,#8184,#5477,.T.);
#10897=EDGE_CURVE('',#8183,#8181,#4578,.T.);
#10898=EDGE_CURVE('',#8184,#8182,#4579,.T.);
#10899=EDGE_CURVE('',#8154,#8185,#4580,.T.);
#10900=EDGE_CURVE('',#8186,#8153,#4581,.T.);
#10901=EDGE_CURVE('',#8187,#8186,#3100,.T.);
#10902=EDGE_CURVE('',#8185,#8187,#4582,.T.);
#10903=EDGE_CURVE('',#8185,#8188,#5478,.T.);
#10904=EDGE_CURVE('',#8188,#8188,#3101,.T.);
#10905=EDGE_CURVE('',#8189,#8183,#4583,.T.);
#10906=EDGE_CURVE('',#8119,#8189,#4584,.T.);
#10907=EDGE_CURVE('',#8186,#8149,#4585,.T.);
#10908=EDGE_CURVE('',#8190,#8184,#4586,.T.);
#10909=EDGE_CURVE('',#8189,#8190,#3102,.T.);
#10910=EDGE_CURVE('',#8150,#8187,#4587,.T.);
#10911=EDGE_CURVE('',#8190,#8120,#4588,.T.);
#10912=EDGE_CURVE('',#8191,#8192,#5479,.T.);
#10913=EDGE_CURVE('',#8191,#8193,#5480,.T.);
#10914=EDGE_CURVE('',#8193,#8194,#5481,.T.);
#10915=EDGE_CURVE('',#8192,#8194,#5482,.T.);
#10916=EDGE_CURVE('',#8195,#8191,#5483,.T.);
#10917=EDGE_CURVE('',#8195,#8196,#5484,.T.);
#10918=EDGE_CURVE('',#8196,#8193,#5485,.T.);
#10919=EDGE_CURVE('',#8197,#8195,#5486,.T.);
#10920=EDGE_CURVE('',#8197,#8198,#5487,.T.);
#10921=EDGE_CURVE('',#8198,#8196,#5488,.T.);
#10922=EDGE_CURVE('',#8199,#8197,#5489,.T.);
#10923=EDGE_CURVE('',#8199,#8200,#5490,.T.);
#10924=EDGE_CURVE('',#8200,#8198,#5491,.T.);
#10925=EDGE_CURVE('',#8201,#8199,#5492,.T.);
#10926=EDGE_CURVE('',#8201,#8202,#5493,.T.);
#10927=EDGE_CURVE('',#8202,#8200,#5494,.T.);
#10928=EDGE_CURVE('',#8192,#8201,#5495,.T.);
#10929=EDGE_CURVE('',#8194,#8202,#5496,.T.);
#10930=EDGE_CURVE('',#8203,#8203,#3103,.T.);
#10931=EDGE_CURVE('',#8203,#8204,#5497,.T.);
#10932=EDGE_CURVE('',#8204,#8204,#3104,.T.);
#16098=ORIENTED_EDGE('',*,*,#10801,.F.);
#16099=ORIENTED_EDGE('',*,*,#10802,.T.);
#16100=ORIENTED_EDGE('',*,*,#10803,.T.);
#16101=ORIENTED_EDGE('',*,*,#10804,.T.);
#16102=ORIENTED_EDGE('',*,*,#10805,.F.);
#16103=ORIENTED_EDGE('',*,*,#10806,.T.);
#16104=ORIENTED_EDGE('',*,*,#10801,.T.);
#16105=ORIENTED_EDGE('',*,*,#10807,.T.);
#16106=ORIENTED_EDGE('',*,*,#10808,.F.);
#16107=ORIENTED_EDGE('',*,*,#10809,.T.);
#16108=ORIENTED_EDGE('',*,*,#10805,.T.);
#16109=ORIENTED_EDGE('',*,*,#10810,.T.);
#16110=ORIENTED_EDGE('',*,*,#10811,.F.);
#16111=ORIENTED_EDGE('',*,*,#10812,.T.);
#16112=ORIENTED_EDGE('',*,*,#10808,.T.);
#16113=ORIENTED_EDGE('',*,*,#10813,.T.);
#16114=ORIENTED_EDGE('',*,*,#10814,.F.);
#16115=ORIENTED_EDGE('',*,*,#10815,.T.);
#16116=ORIENTED_EDGE('',*,*,#10811,.T.);
#16117=ORIENTED_EDGE('',*,*,#10816,.T.);
#16118=ORIENTED_EDGE('',*,*,#10817,.F.);
#16119=ORIENTED_EDGE('',*,*,#10818,.T.);
#16120=ORIENTED_EDGE('',*,*,#10814,.T.);
#16121=ORIENTED_EDGE('',*,*,#10819,.T.);
#16122=ORIENTED_EDGE('',*,*,#10820,.F.);
#16123=ORIENTED_EDGE('',*,*,#10821,.T.);
#16124=ORIENTED_EDGE('',*,*,#10817,.T.);
#16125=ORIENTED_EDGE('',*,*,#10822,.T.);
#16126=ORIENTED_EDGE('',*,*,#10823,.F.);
#16127=ORIENTED_EDGE('',*,*,#10824,.T.);
#16128=ORIENTED_EDGE('',*,*,#10820,.T.);
#16129=ORIENTED_EDGE('',*,*,#10825,.T.);
#16130=ORIENTED_EDGE('',*,*,#10826,.F.);
#16131=ORIENTED_EDGE('',*,*,#10827,.T.);
#16132=ORIENTED_EDGE('',*,*,#10823,.T.);
#16133=ORIENTED_EDGE('',*,*,#10828,.T.);
#16134=ORIENTED_EDGE('',*,*,#10829,.F.);
#16135=ORIENTED_EDGE('',*,*,#10830,.T.);
#16136=ORIENTED_EDGE('',*,*,#10826,.T.);
#16137=ORIENTED_EDGE('',*,*,#10831,.T.);
#16138=ORIENTED_EDGE('',*,*,#10832,.F.);
#16139=ORIENTED_EDGE('',*,*,#10833,.T.);
#16140=ORIENTED_EDGE('',*,*,#10829,.T.);
#16141=ORIENTED_EDGE('',*,*,#10834,.T.);
#16142=ORIENTED_EDGE('',*,*,#10835,.F.);
#16143=ORIENTED_EDGE('',*,*,#10836,.T.);
#16144=ORIENTED_EDGE('',*,*,#10832,.T.);
#16145=ORIENTED_EDGE('',*,*,#10837,.T.);
#16146=ORIENTED_EDGE('',*,*,#10838,.F.);
#16147=ORIENTED_EDGE('',*,*,#10839,.T.);
#16148=ORIENTED_EDGE('',*,*,#10835,.T.);
#16149=ORIENTED_EDGE('',*,*,#10840,.T.);
#16150=ORIENTED_EDGE('',*,*,#10841,.F.);
#16151=ORIENTED_EDGE('',*,*,#10842,.T.);
#16152=ORIENTED_EDGE('',*,*,#10838,.T.);
#16153=ORIENTED_EDGE('',*,*,#10843,.T.);
#16154=ORIENTED_EDGE('',*,*,#10844,.F.);
#16155=ORIENTED_EDGE('',*,*,#10845,.T.);
#16156=ORIENTED_EDGE('',*,*,#10841,.T.);
#16157=ORIENTED_EDGE('',*,*,#10846,.T.);
#16158=ORIENTED_EDGE('',*,*,#10847,.F.);
#16159=ORIENTED_EDGE('',*,*,#10848,.T.);
#16160=ORIENTED_EDGE('',*,*,#10844,.T.);
#16161=ORIENTED_EDGE('',*,*,#10849,.T.);
#16162=ORIENTED_EDGE('',*,*,#10850,.F.);
#16163=ORIENTED_EDGE('',*,*,#10851,.T.);
#16164=ORIENTED_EDGE('',*,*,#10852,.T.);
#16165=ORIENTED_EDGE('',*,*,#10853,.F.);
#16166=ORIENTED_EDGE('',*,*,#10854,.F.);
#16167=ORIENTED_EDGE('',*,*,#10855,.T.);
#16168=ORIENTED_EDGE('',*,*,#10850,.T.);
#16169=ORIENTED_EDGE('',*,*,#10856,.F.);
#16170=ORIENTED_EDGE('',*,*,#10857,.F.);
#16171=ORIENTED_EDGE('',*,*,#10858,.T.);
#16172=ORIENTED_EDGE('',*,*,#10854,.T.);
#16173=ORIENTED_EDGE('',*,*,#10859,.F.);
#16174=ORIENTED_EDGE('',*,*,#10860,.F.);
#16175=ORIENTED_EDGE('',*,*,#10861,.T.);
#16176=ORIENTED_EDGE('',*,*,#10857,.T.);
#16177=ORIENTED_EDGE('',*,*,#10862,.F.);
#16178=ORIENTED_EDGE('',*,*,#10863,.F.);
#16179=ORIENTED_EDGE('',*,*,#10864,.T.);
#16180=ORIENTED_EDGE('',*,*,#10860,.T.);
#16181=ORIENTED_EDGE('',*,*,#10865,.F.);
#16182=ORIENTED_EDGE('',*,*,#10866,.F.);
#16183=ORIENTED_EDGE('',*,*,#10867,.T.);
#16184=ORIENTED_EDGE('',*,*,#10863,.T.);
#16185=ORIENTED_EDGE('',*,*,#10868,.F.);
#16186=ORIENTED_EDGE('',*,*,#10869,.F.);
#16187=ORIENTED_EDGE('',*,*,#10870,.T.);
#16188=ORIENTED_EDGE('',*,*,#10866,.T.);
#16189=ORIENTED_EDGE('',*,*,#10871,.F.);
#16190=ORIENTED_EDGE('',*,*,#10872,.F.);
#16191=ORIENTED_EDGE('',*,*,#10873,.T.);
#16192=ORIENTED_EDGE('',*,*,#10869,.T.);
#16193=ORIENTED_EDGE('',*,*,#10874,.F.);
#16194=ORIENTED_EDGE('',*,*,#10875,.F.);
#16195=ORIENTED_EDGE('',*,*,#10876,.T.);
#16196=ORIENTED_EDGE('',*,*,#10872,.T.);
#16197=ORIENTED_EDGE('',*,*,#10877,.F.);
#16198=ORIENTED_EDGE('',*,*,#10878,.F.);
#16199=ORIENTED_EDGE('',*,*,#10879,.T.);
#16200=ORIENTED_EDGE('',*,*,#10875,.T.);
#16201=ORIENTED_EDGE('',*,*,#10880,.F.);
#16202=ORIENTED_EDGE('',*,*,#10881,.F.);
#16203=ORIENTED_EDGE('',*,*,#10882,.T.);
#16204=ORIENTED_EDGE('',*,*,#10878,.T.);
#16205=ORIENTED_EDGE('',*,*,#10883,.F.);
#16206=ORIENTED_EDGE('',*,*,#10884,.F.);
#16207=ORIENTED_EDGE('',*,*,#10885,.T.);
#16208=ORIENTED_EDGE('',*,*,#10881,.T.);
#16209=ORIENTED_EDGE('',*,*,#10886,.F.);
#16210=ORIENTED_EDGE('',*,*,#10887,.F.);
#16211=ORIENTED_EDGE('',*,*,#10888,.T.);
#16212=ORIENTED_EDGE('',*,*,#10884,.T.);
#16213=ORIENTED_EDGE('',*,*,#10889,.F.);
#16214=ORIENTED_EDGE('',*,*,#10890,.F.);
#16215=ORIENTED_EDGE('',*,*,#10891,.T.);
#16216=ORIENTED_EDGE('',*,*,#10887,.T.);
#16217=ORIENTED_EDGE('',*,*,#10892,.F.);
#16218=ORIENTED_EDGE('',*,*,#10893,.F.);
#16219=ORIENTED_EDGE('',*,*,#10894,.T.);
#16220=ORIENTED_EDGE('',*,*,#10890,.T.);
#16221=ORIENTED_EDGE('',*,*,#10895,.F.);
#16222=ORIENTED_EDGE('',*,*,#10896,.F.);
#16223=ORIENTED_EDGE('',*,*,#10897,.T.);
#16224=ORIENTED_EDGE('',*,*,#10893,.T.);
#16225=ORIENTED_EDGE('',*,*,#10898,.F.);
#16226=ORIENTED_EDGE('',*,*,#10899,.F.);
#16227=ORIENTED_EDGE('',*,*,#10852,.F.);
#16228=ORIENTED_EDGE('',*,*,#10900,.F.);
#16229=ORIENTED_EDGE('',*,*,#10901,.F.);
#16230=ORIENTED_EDGE('',*,*,#10902,.F.);
#16231=ORIENTED_EDGE('',*,*,#10903,.T.);
#16232=ORIENTED_EDGE('',*,*,#10904,.F.);
#16233=ORIENTED_EDGE('',*,*,#10903,.F.);
#16234=ORIENTED_EDGE('',*,*,#10900,.T.);
#16235=ORIENTED_EDGE('',*,*,#10851,.F.);
#16236=ORIENTED_EDGE('',*,*,#10855,.F.);
#16237=ORIENTED_EDGE('',*,*,#10858,.F.);
#16238=ORIENTED_EDGE('',*,*,#10861,.F.);
#16239=ORIENTED_EDGE('',*,*,#10864,.F.);
#16240=ORIENTED_EDGE('',*,*,#10867,.F.);
#16241=ORIENTED_EDGE('',*,*,#10870,.F.);
#16242=ORIENTED_EDGE('',*,*,#10873,.F.);
#16243=ORIENTED_EDGE('',*,*,#10876,.F.);
#16244=ORIENTED_EDGE('',*,*,#10879,.F.);
#16245=ORIENTED_EDGE('',*,*,#10882,.F.);
#16246=ORIENTED_EDGE('',*,*,#10885,.F.);
#16247=ORIENTED_EDGE('',*,*,#10888,.F.);
#16248=ORIENTED_EDGE('',*,*,#10891,.F.);
#16249=ORIENTED_EDGE('',*,*,#10894,.F.);
#16250=ORIENTED_EDGE('',*,*,#10897,.F.);
#16251=ORIENTED_EDGE('',*,*,#10905,.F.);
#16252=ORIENTED_EDGE('',*,*,#10906,.F.);
#16253=ORIENTED_EDGE('',*,*,#10802,.F.);
#16254=ORIENTED_EDGE('',*,*,#10806,.F.);
#16255=ORIENTED_EDGE('',*,*,#10809,.F.);
#16256=ORIENTED_EDGE('',*,*,#10812,.F.);
#16257=ORIENTED_EDGE('',*,*,#10815,.F.);
#16258=ORIENTED_EDGE('',*,*,#10818,.F.);
#16259=ORIENTED_EDGE('',*,*,#10821,.F.);
#16260=ORIENTED_EDGE('',*,*,#10824,.F.);
#16261=ORIENTED_EDGE('',*,*,#10827,.F.);
#16262=ORIENTED_EDGE('',*,*,#10830,.F.);
#16263=ORIENTED_EDGE('',*,*,#10833,.F.);
#16264=ORIENTED_EDGE('',*,*,#10836,.F.);
#16265=ORIENTED_EDGE('',*,*,#10839,.F.);
#16266=ORIENTED_EDGE('',*,*,#10842,.F.);
#16267=ORIENTED_EDGE('',*,*,#10845,.F.);
#16268=ORIENTED_EDGE('',*,*,#10848,.F.);
#16269=ORIENTED_EDGE('',*,*,#10907,.F.);
#16270=ORIENTED_EDGE('',*,*,#10896,.T.);
#16271=ORIENTED_EDGE('',*,*,#10908,.F.);
#16272=ORIENTED_EDGE('',*,*,#10909,.F.);
#16273=ORIENTED_EDGE('',*,*,#10905,.T.);
#16274=ORIENTED_EDGE('',*,*,#10899,.T.);
#16275=ORIENTED_EDGE('',*,*,#10902,.T.);
#16276=ORIENTED_EDGE('',*,*,#10910,.F.);
#16277=ORIENTED_EDGE('',*,*,#10849,.F.);
#16278=ORIENTED_EDGE('',*,*,#10846,.F.);
#16279=ORIENTED_EDGE('',*,*,#10843,.F.);
#16280=ORIENTED_EDGE('',*,*,#10840,.F.);
#16281=ORIENTED_EDGE('',*,*,#10837,.F.);
#16282=ORIENTED_EDGE('',*,*,#10834,.F.);
#16283=ORIENTED_EDGE('',*,*,#10831,.F.);
#16284=ORIENTED_EDGE('',*,*,#10828,.F.);
#16285=ORIENTED_EDGE('',*,*,#10825,.F.);
#16286=ORIENTED_EDGE('',*,*,#10822,.F.);
#16287=ORIENTED_EDGE('',*,*,#10819,.F.);
#16288=ORIENTED_EDGE('',*,*,#10816,.F.);
#16289=ORIENTED_EDGE('',*,*,#10813,.F.);
#16290=ORIENTED_EDGE('',*,*,#10810,.F.);
#16291=ORIENTED_EDGE('',*,*,#10807,.F.);
#16292=ORIENTED_EDGE('',*,*,#10804,.F.);
#16293=ORIENTED_EDGE('',*,*,#10911,.F.);
#16294=ORIENTED_EDGE('',*,*,#10908,.T.);
#16295=ORIENTED_EDGE('',*,*,#10898,.T.);
#16296=ORIENTED_EDGE('',*,*,#10895,.T.);
#16297=ORIENTED_EDGE('',*,*,#10892,.T.);
#16298=ORIENTED_EDGE('',*,*,#10889,.T.);
#16299=ORIENTED_EDGE('',*,*,#10886,.T.);
#16300=ORIENTED_EDGE('',*,*,#10883,.T.);
#16301=ORIENTED_EDGE('',*,*,#10880,.T.);
#16302=ORIENTED_EDGE('',*,*,#10877,.T.);
#16303=ORIENTED_EDGE('',*,*,#10874,.T.);
#16304=ORIENTED_EDGE('',*,*,#10871,.T.);
#16305=ORIENTED_EDGE('',*,*,#10868,.T.);
#16306=ORIENTED_EDGE('',*,*,#10865,.T.);
#16307=ORIENTED_EDGE('',*,*,#10862,.T.);
#16308=ORIENTED_EDGE('',*,*,#10859,.T.);
#16309=ORIENTED_EDGE('',*,*,#10856,.T.);
#16310=ORIENTED_EDGE('',*,*,#10853,.T.);
#16311=ORIENTED_EDGE('',*,*,#10847,.T.);
#16312=ORIENTED_EDGE('',*,*,#10910,.T.);
#16313=ORIENTED_EDGE('',*,*,#10901,.T.);
#16314=ORIENTED_EDGE('',*,*,#10907,.T.);
#16315=ORIENTED_EDGE('',*,*,#10912,.F.);
#16316=ORIENTED_EDGE('',*,*,#10913,.T.);
#16317=ORIENTED_EDGE('',*,*,#10914,.T.);
#16318=ORIENTED_EDGE('',*,*,#10915,.F.);
#16319=ORIENTED_EDGE('',*,*,#10916,.F.);
#16320=ORIENTED_EDGE('',*,*,#10917,.T.);
#16321=ORIENTED_EDGE('',*,*,#10918,.T.);
#16322=ORIENTED_EDGE('',*,*,#10913,.F.);
#16323=ORIENTED_EDGE('',*,*,#10919,.F.);
#16324=ORIENTED_EDGE('',*,*,#10920,.T.);
#16325=ORIENTED_EDGE('',*,*,#10921,.T.);
#16326=ORIENTED_EDGE('',*,*,#10917,.F.);
#16327=ORIENTED_EDGE('',*,*,#10922,.F.);
#16328=ORIENTED_EDGE('',*,*,#10923,.T.);
#16329=ORIENTED_EDGE('',*,*,#10924,.T.);
#16330=ORIENTED_EDGE('',*,*,#10920,.F.);
#16331=ORIENTED_EDGE('',*,*,#10925,.F.);
#16332=ORIENTED_EDGE('',*,*,#10926,.T.);
#16333=ORIENTED_EDGE('',*,*,#10927,.T.);
#16334=ORIENTED_EDGE('',*,*,#10923,.F.);
#16335=ORIENTED_EDGE('',*,*,#10928,.F.);
#16336=ORIENTED_EDGE('',*,*,#10915,.T.);
#16337=ORIENTED_EDGE('',*,*,#10929,.T.);
#16338=ORIENTED_EDGE('',*,*,#10926,.F.);
#16339=ORIENTED_EDGE('',*,*,#10929,.F.);
#16340=ORIENTED_EDGE('',*,*,#10914,.F.);
#16341=ORIENTED_EDGE('',*,*,#10918,.F.);
#16342=ORIENTED_EDGE('',*,*,#10921,.F.);
#16343=ORIENTED_EDGE('',*,*,#10924,.F.);
#16344=ORIENTED_EDGE('',*,*,#10927,.F.);
#16345=ORIENTED_EDGE('',*,*,#10930,.T.);
#16346=ORIENTED_EDGE('',*,*,#10906,.T.);
#16347=ORIENTED_EDGE('',*,*,#10909,.T.);
#16348=ORIENTED_EDGE('',*,*,#10911,.T.);
#16349=ORIENTED_EDGE('',*,*,#10803,.F.);
#16350=ORIENTED_EDGE('',*,*,#10930,.F.);
#16351=ORIENTED_EDGE('',*,*,#10931,.T.);
#16352=ORIENTED_EDGE('',*,*,#10932,.T.);
#16353=ORIENTED_EDGE('',*,*,#10931,.F.);
#16354=ORIENTED_EDGE('',*,*,#10932,.F.);
#16355=ORIENTED_EDGE('',*,*,#10912,.T.);
#16356=ORIENTED_EDGE('',*,*,#10928,.T.);
#16357=ORIENTED_EDGE('',*,*,#10925,.T.);
#16358=ORIENTED_EDGE('',*,*,#10922,.T.);
#16359=ORIENTED_EDGE('',*,*,#10919,.T.);
#16360=ORIENTED_EDGE('',*,*,#10916,.T.);
#16361=ORIENTED_EDGE('',*,*,#10904,.T.);
#17220=CYLINDRICAL_SURFACE('',#19648,1.954);
#17221=CYLINDRICAL_SURFACE('',#19650,1.954);
#17222=CYLINDRICAL_SURFACE('',#19651,1.954);
#17223=CYLINDRICAL_SURFACE('',#19652,1.954);
#17224=CYLINDRICAL_SURFACE('',#19653,1.954);
#17225=CYLINDRICAL_SURFACE('',#19654,1.954);
#17226=CYLINDRICAL_SURFACE('',#19655,1.954);
#17227=CYLINDRICAL_SURFACE('',#19656,1.954);
#17228=CYLINDRICAL_SURFACE('',#19657,1.954);
#17229=CYLINDRICAL_SURFACE('',#19658,1.954);
#17230=CYLINDRICAL_SURFACE('',#19659,1.954);
#17231=CYLINDRICAL_SURFACE('',#19660,1.954);
#17232=CYLINDRICAL_SURFACE('',#19661,1.954);
#17233=CYLINDRICAL_SURFACE('',#19662,1.954);
#17234=CYLINDRICAL_SURFACE('',#19663,1.954);
#17235=CYLINDRICAL_SURFACE('',#19664,1.954);
#17236=CYLINDRICAL_SURFACE('',#19665,1.5555);
#17237=CYLINDRICAL_SURFACE('',#19667,1.5555);
#17238=CYLINDRICAL_SURFACE('',#19668,1.5555);
#17239=CYLINDRICAL_SURFACE('',#19669,1.5555);
#17240=CYLINDRICAL_SURFACE('',#19670,1.5555);
#17241=CYLINDRICAL_SURFACE('',#19671,1.5555);
#17242=CYLINDRICAL_SURFACE('',#19672,1.5555);
#17243=CYLINDRICAL_SURFACE('',#19673,1.5555);
#17244=CYLINDRICAL_SURFACE('',#19674,1.5555);
#17245=CYLINDRICAL_SURFACE('',#19675,1.5555);
#17246=CYLINDRICAL_SURFACE('',#19676,1.5555);
#17247=CYLINDRICAL_SURFACE('',#19677,1.5555);
#17248=CYLINDRICAL_SURFACE('',#19678,1.5555);
#17249=CYLINDRICAL_SURFACE('',#19679,1.5555);
#17250=CYLINDRICAL_SURFACE('',#19680,1.5555);
#17251=CYLINDRICAL_SURFACE('',#19681,1.5555);
#17252=CYLINDRICAL_SURFACE('',#19685,1.5555);
#17253=CYLINDRICAL_SURFACE('',#19687,1.954);
#17254=CYLINDRICAL_SURFACE('',#19697,3.5);
#18190=ADVANCED_FACE('',(#1592),#17220,.T.);
#18191=ADVANCED_FACE('',(#1593),#17221,.T.);
#18192=ADVANCED_FACE('',(#1594),#17222,.T.);
#18193=ADVANCED_FACE('',(#1595),#17223,.T.);
#18194=ADVANCED_FACE('',(#1596),#17224,.T.);
#18195=ADVANCED_FACE('',(#1597),#17225,.T.);
#18196=ADVANCED_FACE('',(#1598),#17226,.T.);
#18197=ADVANCED_FACE('',(#1599),#17227,.T.);
#18198=ADVANCED_FACE('',(#1600),#17228,.T.);
#18199=ADVANCED_FACE('',(#1601),#17229,.T.);
#18200=ADVANCED_FACE('',(#1602),#17230,.T.);
#18201=ADVANCED_FACE('',(#1603),#17231,.T.);
#18202=ADVANCED_FACE('',(#1604),#17232,.T.);
#18203=ADVANCED_FACE('',(#1605),#17233,.T.);
#18204=ADVANCED_FACE('',(#1606),#17234,.T.);
#18205=ADVANCED_FACE('',(#1607),#17235,.T.);
#18206=ADVANCED_FACE('',(#1608),#17236,.T.);
#18207=ADVANCED_FACE('',(#1609),#17237,.T.);
#18208=ADVANCED_FACE('',(#1610),#17238,.T.);
#18209=ADVANCED_FACE('',(#1611),#17239,.T.);
#18210=ADVANCED_FACE('',(#1612),#17240,.T.);
#18211=ADVANCED_FACE('',(#1613),#17241,.T.);
#18212=ADVANCED_FACE('',(#1614),#17242,.T.);
#18213=ADVANCED_FACE('',(#1615),#17243,.T.);
#18214=ADVANCED_FACE('',(#1616),#17244,.T.);
#18215=ADVANCED_FACE('',(#1617),#17245,.T.);
#18216=ADVANCED_FACE('',(#1618),#17246,.T.);
#18217=ADVANCED_FACE('',(#1619),#17247,.T.);
#18218=ADVANCED_FACE('',(#1620),#17248,.T.);
#18219=ADVANCED_FACE('',(#1621),#17249,.T.);
#18220=ADVANCED_FACE('',(#1622),#17250,.T.);
#18221=ADVANCED_FACE('',(#1623),#17251,.T.);
#18222=ADVANCED_FACE('',(#1624),#253,.T.);
#18223=ADVANCED_FACE('',(#1625),#671,.F.);
#18224=ADVANCED_FACE('',(#1626),#17252,.T.);
#18225=ADVANCED_FACE('',(#1627),#672,.F.);
#18226=ADVANCED_FACE('',(#1628),#17253,.T.);
#18227=ADVANCED_FACE('',(#1629),#594,.F.);
#18228=ADVANCED_FACE('',(#1630),#595,.F.);
#18229=ADVANCED_FACE('',(#1631),#596,.F.);
#18230=ADVANCED_FACE('',(#1632),#597,.F.);
#18231=ADVANCED_FACE('',(#1633),#598,.F.);
#18232=ADVANCED_FACE('',(#1634),#599,.F.);
#18233=ADVANCED_FACE('',(#1635),#600,.F.);
#18234=ADVANCED_FACE('',(#1636,#437),#601,.T.);
#18235=ADVANCED_FACE('',(#1637),#17254,.T.);
#18236=ADVANCED_FACE('',(#1638,#438),#602,.F.);
#18237=ADVANCED_FACE('',(#1639),#603,.T.);
#18284=CLOSED_SHELL('',(#18190,#18191,#18192,#18193,#18194,#18195,#18196,
#18197,#18198,#18199,#18200,#18201,#18202,#18203,#18204,#18205,#18206,#18207,
#18208,#18209,#18210,#18211,#18212,#18213,#18214,#18215,#18216,#18217,#18218,
#18219,#18220,#18221,#18222,#18223,#18224,#18225,#18226,#18227,#18228,#18229,
#18230,#18231,#18232,#18233,#18234,#18235,#18236,#18237));
#19647=AXIS2_PLACEMENT_3D('',#95263,#22983,#22984);
#19648=AXIS2_PLACEMENT_3D('',#95264,#22985,#22986);
#19649=AXIS2_PLACEMENT_3D('',#95280,#22988,#22989);
#19650=AXIS2_PLACEMENT_3D('',#95288,#22990,#22991);
#19651=AXIS2_PLACEMENT_3D('',#95336,#22993,#22994);
#19652=AXIS2_PLACEMENT_3D('',#95384,#22996,#22997);
#19653=AXIS2_PLACEMENT_3D('',#95438,#22999,#23000);
#19654=AXIS2_PLACEMENT_3D('',#95486,#23002,#23003);
#19655=AXIS2_PLACEMENT_3D('',#95534,#23005,#23006);
#19656=AXIS2_PLACEMENT_3D('',#95582,#23008,#23009);
#19657=AXIS2_PLACEMENT_3D('',#95636,#23011,#23012);
#19658=AXIS2_PLACEMENT_3D('',#95684,#23014,#23015);
#19659=AXIS2_PLACEMENT_3D('',#95732,#23017,#23018);
#19660=AXIS2_PLACEMENT_3D('',#95786,#23020,#23021);
#19661=AXIS2_PLACEMENT_3D('',#95834,#23023,#23024);
#19662=AXIS2_PLACEMENT_3D('',#95882,#23026,#23027);
#19663=AXIS2_PLACEMENT_3D('',#95933,#23029,#23030);
#19664=AXIS2_PLACEMENT_3D('',#95984,#23032,#23033);
#19665=AXIS2_PLACEMENT_3D('',#96032,#23035,#23036);
#19666=AXIS2_PLACEMENT_3D('',#96046,#23038,#23039);
#19667=AXIS2_PLACEMENT_3D('',#96054,#23040,#23041);
#19668=AXIS2_PLACEMENT_3D('',#96078,#23043,#23044);
#19669=AXIS2_PLACEMENT_3D('',#96102,#23046,#23047);
#19670=AXIS2_PLACEMENT_3D('',#96128,#23049,#23050);
#19671=AXIS2_PLACEMENT_3D('',#96152,#23052,#23053);
#19672=AXIS2_PLACEMENT_3D('',#96176,#23055,#23056);
#19673=AXIS2_PLACEMENT_3D('',#96201,#23058,#23059);
#19674=AXIS2_PLACEMENT_3D('',#96226,#23061,#23062);
#19675=AXIS2_PLACEMENT_3D('',#96250,#23064,#23065);
#19676=AXIS2_PLACEMENT_3D('',#96275,#23067,#23068);
#19677=AXIS2_PLACEMENT_3D('',#96300,#23070,#23071);
#19678=AXIS2_PLACEMENT_3D('',#96324,#23073,#23074);
#19679=AXIS2_PLACEMENT_3D('',#96348,#23076,#23077);
#19680=AXIS2_PLACEMENT_3D('',#96373,#23079,#23080);
#19681=AXIS2_PLACEMENT_3D('',#96398,#23082,#23083);
#19682=AXIS2_PLACEMENT_3D('',#96422,#23085,#23086);
#19683=AXIS2_PLACEMENT_3D('',#96611,#23087,#23088);
#19684=AXIS2_PLACEMENT_3D('',#96717,#23090,#23091);
#19685=AXIS2_PLACEMENT_3D('',#97249,#23092,#23093);
#19686=AXIS2_PLACEMENT_3D('',#97260,#23094,#23095);
#19687=AXIS2_PLACEMENT_3D('',#97794,#23096,#23097);
#19688=AXIS2_PLACEMENT_3D('',#97795,#23098,#23099);
#19689=AXIS2_PLACEMENT_3D('',#97804,#23104,#23105);
#19690=AXIS2_PLACEMENT_3D('',#97810,#23109,#23110);
#19691=AXIS2_PLACEMENT_3D('',#97816,#23114,#23115);
#19692=AXIS2_PLACEMENT_3D('',#97822,#23119,#23120);
#19693=AXIS2_PLACEMENT_3D('',#97828,#23124,#23125);
#19694=AXIS2_PLACEMENT_3D('',#97831,#23128,#23129);
#19695=AXIS2_PLACEMENT_3D('',#97832,#23130,#23131);
#19696=AXIS2_PLACEMENT_3D('',#97834,#23132,#23133);
#19697=AXIS2_PLACEMENT_3D('',#97835,#23134,#23135);
#19698=AXIS2_PLACEMENT_3D('',#97838,#23137,#23138);
#19699=AXIS2_PLACEMENT_3D('',#97839,#23139,#23140);
#19700=AXIS2_PLACEMENT_3D('',#97840,#23141,#23142);
#22983=DIRECTION('axis',(0.,0.,1.));
#22984=DIRECTION('refdir',(1.,0.,0.));
#22985=DIRECTION('center_axis',(0.,0.,1.));
#22986=DIRECTION('ref_axis',(1.,0.,0.));
#22987=DIRECTION('',(0.,0.,-1.));
#22988=DIRECTION('center_axis',(0.,0.,-1.));
#22989=DIRECTION('ref_axis',(1.,0.,0.));
#22990=DIRECTION('center_axis',(0.,0.,1.));
#22991=DIRECTION('ref_axis',(1.,0.,0.));
#22992=DIRECTION('',(0.,0.,-1.));
#22993=DIRECTION('center_axis',(0.,0.,1.));
#22994=DIRECTION('ref_axis',(1.,0.,0.));
#22995=DIRECTION('',(0.,0.,-1.));
#22996=DIRECTION('center_axis',(0.,0.,1.));
#22997=DIRECTION('ref_axis',(1.,0.,0.));
#22998=DIRECTION('',(0.,0.,-1.));
#22999=DIRECTION('center_axis',(0.,0.,1.));
#23000=DIRECTION('ref_axis',(1.,0.,0.));
#23001=DIRECTION('',(0.,0.,-1.));
#23002=DIRECTION('center_axis',(0.,0.,1.));
#23003=DIRECTION('ref_axis',(1.,0.,0.));
#23004=DIRECTION('',(0.,0.,-1.));
#23005=DIRECTION('center_axis',(0.,0.,1.));
#23006=DIRECTION('ref_axis',(1.,0.,0.));
#23007=DIRECTION('',(0.,0.,-1.));
#23008=DIRECTION('center_axis',(0.,0.,1.));
#23009=DIRECTION('ref_axis',(1.,0.,0.));
#23010=DIRECTION('',(0.,0.,-1.));
#23011=DIRECTION('center_axis',(0.,0.,1.));
#23012=DIRECTION('ref_axis',(1.,0.,0.));
#23013=DIRECTION('',(0.,0.,-1.));
#23014=DIRECTION('center_axis',(0.,0.,1.));
#23015=DIRECTION('ref_axis',(1.,0.,0.));
#23016=DIRECTION('',(0.,0.,-1.));
#23017=DIRECTION('center_axis',(0.,0.,1.));
#23018=DIRECTION('ref_axis',(1.,0.,0.));
#23019=DIRECTION('',(0.,0.,-1.));
#23020=DIRECTION('center_axis',(0.,0.,1.));
#23021=DIRECTION('ref_axis',(1.,0.,0.));
#23022=DIRECTION('',(0.,0.,-1.));
#23023=DIRECTION('center_axis',(0.,0.,1.));
#23024=DIRECTION('ref_axis',(1.,0.,0.));
#23025=DIRECTION('',(0.,0.,-1.));
#23026=DIRECTION('center_axis',(0.,0.,1.));
#23027=DIRECTION('ref_axis',(1.,0.,0.));
#23028=DIRECTION('',(0.,0.,-1.));
#23029=DIRECTION('center_axis',(0.,0.,1.));
#23030=DIRECTION('ref_axis',(1.,0.,0.));
#23031=DIRECTION('',(0.,0.,-1.));
#23032=DIRECTION('center_axis',(0.,0.,1.));
#23033=DIRECTION('ref_axis',(1.,0.,0.));
#23034=DIRECTION('',(0.,0.,-1.));
#23035=DIRECTION('center_axis',(0.,0.,1.));
#23036=DIRECTION('ref_axis',(1.,1.29731060939901E-13,0.));
#23037=DIRECTION('',(0.,0.,1.));
#23038=DIRECTION('center_axis',(0.,0.,-1.));
#23039=DIRECTION('ref_axis',(1.,1.29731060939901E-13,0.));
#23040=DIRECTION('center_axis',(0.,0.,1.));
#23041=DIRECTION('ref_axis',(1.,1.29731060939901E-13,0.));
#23042=DIRECTION('',(0.,0.,1.));
#23043=DIRECTION('center_axis',(0.,0.,1.));
#23044=DIRECTION('ref_axis',(1.,1.29731060939901E-13,0.));
#23045=DIRECTION('',(0.,0.,1.));
#23046=DIRECTION('center_axis',(0.,0.,1.));
#23047=DIRECTION('ref_axis',(1.,1.29731060939901E-13,0.));
#23048=DIRECTION('',(0.,0.,1.));
#23049=DIRECTION('center_axis',(0.,0.,1.));
#23050=DIRECTION('ref_axis',(1.,1.29731060939901E-13,0.));
#23051=DIRECTION('',(0.,0.,1.));
#23052=DIRECTION('center_axis',(0.,0.,1.));
#23053=DIRECTION('ref_axis',(1.,1.29731060939901E-13,0.));
#23054=DIRECTION('',(0.,0.,1.));
#23055=DIRECTION('center_axis',(0.,0.,1.));
#23056=DIRECTION('ref_axis',(1.,1.29731060939901E-13,0.));
#23057=DIRECTION('',(0.,0.,1.));
#23058=DIRECTION('center_axis',(0.,0.,1.));
#23059=DIRECTION('ref_axis',(1.,1.29731060939901E-13,0.));
#23060=DIRECTION('',(0.,0.,1.));
#23061=DIRECTION('center_axis',(0.,0.,1.));
#23062=DIRECTION('ref_axis',(1.,1.29731060939901E-13,0.));
#23063=DIRECTION('',(0.,0.,1.));
#23064=DIRECTION('center_axis',(0.,0.,1.));
#23065=DIRECTION('ref_axis',(1.,1.29731060939901E-13,0.));
#23066=DIRECTION('',(0.,0.,1.));
#23067=DIRECTION('center_axis',(0.,0.,1.));
#23068=DIRECTION('ref_axis',(1.,1.29731060939901E-13,0.));
#23069=DIRECTION('',(0.,0.,1.));
#23070=DIRECTION('center_axis',(0.,0.,1.));
#23071=DIRECTION('ref_axis',(1.,1.29731060939901E-13,0.));
#23072=DIRECTION('',(0.,0.,1.));
#23073=DIRECTION('center_axis',(0.,0.,1.));
#23074=DIRECTION('ref_axis',(1.,1.29731060939901E-13,0.));
#23075=DIRECTION('',(0.,0.,1.));
#23076=DIRECTION('center_axis',(0.,0.,1.));
#23077=DIRECTION('ref_axis',(1.,1.29731060939901E-13,0.));
#23078=DIRECTION('',(0.,0.,1.));
#23079=DIRECTION('center_axis',(0.,0.,1.));
#23080=DIRECTION('ref_axis',(1.,1.29731060939901E-13,0.));
#23081=DIRECTION('',(0.,0.,1.));
#23082=DIRECTION('center_axis',(0.,0.,1.));
#23083=DIRECTION('ref_axis',(1.,1.29731060939901E-13,0.));
#23084=DIRECTION('',(0.,0.,1.));
#23085=DIRECTION('center_axis',(0.,0.,-1.));
#23086=DIRECTION('ref_axis',(1.,0.,0.));
#23087=DIRECTION('center_axis',(0.,0.,-1.));
#23088=DIRECTION('ref_axis',(1.,0.,0.));
#23089=DIRECTION('',(0.707106781186548,8.65956056235494E-17,0.707106781186547));
#23090=DIRECTION('center_axis',(0.,0.,1.));
#23091=DIRECTION('ref_axis',(1.,0.,0.));
#23092=DIRECTION('center_axis',(0.,0.,1.));
#23093=DIRECTION('ref_axis',(1.,1.29731060939901E-13,0.));
#23094=DIRECTION('center_axis',(0.,0.,-1.));
#23095=DIRECTION('ref_axis',(1.,1.29731060939901E-13,0.));
#23096=DIRECTION('center_axis',(0.,0.,1.));
#23097=DIRECTION('ref_axis',(1.,0.,0.));
#23098=DIRECTION('center_axis',(-1.60246890531964E-16,-1.,0.));
#23099=DIRECTION('ref_axis',(1.,-1.60246890531964E-16,0.));
#23100=DIRECTION('',(1.,-1.60246890531964E-16,0.));
#23101=DIRECTION('',(0.,0.,1.));
#23102=DIRECTION('',(1.,-1.60246890531964E-16,0.));
#23103=DIRECTION('',(0.,0.,1.));
#23104=DIRECTION('center_axis',(-0.866025403784439,-0.5,0.));
#23105=DIRECTION('ref_axis',(0.5,-0.866025403784439,0.));
#23106=DIRECTION('',(0.5,-0.866025403784439,0.));
#23107=DIRECTION('',(0.,0.,1.));
#23108=DIRECTION('',(0.5,-0.866025403784439,0.));
#23109=DIRECTION('center_axis',(-0.866025403784439,0.5,0.));
#23110=DIRECTION('ref_axis',(-0.5,-0.866025403784439,0.));
#23111=DIRECTION('',(-0.5,-0.866025403784439,0.));
#23112=DIRECTION('',(0.,0.,1.));
#23113=DIRECTION('',(-0.5,-0.866025403784439,0.));
#23114=DIRECTION('center_axis',(1.60246890531964E-16,1.,0.));
#23115=DIRECTION('ref_axis',(-1.,1.60246890531964E-16,0.));
#23116=DIRECTION('',(-1.,1.60246890531964E-16,0.));
#23117=DIRECTION('',(0.,0.,1.));
#23118=DIRECTION('',(-1.,1.60246890531964E-16,0.));
#23119=DIRECTION('center_axis',(0.866025403784439,0.5,0.));
#23120=DIRECTION('ref_axis',(-0.5,0.866025403784439,0.));
#23121=DIRECTION('',(-0.5,0.866025403784439,0.));
#23122=DIRECTION('',(0.,0.,1.));
#23123=DIRECTION('',(-0.5,0.866025403784439,0.));
#23124=DIRECTION('center_axis',(0.866025403784439,-0.5,0.));
#23125=DIRECTION('ref_axis',(0.5,0.866025403784439,0.));
#23126=DIRECTION('',(0.5,0.866025403784439,0.));
#23127=DIRECTION('',(0.5,0.866025403784439,0.));
#23128=DIRECTION('center_axis',(0.,0.,1.));
#23129=DIRECTION('ref_axis',(1.,0.,0.));
#23130=DIRECTION('center_axis',(0.,0.,1.));
#23131=DIRECTION('ref_axis',(1.,0.,0.));
#23132=DIRECTION('center_axis',(0.,0.,1.));
#23133=DIRECTION('ref_axis',(1.,0.,0.));
#23134=DIRECTION('center_axis',(0.,0.,1.));
#23135=DIRECTION('ref_axis',(1.,0.,0.));
#23136=DIRECTION('',(0.,0.,-1.));
#23137=DIRECTION('center_axis',(0.,0.,1.));
#23138=DIRECTION('ref_axis',(1.,0.,0.));
#23139=DIRECTION('center_axis',(0.,0.,1.));
#23140=DIRECTION('ref_axis',(1.,0.,0.));
#23141=DIRECTION('center_axis',(0.,0.,1.));
#23142=DIRECTION('ref_axis',(1.,0.,0.));
#95263=CARTESIAN_POINT('',(0.,0.,0.));
#95264=CARTESIAN_POINT('Origin',(0.,0.,0.));
#95265=CARTESIAN_POINT('',(-1.95633559071744,0.0012731057411345,0.225869692124231));
#95266=CARTESIAN_POINT('',(-1.95587799559821,0.00207186393275607,0.124130307875758));
#95267=CARTESIAN_POINT('',(-1.954,-2.39295984553393E-16,0.));
#95268=CARTESIAN_POINT('',(0.861525859670522,1.75382131162755,0.));
#95269=CARTESIAN_POINT('Ctrl Pts',(-1.95633559071744,0.0012731057411345,
0.225869692124231));
#95270=CARTESIAN_POINT('Ctrl Pts',(-1.95680032440099,0.0682557629313676,
0.222037301306047));
#95271=CARTESIAN_POINT('Ctrl Pts',(-1.95365903766855,0.135191473590706,
0.218204910487863));
#95272=CARTESIAN_POINT('Ctrl Pts',(-1.94676806606145,0.201735328972743,
0.214372519669679));
#95273=CARTESIAN_POINT('Ctrl Pts',(-1.88017193281744,0.844832371344698,
0.1773353028412));
#95274=CARTESIAN_POINT('Ctrl Pts',(-1.46336311091822,1.45133095416213,0.140298086012721));
#95275=CARTESIAN_POINT('Ctrl Pts',(-0.886884671668765,1.7445317403525,0.103260869184242));
#95276=CARTESIAN_POINT('Ctrl Pts',(-0.351138290053491,2.01701592986141,
0.0688405794561611));
#95277=CARTESIAN_POINT('Ctrl Pts',(0.322511385444639,2.01891139473935,0.0344202897280807));
#95278=CARTESIAN_POINT('Ctrl Pts',(0.863567639152679,1.75641488315944,2.92734586571086E-17));
#95279=CARTESIAN_POINT('',(-0.861525859670574,1.75382131162752,1.38777878078145E-16));
#95280=CARTESIAN_POINT('Origin',(0.,0.,0.));
#95281=CARTESIAN_POINT('Ctrl Pts',(-0.861525859670571,1.75382131162752,
2.28983498828939E-15));
#95282=CARTESIAN_POINT('Ctrl Pts',(-1.44496782441851,1.46721837385109,0.0370621399437224));
#95283=CARTESIAN_POINT('Ctrl Pts',(-1.8691020329229,0.869083656944534,0.0741242798874424));
#95284=CARTESIAN_POINT('Ctrl Pts',(-1.94380023116171,0.227435527544788,
0.111186419831163));
#95285=CARTESIAN_POINT('Ctrl Pts',(-1.95249630318745,0.152737362394887,
0.115501049179361));
#95286=CARTESIAN_POINT('Ctrl Pts',(-1.95645657185248,0.0774494727773659,
0.119815678527559));
#95287=CARTESIAN_POINT('Ctrl Pts',(-1.95587799559821,0.00207186393275607,
0.124130307875758));
#95288=CARTESIAN_POINT('Origin',(0.,0.,0.));
#95289=CARTESIAN_POINT('',(-1.95128203910989,0.000979727872364722,0.92586969212423));
#95290=CARTESIAN_POINT('',(-1.95118672945361,0.000916100096969453,0.824130307875757));
#95291=CARTESIAN_POINT('',(-1.954,-2.39295984553393E-16,0.));
#95292=CARTESIAN_POINT('Ctrl Pts',(-1.95128203910989,0.000979727872364722,
0.92586969212423));
#95293=CARTESIAN_POINT('Ctrl Pts',(-1.9524730612105,0.263901717292074,0.910927268943587));
#95294=CARTESIAN_POINT('Ctrl Pts',(-1.90305141123492,0.526394079969068,
0.895984845762944));
#95295=CARTESIAN_POINT('Ctrl Pts',(-1.80089049647467,0.766440059940591,
0.881042422582301));
#95296=CARTESIAN_POINT('Ctrl Pts',(-1.54766811710363,1.36143291361156,0.844005205753822));
#95297=CARTESIAN_POINT('Ctrl Pts',(-0.970428066964404,1.81852045762203,
0.806967988925342));
#95298=CARTESIAN_POINT('Ctrl Pts',(-0.333230591869142,1.92861999489257,
0.769930772096863));
#95299=CARTESIAN_POINT('Ctrl Pts',(0.30396688322612,2.0387195321631,0.732893555268385));
#95300=CARTESIAN_POINT('Ctrl Pts',(1.00112178327742,1.8018310626937,0.695856338439906));
#95301=CARTESIAN_POINT('Ctrl Pts',(1.43930998255098,1.32629143144902,0.658819121611426));
#95302=CARTESIAN_POINT('Ctrl Pts',(1.87749818182454,0.850751800204341,0.621781904782947));
#95303=CARTESIAN_POINT('Ctrl Pts',(2.05671968032037,0.136561007184397,0.584744687954468));
#95304=CARTESIAN_POINT('Ctrl Pts',(1.89499805994521,-0.489512382298273,
0.547707471125989));
#95305=CARTESIAN_POINT('Ctrl Pts',(1.73327643957006,-1.11558577178094,0.51067025429751));
#95306=CARTESIAN_POINT('Ctrl Pts',(1.23061170032392,-1.65354175772633,0.473633037469032));
#95307=CARTESIAN_POINT('Ctrl Pts',(0.616932989107385,-1.8573955796291,0.436595820640553));
#95308=CARTESIAN_POINT('Ctrl Pts',(0.00325427789084558,-2.06124940153187,
0.399558603812074));
#95309=CARTESIAN_POINT('Ctrl Pts',(-0.721438405296094,-1.93100105939202,
0.362521386983595));
#95310=CARTESIAN_POINT('Ctrl Pts',(-1.22559302459517,-1.52602913735885,
0.325484170155115));
#95311=CARTESIAN_POINT('Ctrl Pts',(-1.67758072371516,-1.1629613001496,0.29227934414482));
#95312=CARTESIAN_POINT('Ctrl Pts',(-1.95230901779331,-0.579081973692791,
0.259074518134526));
#95313=CARTESIAN_POINT('Ctrl Pts',(-1.95633559071744,0.0012731057411345,
0.225869692124231));
#95314=CARTESIAN_POINT('Ctrl Pts',(-1.95587799559821,0.00207186393275607,
0.124130307875758));
#95315=CARTESIAN_POINT('Ctrl Pts',(-1.95148667238412,-0.570034995103637,
0.15687781847128));
#95316=CARTESIAN_POINT('Ctrl Pts',(-1.68562951923343,-1.14731024226281,
0.189625329066803));
#95317=CARTESIAN_POINT('Ctrl Pts',(-1.2444215732779,-1.51113938431406,0.222372839662326));
#95318=CARTESIAN_POINT('Ctrl Pts',(-0.745082529182101,-1.92290462488019,
0.259434979606046));
#95319=CARTESIAN_POINT('Ctrl Pts',(-0.0211422530173012,-2.0612735641195,
0.296497119549767));
#95320=CARTESIAN_POINT('Ctrl Pts',(0.595334795120667,-1.86428772433344,
0.333559259493488));
#95321=CARTESIAN_POINT('Ctrl Pts',(1.21181184325864,-1.66730188454737,0.370621399437209));
#95322=CARTESIAN_POINT('Ctrl Pts',(1.72082566336977,-1.13496126573593,0.40768353938093));
#95323=CARTESIAN_POINT('Ctrl Pts',(1.8894870924304,-0.510370283185346,0.444745679324651));
#95324=CARTESIAN_POINT('Ctrl Pts',(2.05814852149104,0.114220699365238,0.481807819268372));
#95325=CARTESIAN_POINT('Ctrl Pts',(1.88645755950116,0.831062045654966,0.518869959212093));
#95326=CARTESIAN_POINT('Ctrl Pts',(1.45292142815886,1.31145007703775,0.555932099155814));
#95327=CARTESIAN_POINT('Ctrl Pts',(1.01938529681656,1.79183810842053,0.592994239099535));
#95328=CARTESIAN_POINT('Ctrl Pts',(0.324003996121834,2.03577282489637,0.630056379043256));
#95329=CARTESIAN_POINT('Ctrl Pts',(-0.314654015224673,1.93172336479658,
0.667118518986976));
#95330=CARTESIAN_POINT('Ctrl Pts',(-0.953312026571179,1.8276739046968,0.704180658930697));
#95331=CARTESIAN_POINT('Ctrl Pts',(-1.53524674856946,1.37564026802139,0.741242798874417));
#95332=CARTESIAN_POINT('Ctrl Pts',(-1.79395555636014,0.782560471576942,
0.778304938818138));
#95333=CARTESIAN_POINT('Ctrl Pts',(-1.90058212652462,0.538123240897563,
0.793580061837345));
#95334=CARTESIAN_POINT('Ctrl Pts',(-1.95230335199157,0.269726953471863,
0.808855184856551));
#95335=CARTESIAN_POINT('Ctrl Pts',(-1.95118672945361,0.000916100096969453,
0.824130307875757));
#95336=CARTESIAN_POINT('Origin',(0.,0.,0.));
#95337=CARTESIAN_POINT('',(-1.95279554503994,-0.00168121501241181,1.62586969212423));
#95338=CARTESIAN_POINT('',(-1.95287184048439,-0.001702989282844,1.52413030787576));
#95339=CARTESIAN_POINT('',(-1.954,-2.39295984553393E-16,0.));
#95340=CARTESIAN_POINT('Ctrl Pts',(-1.95279554503994,-0.00168121501241181,
1.62586969212423));
#95341=CARTESIAN_POINT('Ctrl Pts',(-1.94903656010943,0.455834752155161,
1.59981723658113));
#95342=CARTESIAN_POINT('Ctrl Pts',(-1.78856730317397,0.91572573117829,1.57376478103802));
#95343=CARTESIAN_POINT('Ctrl Pts',(-1.49500760249196,1.26316552728133,1.54771232549492));
#95344=CARTESIAN_POINT('Ctrl Pts',(-1.07767134532899,1.75709989142681,1.51067510866644));
#95345=CARTESIAN_POINT('Ctrl Pts',(-0.39135122029848,2.02376358702057,1.47363789183796));
#95346=CARTESIAN_POINT('Ctrl Pts',(0.249990333148566,1.94116955279127,1.43660067500948));
#95347=CARTESIAN_POINT('Ctrl Pts',(0.891331886595613,1.85857551856197,1.39956345818101));
#95348=CARTESIAN_POINT('Ctrl Pts',(1.4876948684592,1.42672375450961,1.36252624135253));
#95349=CARTESIAN_POINT('Ctrl Pts',(1.76626827046517,0.843167597229759,1.32548902452405));
#95350=CARTESIAN_POINT('Ctrl Pts',(2.04484167247113,0.259611439949913,1.28845180769557));
#95351=CARTESIAN_POINT('Ctrl Pts',(2.00562549461947,-0.475649110557425,
1.25141459086709));
#95352=CARTESIAN_POINT('Ctrl Pts',(1.66655969053473,-1.02626219289756,1.21437737403861));
#95353=CARTESIAN_POINT('Ctrl Pts',(1.32749388644999,-1.57687527523771,1.17734015721013));
#95354=CARTESIAN_POINT('Ctrl Pts',(0.688578456132156,-1.94284088941065,
1.14030294038165));
#95355=CARTESIAN_POINT('Ctrl Pts',(0.0420898544956178,-1.9567474659654,
1.10326572355317));
#95356=CARTESIAN_POINT('Ctrl Pts',(-0.604398747140919,-1.97065404252014,
1.06622850672469));
#95357=CARTESIAN_POINT('Ctrl Pts',(-1.25846052009616,-1.6325015814567,1.02919128989622));
#95358=CARTESIAN_POINT('Ctrl Pts',(-1.62088905227235,-1.09697626925925,
0.992154073067737));
#95359=CARTESIAN_POINT('Ctrl Pts',(-1.83709816073764,-0.777505145902677,
0.970059279419901));
#95360=CARTESIAN_POINT('Ctrl Pts',(-1.94952091996443,-0.387793032173158,
0.947964485772066));
#95361=CARTESIAN_POINT('Ctrl Pts',(-1.95128203910989,0.000979727872364722,
0.92586969212423));
#95362=CARTESIAN_POINT('Ctrl Pts',(-1.95118672945361,0.000916100096969453,
0.824130307875757));
#95363=CARTESIAN_POINT('Ctrl Pts',(-1.94959408276249,-0.382490737583375,
0.845917324800272));
#95364=CARTESIAN_POINT('Ctrl Pts',(-1.84051065227066,-0.766740948347571,
0.867704341724787));
#95365=CARTESIAN_POINT('Ctrl Pts',(-1.62993550876047,-1.0835175828476,0.889491358649302));
#95366=CARTESIAN_POINT('Ctrl Pts',(-1.27172375978704,-1.62238988461419,
0.926553498593023));
#95367=CARTESIAN_POINT('Ctrl Pts',(-0.619817368257128,-1.96600853193387,
0.963615638536743));
#95368=CARTESIAN_POINT('Ctrl Pts',(0.0271864367452719,-1.95701720127518,
1.00067777848046));
#95369=CARTESIAN_POINT('Ctrl Pts',(0.674190241747668,-1.94802587061648,
1.03773991842418));
#95370=CARTESIAN_POINT('Ctrl Pts',(1.31629146022255,-1.5864245619794,1.07480205836791));
#95371=CARTESIAN_POINT('Ctrl Pts',(1.65939903784035,-1.03781956343241,1.11186419831163));
#95372=CARTESIAN_POINT('Ctrl Pts',(2.00250661545815,-0.489214564885407,
1.14892633825535));
#95373=CARTESIAN_POINT('Ctrl Pts',(2.04662055221888,0.246394123571516,1.18598847819907));
#95374=CARTESIAN_POINT('Ctrl Pts',(1.77153295980734,0.832073910176122,1.22305061814279));
#95375=CARTESIAN_POINT('Ctrl Pts',(1.49644536739581,1.41775369678073,1.26011275808651));
#95376=CARTESIAN_POINT('Ctrl Pts',(0.902156245812001,1.85350458153303,1.29717489803023));
#95377=CARTESIAN_POINT('Ctrl Pts',(0.260864347694114,1.93974733338565,1.33423703797395));
#95378=CARTESIAN_POINT('Ctrl Pts',(-0.380427550423769,2.02599008523827,
1.37129917791767));
#95379=CARTESIAN_POINT('Ctrl Pts',(-1.06872222507573,1.76272470419122,1.40836131786139));
#95380=CARTESIAN_POINT('Ctrl Pts',(-1.48876654315921,1.27053027794487,1.44542345780511));
#95381=CARTESIAN_POINT('Ctrl Pts',(-1.78610829781436,0.922114770268632,
1.47165907449533));
#95382=CARTESIAN_POINT('Ctrl Pts',(-1.94903067523895,0.458983666015645,
1.49789469118554));
#95383=CARTESIAN_POINT('Ctrl Pts',(-1.95287184048439,-0.001702989282844,
1.52413030787576));
#95384=CARTESIAN_POINT('Origin',(0.,0.,0.));
#95385=CARTESIAN_POINT('',(-1.9571996697324,4.08272333451705E-5,2.32586969212423));
#95386=CARTESIAN_POINT('',(-1.95720915199432,4.37834080700025E-5,2.22413030787575));
#95387=CARTESIAN_POINT('',(-1.954,-2.39295984553393E-16,0.));
#95388=CARTESIAN_POINT('Ctrl Pts',(-1.9571996697324,4.08272333451412E-5,
2.32586969212423));
#95389=CARTESIAN_POINT('Ctrl Pts',(-1.9572003426898,0.00222795607483405,
2.32574442104715));
#95390=CARTESIAN_POINT('Ctrl Pts',(-1.95719699336635,0.00441508279392128,
2.32561914997006));
#95391=CARTESIAN_POINT('Ctrl Pts',(-1.95718961556757,0.00660219592375261,
2.32549387889298));
#95392=CARTESIAN_POINT('Ctrl Pts',(-1.9550083208942,0.653236559609951,2.2884566620645));
#95393=CARTESIAN_POINT('Ctrl Pts',(-1.60068669068514,1.29868304829585,2.25141944523602));
#95394=CARTESIAN_POINT('Ctrl Pts',(-1.05631192010051,1.64767712566922,2.21438222840754));
#95395=CARTESIAN_POINT('Ctrl Pts',(-0.511937149515876,1.9966712030426,2.17734501157906));
#95396=CARTESIAN_POINT('Ctrl Pts',(0.222490761444335,2.04921286910345,2.14030779475058));
#95397=CARTESIAN_POINT('Ctrl Pts',(0.811002035332165,1.78126653559889,2.10327057792211));
#95398=CARTESIAN_POINT('Ctrl Pts',(1.39951330921999,1.51332020209433,2.06623336109363));
#95399=CARTESIAN_POINT('Ctrl Pts',(1.84210794603544,0.92488586902436,2.02919614426515));
#95400=CARTESIAN_POINT('Ctrl Pts',(1.93631757329266,0.28514740055385,1.99215892743667));
#95401=CARTESIAN_POINT('Ctrl Pts',(2.03052720054988,-0.354591067916664,
1.95512171060819));
#95402=CARTESIAN_POINT('Ctrl Pts',(1.77635181824887,-1.04563367178771,1.91808449377971));
#95403=CARTESIAN_POINT('Ctrl Pts',(1.29006594271768,-1.47185755477259,1.88104727695123));
#95404=CARTESIAN_POINT('Ctrl Pts',(0.803780067186484,-1.89808143775746,
1.84401006012275));
#95405=CARTESIAN_POINT('Ctrl Pts',(0.0853836984250916,-2.05948659985616,
1.80697284329427));
#95406=CARTESIAN_POINT('Ctrl Pts',(-0.536487147273854,-1.88223703762279,
1.76993562646579));
#95407=CARTESIAN_POINT('Ctrl Pts',(-1.1583579929728,-1.70498747538942,1.73289840963732));
#95408=CARTESIAN_POINT('Ctrl Pts',(-1.68370331560931,-1.18908318882399,
1.69586119280884));
#95409=CARTESIAN_POINT('Ctrl Pts',(-1.87219978227984,-0.570528529192665,
1.65882397598036));
#95410=CARTESIAN_POINT('Ctrl Pts',(-1.92810540551016,-0.387073187246384,
1.64783921469498));
#95411=CARTESIAN_POINT('Ctrl Pts',(-1.95438048401311,-0.194588316428208,
1.63685445340961));
#95412=CARTESIAN_POINT('Ctrl Pts',(-1.95279554503994,-0.00168121501241192,
1.62586969212423));
#95413=CARTESIAN_POINT('Ctrl Pts',(-1.95287184048439,-0.00170298928284375,
1.52413030787576));
#95414=CARTESIAN_POINT('Ctrl Pts',(-1.95445695530526,-0.191812291650776,
1.53495683112926));
#95415=CARTESIAN_POINT('Ctrl Pts',(-1.92895173588402,-0.381505322742495,
1.54578335438277));
#95416=CARTESIAN_POINT('Ctrl Pts',(-1.87462310228398,-0.562548805321496,
1.55660987763628));
#95417=CARTESIAN_POINT('Ctrl Pts',(-1.68864138181028,-1.18230999089587,
1.59367201758));
#95418=CARTESIAN_POINT('Ctrl Pts',(-1.16488397934787,-1.70070889059895,
1.63073415752372));
#95419=CARTESIAN_POINT('Ctrl Pts',(-0.543243355780667,-1.88030816136644,
1.66779629746744));
#95420=CARTESIAN_POINT('Ctrl Pts',(0.0783972677865321,-2.05990743213392,
1.70485843741116));
#95421=CARTESIAN_POINT('Ctrl Pts',(0.797921112458524,-1.90070707396579,
1.74192057735488));
#95422=CARTESIAN_POINT('Ctrl Pts',(1.28577075941843,-1.47562399010748,1.7789827172986));
#95423=CARTESIAN_POINT('Ctrl Pts',(1.77362040637834,-1.05054090624917,1.81604485724232));
#95424=CARTESIAN_POINT('Ctrl Pts',(2.02979585562615,-0.359575096700667,
1.85310699718604));
#95425=CARTESIAN_POINT('Ctrl Pts',(1.93696313672928,0.28079594435252,1.89016913712977));
#95426=CARTESIAN_POINT('Ctrl Pts',(1.84413041783241,0.921166985405712,1.92723127707349));
#95427=CARTESIAN_POINT('Ctrl Pts',(1.40228953079084,1.51094325796358,1.96429341701721));
#95428=CARTESIAN_POINT('Ctrl Pts',(0.813813216582781,1.77999452248681,2.00135555696093));
#95429=CARTESIAN_POINT('Ctrl Pts',(0.225336902374724,2.04904578701004,2.03841769690465));
#95430=CARTESIAN_POINT('Ctrl Pts',(-0.509774838999831,1.99737204349863,
2.07547983684837));
#95431=CARTESIAN_POINT('Ctrl Pts',(-1.05482489992153,1.64864094185095,2.11254197679209));
#95432=CARTESIAN_POINT('Ctrl Pts',(-1.59987496084323,1.29990984020327,2.14960411673581));
#95433=CARTESIAN_POINT('Ctrl Pts',(-1.95486334131209,0.654121380419318,
2.18666625667953));
#95434=CARTESIAN_POINT('Ctrl Pts',(-1.95719765431867,0.0070607094029605,
2.22372839662325));
#95435=CARTESIAN_POINT('Ctrl Pts',(-1.95720609227958,0.00472174601940803,
2.22386236704075));
#95436=CARTESIAN_POINT('Ctrl Pts',(-1.95720992231195,0.00238276601260064,
2.22399633745825));
#95437=CARTESIAN_POINT('Ctrl Pts',(-1.95720915199432,4.37834080701142E-5,
2.22413030787575));
#95438=CARTESIAN_POINT('Origin',(0.,0.,0.));
#95439=CARTESIAN_POINT('',(-1.95267691385146,0.00165493661177622,3.02586969212423));
#95440=CARTESIAN_POINT('',(-1.95274315056508,0.00167675988910205,2.92413030787576));
#95441=CARTESIAN_POINT('',(-1.954,-2.39295984553393E-16,0.));
#95442=CARTESIAN_POINT('Ctrl Pts',(-1.95267691385146,0.00165493661177622,
3.02586969212423));
#95443=CARTESIAN_POINT('Ctrl Pts',(-1.95426560914452,0.198992208020636,
3.01463438868469));
#95444=CARTESIAN_POINT('Ctrl Pts',(-1.92675342506316,0.395896803504792,
3.00339908524515));
#95445=CARTESIAN_POINT('Ctrl Pts',(-1.86830808103941,0.583146374609883,
2.9921637818056));
#95446=CARTESIAN_POINT('Ctrl Pts',(-1.67564280138135,1.20041523640586,2.95512656497712));
#95447=CARTESIAN_POINT('Ctrl Pts',(-1.14682887836242,1.71276357431471,2.91808934814864));
#95448=CARTESIAN_POINT('Ctrl Pts',(-0.523776367443795,1.8858136432031,2.88105213132016));
#95449=CARTESIAN_POINT('Ctrl Pts',(0.0992761434748341,2.0588637120915,2.84401491449168));
#95450=CARTESIAN_POINT('Ctrl Pts',(0.816567242293159,1.89261551195942,2.80697769766321));
#95451=CARTESIAN_POINT('Ctrl Pts',(1.29996651882171,1.46312057934516,2.76994048083473));
#95452=CARTESIAN_POINT('Ctrl Pts',(1.78336579535026,1.03362564673089,2.73290326400625));
#95453=CARTESIAN_POINT('Ctrl Pts',(2.03287324958903,0.340883981634439,2.69586604717777));
#95454=CARTESIAN_POINT('Ctrl Pts',(1.93434974962867,-0.298204336020968,
2.65882883034929));
#95455=CARTESIAN_POINT('Ctrl Pts',(1.83582624966831,-0.937292653676373,
2.62179161352081));
#95456=CARTESIAN_POINT('Ctrl Pts',(1.38927179550881,-1.52272762389073,2.58475439669233));
#95457=CARTESIAN_POINT('Ctrl Pts',(0.798966206784796,-1.78669745083631,
2.54771717986385));
#95458=CARTESIAN_POINT('Ctrl Pts',(0.208660618060775,-2.05066727778188,
2.51067996303538));
#95459=CARTESIAN_POINT('Ctrl Pts',(-0.525396105227766,-1.99317196145866,
2.4736427462069));
#95460=CARTESIAN_POINT('Ctrl Pts',(-1.0674039873032,-1.6405131839538,2.43660552937842));
#95461=CARTESIAN_POINT('Ctrl Pts',(-1.60757863467609,-1.28904720517098,
2.39969358362702));
#95462=CARTESIAN_POINT('Ctrl Pts',(-1.95700137841649,-0.644411052866131,
2.36278163787563));
#95463=CARTESIAN_POINT('Ctrl Pts',(-1.9571996697324,4.08272333451705E-5,
2.32586969212423));
#95464=CARTESIAN_POINT('Ctrl Pts',(-1.95720915199432,4.37834080700025E-5,
2.22413030787575));
#95465=CARTESIAN_POINT('Ctrl Pts',(-1.95699681840184,-0.644683222376,2.26105847740198));
#95466=CARTESIAN_POINT('Ctrl Pts',(-1.60725113883781,-1.28960760246236,
2.2979866469282));
#95467=CARTESIAN_POINT('Ctrl Pts',(-1.06669244200308,-1.64098742623895,
2.33491481645442));
#95468=CARTESIAN_POINT('Ctrl Pts',(-0.524172671136578,-1.99364200861572,
2.37197695639814));
#95469=CARTESIAN_POINT('Ctrl Pts',(0.210547116140745,-2.05061829112049,
2.40903909634186));
#95470=CARTESIAN_POINT('Ctrl Pts',(0.800949322066953,-1.78581989384044,
2.44610123628558));
#95471=CARTESIAN_POINT('Ctrl Pts',(1.39135152799316,-1.52102149656038,2.4831633762293));
#95472=CARTESIAN_POINT('Ctrl Pts',(1.83743615256826,-0.934448419495488,
2.52022551617302));
#95473=CARTESIAN_POINT('Ctrl Pts',(1.93488676008295,-0.294763859316313,
2.55728765611674));
#95474=CARTESIAN_POINT('Ctrl Pts',(2.03233736759764,0.344920700862864,2.59434979606046));
#95475=CARTESIAN_POINT('Ctrl Pts',(1.78115395805193,1.03771674415633,2.63141193600418));
#95476=CARTESIAN_POINT('Ctrl Pts',(1.29638398231036,1.46630865646616,2.6684740759479));
#95477=CARTESIAN_POINT('Ctrl Pts',(0.811614006568792,1.894900568776,2.70553621589162));
#95478=CARTESIAN_POINT('Ctrl Pts',(0.0932574646313782,2.05928835010221,
2.74259835583535));
#95479=CARTESIAN_POINT('Ctrl Pts',(-0.529662765081927,1.88417882975093,
2.77966049577907));
#95480=CARTESIAN_POINT('Ctrl Pts',(-1.15258299479523,1.70906930939964,2.81672263572279));
#95481=CARTESIAN_POINT('Ctrl Pts',(-1.68006691228442,1.19446248737086,2.85378477566651));
#95482=CARTESIAN_POINT('Ctrl Pts',(-1.87051544101399,0.576059451476712,
2.89084691561023));
#95483=CARTESIAN_POINT('Ctrl Pts',(-1.92752575844056,0.390941962730205,
2.90194137969874));
#95484=CARTESIAN_POINT('Ctrl Pts',(-1.95433466869055,0.196523398123763,
2.91303584378725));
#95485=CARTESIAN_POINT('Ctrl Pts',(-1.95274315056508,0.00167675988910205,
2.92413030787576));
#95486=CARTESIAN_POINT('Origin',(0.,0.,0.));
#95487=CARTESIAN_POINT('',(-1.95135107115213,-0.00103745302926256,3.72586969212423));
#95488=CARTESIAN_POINT('',(-1.95125983814034,-0.000967513988672578,3.62413030787576));
#95489=CARTESIAN_POINT('',(-1.954,-2.39295984553393E-16,0.));
#95490=CARTESIAN_POINT('Ctrl Pts',(-1.95135107115213,-0.00103745302926256,
3.72586969212423));
#95491=CARTESIAN_POINT('Ctrl Pts',(-1.9494564270682,0.392108141373472,3.70352435632223));
#95492=CARTESIAN_POINT('Ctrl Pts',(-1.83428685915158,0.78627490539017,3.68117902052023));
#95493=CARTESIAN_POINT('Ctrl Pts',(-1.61345116677478,1.10788542383069,3.65883368471823));
#95494=CARTESIAN_POINT('Ctrl Pts',(-1.24741775852795,1.64095230684139,3.62179646788975));
#95495=CARTESIAN_POINT('Ctrl Pts',(-0.591089924893776,1.97468687095231,
3.58475925106126));
#95496=CARTESIAN_POINT('Ctrl Pts',(0.0552900452708404,1.95641963566092,
3.54772203423278));
#95497=CARTESIAN_POINT('Ctrl Pts',(0.701670015435453,1.93815240036952,3.51068481740431));
#95498=CARTESIAN_POINT('Ctrl Pts',(1.3381021221305,1.56788336567581,3.47364760057583));
#95499=CARTESIAN_POINT('Ctrl Pts',(1.6734455320356,1.01499499073225,3.43661038374735));
#95500=CARTESIAN_POINT('Ctrl Pts',(2.0087889419407,0.462106615788698,3.39957316691887));
#95501=CARTESIAN_POINT('Ctrl Pts',(2.04304365505584,-0.273401099404705,
3.36253595009039));
#95502=CARTESIAN_POINT('Ctrl Pts',(1.76053958557416,-0.855064411333041,
3.32549873326191));
#95503=CARTESIAN_POINT('Ctrl Pts',(1.47803551609248,-1.43672772326139,3.28846151643343));
#95504=CARTESIAN_POINT('Ctrl Pts',(0.878772664013962,-1.86454663192466,
3.25142429960495));
#95505=CARTESIAN_POINT('Ctrl Pts',(0.236888497103484,-1.94281203925035,
3.21438708277648));
#95506=CARTESIAN_POINT('Ctrl Pts',(-0.404995669806982,-2.02107744657604,
3.177349865948));
#95507=CARTESIAN_POINT('Ctrl Pts',(-1.08950115154941,-1.74978935256416,
3.14031264911952));
#95508=CARTESIAN_POINT('Ctrl Pts',(-1.50349557427203,-1.25305061271667,
3.10327543229104));
#95509=CARTESIAN_POINT('Ctrl Pts',(-1.79190407667273,-0.906998424134863,
3.0774735189021));
#95510=CARTESIAN_POINT('Ctrl Pts',(-1.94902846959061,-0.451530792879088,
3.05167160551317));
#95511=CARTESIAN_POINT('Ctrl Pts',(-1.95267691385146,0.00165493661177622,
3.02586969212423));
#95512=CARTESIAN_POINT('Ctrl Pts',(-1.95274315056508,0.00167675988910205,
2.92413030787576));
#95513=CARTESIAN_POINT('Ctrl Pts',(-1.94901804708373,-0.45438081105706,
2.95009798373097));
#95514=CARTESIAN_POINT('Ctrl Pts',(-1.78970412039892,-0.912783539307832,
2.97606565958618));
#95515=CARTESIAN_POINT('Ctrl Pts',(-1.49789482266332,-1.25975537577289,
3.00203333544139));
#95516=CARTESIAN_POINT('Ctrl Pts',(-1.08141253561316,-1.75496791736879,
3.03909547538511));
#95517=CARTESIAN_POINT('Ctrl Pts',(-0.3950348215429,-2.02319375080107,3.07615761532883));
#95518=CARTESIAN_POINT('Ctrl Pts',(0.246862437687336,-1.94157962588032,
3.11321975527255));
#95519=CARTESIAN_POINT('Ctrl Pts',(0.888759696917571,-1.85996550095957,
3.15028189521628));
#95520=CARTESIAN_POINT('Ctrl Pts',(1.48617650130778,-1.4285114176858,3.18734403516));
#95521=CARTESIAN_POINT('Ctrl Pts',(1.76548299529208,-0.84483270534745,3.22440617510372));
#95522=CARTESIAN_POINT('Ctrl Pts',(2.04478948927638,-0.261153993009101,
3.26146831504744));
#95523=CARTESIAN_POINT('Ctrl Pts',(2.00598567285476,0.474749348393822,3.29853045499116));
#95524=CARTESIAN_POINT('Ctrl Pts',(1.66684453569178,1.02581762536563,3.33559259493488));
#95525=CARTESIAN_POINT('Ctrl Pts',(1.3277033985288,1.57688590233743,3.3726547348786));
#95526=CARTESIAN_POINT('Ctrl Pts',(0.688224940624468,1.94311911487812,3.40971687482232));
#95527=CARTESIAN_POINT('Ctrl Pts',(0.0413041672205065,1.95677450731496,
3.44677901476604));
#95528=CARTESIAN_POINT('Ctrl Pts',(-0.605616606183457,1.9704298997518,3.48384115470976));
#95529=CARTESIAN_POINT('Ctrl Pts',(-1.25997969508704,1.63150747208479,3.52090329465349));
#95530=CARTESIAN_POINT('Ctrl Pts',(-1.62207261036362,1.09524104808107,3.55796543459721));
#95531=CARTESIAN_POINT('Ctrl Pts',(-1.83754705311226,0.776119342016343,
3.58002039235672));
#95532=CARTESIAN_POINT('Ctrl Pts',(-1.94952253842872,0.387114015523011,
3.60207535011624));
#95533=CARTESIAN_POINT('Ctrl Pts',(-1.95125983814034,-0.000967513988672578,
3.62413030787576));
#95534=CARTESIAN_POINT('Origin',(0.,0.,0.));
#95535=CARTESIAN_POINT('',(-1.95645574651684,-0.00107576288577632,4.42586969212423));
#95536=CARTESIAN_POINT('',(-1.95628130950281,-0.00119277919923279,4.32413030787576));
#95537=CARTESIAN_POINT('',(-1.954,-2.39295984553393E-16,0.));
#95538=CARTESIAN_POINT('Ctrl Pts',(-1.95645574651684,-0.00107576288577632,
4.42586969212423));
#95539=CARTESIAN_POINT('Ctrl Pts',(-1.95258201164419,0.583617837825317,
4.39241432395977));
#95540=CARTESIAN_POINT('Ctrl Pts',(-1.67312331125722,1.17152394520949,4.35895895579531));
#95541=CARTESIAN_POINT('Ctrl Pts',(-1.21525966387556,1.53420296221226,4.32550358763085));
#95542=CARTESIAN_POINT('Ctrl Pts',(-0.70837553387317,1.93571166257503,4.28846637080237));
#95543=CARTESIAN_POINT('Ctrl Pts',(0.0171598407939347,2.06118438706562,
4.25142915397389));
#95544=CARTESIAN_POINT('Ctrl Pts',(0.629444641593513,1.8532226587955,4.21439193714541));
#95545=CARTESIAN_POINT('Ctrl Pts',(1.24172944239309,1.64526093052537,4.17735472031693));
#95546=CARTESIAN_POINT('Ctrl Pts',(1.74076366932515,1.10386474949453,4.14031750348845));
#95547=CARTESIAN_POINT('Ctrl Pts',(1.89826022128925,0.476700023258525,4.10328028665997));
#95548=CARTESIAN_POINT('Ctrl Pts',(2.05575677325334,-0.150464702977478,
4.06624306983149));
#95549=CARTESIAN_POINT('Ctrl Pts',(1.87171565024948,-0.86339797441863,4.02920585300301));
#95550=CARTESIAN_POINT('Ctrl Pts',(1.43032790007833,-1.33596290298842,3.99216863617453));
#95551=CARTESIAN_POINT('Ctrl Pts',(0.988940149907184,-1.80852783155821,
3.95513141934605));
#95552=CARTESIAN_POINT('Ctrl Pts',(0.290205772568748,-2.04072441725662,
3.91809420251758));
#95553=CARTESIAN_POINT('Ctrl Pts',(-0.346233738762281,-1.92633252011348,
3.8810569856891));
#95554=CARTESIAN_POINT('Ctrl Pts',(-0.982673250093302,-1.81194062297035,
3.84401976886062));
#95555=CARTESIAN_POINT('Ctrl Pts',(-1.55681789541692,-1.35096024298568,
3.80698255203214));
#95556=CARTESIAN_POINT('Ctrl Pts',(-1.806020726649,-0.754270452038098,3.76994533520366));
#95557=CARTESIAN_POINT('Ctrl Pts',(-1.90487422217158,-0.517576224744695,
3.75525345417718));
#95558=CARTESIAN_POINT('Ctrl Pts',(-1.9525967846073,-0.259527562563923,
3.74056157315071));
#95559=CARTESIAN_POINT('Ctrl Pts',(-1.95135107115213,-0.00103745302926256,
3.72586969212423));
#95560=CARTESIAN_POINT('Ctrl Pts',(-1.95125983814034,-0.000967513988672578,
3.62413030787576));
#95561=CARTESIAN_POINT('Ctrl Pts',(-1.95244197476311,-0.265035587897937,
3.63913749005996));
#95562=CARTESIAN_POINT('Ctrl Pts',(-1.90258326051973,-0.528675939020291,
3.65414467224416));
#95563=CARTESIAN_POINT('Ctrl Pts',(-1.799560505048,-0.769580726996389,3.66915185442837));
#95564=CARTESIAN_POINT('Ctrl Pts',(-1.54513274280624,-1.36452565772967,
3.70621399437209));
#95565=CARTESIAN_POINT('Ctrl Pts',(-0.966454476673152,-1.8208050988558,
3.74327613431581));
#95566=CARTESIAN_POINT('Ctrl Pts',(-0.328572905191125,-1.92943316874967,
3.78033827425953));
#95567=CARTESIAN_POINT('Ctrl Pts',(0.309308666290907,-2.03806123864353,
3.81740041420325));
#95568=CARTESIAN_POINT('Ctrl Pts',(1.00639354312189,-1.79903793730513,3.85446255414697));
#95569=CARTESIAN_POINT('Ctrl Pts',(1.44340173058911,-1.32184112162819,3.89152469409069));
#95570=CARTESIAN_POINT('Ctrl Pts',(1.88040991805633,-0.844644305951239,
3.92858683403441));
#95571=CARTESIAN_POINT('Ctrl Pts',(2.05734141615979,-0.129273975935752,
3.96564897397814));
#95572=CARTESIAN_POINT('Ctrl Pts',(1.89315776078089,0.496614739501458,4.00271111392186));
#95573=CARTESIAN_POINT('Ctrl Pts',(1.72897410540198,1.12250345493866,4.03977325386558));
#95574=CARTESIAN_POINT('Ctrl Pts',(1.22367529654071,1.65891055579759,4.0768353938093));
#95575=CARTESIAN_POINT('Ctrl Pts',(0.608699149567017,1.86014995417357,4.11389753375302));
#95576=CARTESIAN_POINT('Ctrl Pts',(-0.00627699740667481,2.06138935254956,
4.15095967369674));
#95577=CARTESIAN_POINT('Ctrl Pts',(-0.730930482492791,1.9274610484426,4.18802181364046));
#95578=CARTESIAN_POINT('Ctrl Pts',(-1.23335429038162,1.51970711029871,4.22508395358418));
#95579=CARTESIAN_POINT('Ctrl Pts',(-1.68092015819396,1.15647443240051,4.25809940501471));
#95580=CARTESIAN_POINT('Ctrl Pts',(-1.95213599025838,0.575947822566119,
4.29111485644523));
#95581=CARTESIAN_POINT('Ctrl Pts',(-1.95628130950281,-0.00119277919923279,
4.32413030787576));
#95582=CARTESIAN_POINT('Origin',(0.,0.,0.));
#95583=CARTESIAN_POINT('',(-1.95458266482996,0.00173443779922018,5.12586969212423));
#95584=CARTESIAN_POINT('',(-1.95491180920002,0.00168629508682236,5.02413030787576));
#95585=CARTESIAN_POINT('',(-1.954,-2.39295984553393E-16,0.));
#95586=CARTESIAN_POINT('Ctrl Pts',(-1.95458266482996,0.00173443779922018,
5.12586969212423));
#95587=CARTESIAN_POINT('Ctrl Pts',(-1.95579683437623,0.13363129532035,5.11834150842579));
#95588=CARTESIAN_POINT('Ctrl Pts',(-1.94358523444966,0.265304620125551,
5.11081332472735));
#95589=CARTESIAN_POINT('Ctrl Pts',(-1.91712292268468,0.394048828472761,
5.10328514102891));
#95590=CARTESIAN_POINT('Ctrl Pts',(-1.78693343503641,1.0274455880328,5.06624792420043));
#95591=CARTESIAN_POINT('Ctrl Pts',(-1.31181246839585,1.58994452273665,5.02921070737195));
#95592=CARTESIAN_POINT('Ctrl Pts',(-0.709107816346671,1.8242261056952,4.99217349054347));
#95593=CARTESIAN_POINT('Ctrl Pts',(-0.106403164297495,2.05850768865374,
4.95513627371499));
#95594=CARTESIAN_POINT('Ctrl Pts',(0.623885173160298,1.96457191986698,4.91809905688651));
#95595=CARTESIAN_POINT('Ctrl Pts',(1.14768109757825,1.58539044975217,4.88106184005803));
#95596=CARTESIAN_POINT('Ctrl Pts',(1.67147702199619,1.20620897963737,4.84402462322955));
#95597=CARTESIAN_POINT('Ctrl Pts',(1.9887805333743,0.541781808194522,4.80698740640107));
#95598=CARTESIAN_POINT('Ctrl Pts',(1.95443866449662,-0.103943670439598,
4.76995018957259));
#95599=CARTESIAN_POINT('Ctrl Pts',(1.92009679561895,-0.749669149073727,
4.73291297274411));
#95600=CARTESIAN_POINT('Ctrl Pts',(1.53410954648549,-1.37669293489913,4.69587575591563));
#95601=CARTESIAN_POINT('Ctrl Pts',(0.973049796091196,-1.69817810439032,
4.65883853908716));
#95602=CARTESIAN_POINT('Ctrl Pts',(0.411990045696909,-2.0196632738815,4.62180132225868));
#95603=CARTESIAN_POINT('Ctrl Pts',(-0.324142205958206,-2.03560982703848,
4.5847641054302));
#95604=CARTESIAN_POINT('Ctrl Pts',(-0.898597516275757,-1.7387228886878,
4.54772688860172));
#95605=CARTESIAN_POINT('Ctrl Pts',(-1.47305282659331,-1.44183595033712,
4.51068967177324));
#95606=CARTESIAN_POINT('Ctrl Pts',(-1.8858311955733,-0.832115520478776,
4.47365245494476));
#95607=CARTESIAN_POINT('Ctrl Pts',(-1.94810393739446,-0.188482967432129,
4.43661523811628));
#95608=CARTESIAN_POINT('Ctrl Pts',(-1.9541262996613,-0.126237620787308,
4.43303338945226));
#95609=CARTESIAN_POINT('Ctrl Pts',(-1.95687048211354,-0.0636751036633503,
4.42945154078825));
#95610=CARTESIAN_POINT('Ctrl Pts',(-1.95645574651684,-0.00107576288577632,
4.42586969212423));
#95611=CARTESIAN_POINT('Ctrl Pts',(-1.95628130950281,-0.00119277919923279,
4.32413030787576));
#95612=CARTESIAN_POINT('Ctrl Pts',(-1.95678939935296,-0.0719326340995119,
4.32817699638895));
#95613=CARTESIAN_POINT('Ctrl Pts',(-1.95328521122814,-0.14262162001596,
4.33222368490215));
#95614=CARTESIAN_POINT('Ctrl Pts',(-1.94560169264522,-0.212853377401693,
4.33627037341534));
#95615=CARTESIAN_POINT('Ctrl Pts',(-1.87523115632842,-0.856080354777335,
4.37333251335906));
#95616=CARTESIAN_POINT('Ctrl Pts',(-1.45429595300328,-1.46095473734778,
4.41039465330279));
#95617=CARTESIAN_POINT('Ctrl Pts',(-0.875593536694013,-1.75043093699665,
4.44745679324651));
#95618=CARTESIAN_POINT('Ctrl Pts',(-0.296891120384743,-2.03990713664554,
4.48451893319023));
#95619=CARTESIAN_POINT('Ctrl Pts',(0.439578508908652,-2.01398515337285,
4.52158107313395));
#95620=CARTESIAN_POINT('Ctrl Pts',(0.9964962855145,-1.68453781781564,4.55864321307767));
#95621=CARTESIAN_POINT('Ctrl Pts',(1.55341406212034,-1.35509048225843,4.59570535302139));
#95622=CARTESIAN_POINT('Ctrl Pts',(1.93077998603865,-0.72211779441669,4.63276749296511));
#95623=CARTESIAN_POINT('Ctrl Pts',(1.95575227831571,-0.0755349757277263,
4.66982963290883));
#95624=CARTESIAN_POINT('Ctrl Pts',(1.98072457059277,0.571047842961237,4.70689177285256));
#95625=CARTESIAN_POINT('Ctrl Pts',(1.6533032312286,1.23124079249743,4.74395391279628));
#95626=CARTESIAN_POINT('Ctrl Pts',(1.12345433605614,1.60266118112717,4.78101605273999));
#95627=CARTESIAN_POINT('Ctrl Pts',(0.59360544088369,1.97408156975691,4.81807819268371));
#95628=CARTESIAN_POINT('Ctrl Pts',(-0.138671010097046,2.05672939748021,
4.85514033262744));
#95629=CARTESIAN_POINT('Ctrl Pts',(-0.737976517839776,1.81275016640803,
4.89220247257116));
#95630=CARTESIAN_POINT('Ctrl Pts',(-1.33728202558251,1.56877093533586,4.92926461251488));
#95631=CARTESIAN_POINT('Ctrl Pts',(-1.80361659008724,0.998164645468222,
4.9663267524586));
#95632=CARTESIAN_POINT('Ctrl Pts',(-1.92338886510923,0.362281355122108,
5.00338889240232));
#95633=CARTESIAN_POINT('Ctrl Pts',(-1.94573194011967,0.243659678682544,
5.01030269756014));
#95634=CARTESIAN_POINT('Ctrl Pts',(-1.95601481281436,0.122766393772507,
5.01721650271795));
#95635=CARTESIAN_POINT('Ctrl Pts',(-1.95491180920002,0.00168629508682236,
5.02413030787576));
#95636=CARTESIAN_POINT('Origin',(0.,0.,0.));
#95637=CARTESIAN_POINT('',(-1.9507978584999,-3.45334863967226E-5,5.82586969212423));
#95638=CARTESIAN_POINT('',(-1.95080468396925,0.00018981806121043,5.72413030787576));
#95639=CARTESIAN_POINT('',(-1.954,-2.39295984553393E-16,0.));
#95640=CARTESIAN_POINT('Ctrl Pts',(-1.95079815420139,-3.45302974047446E-5,
5.82586969212423));
#95641=CARTESIAN_POINT('Ctrl Pts',(-1.95074640707532,0.328120037045956,
5.80723147606333));
#95642=CARTESIAN_POINT('Ctrl Pts',(-1.87237758907749,0.656297824114404,
5.78859326000243));
#95643=CARTESIAN_POINT('Ctrl Pts',(-1.715829951129,0.941574404236039,5.76995504394152));
#95644=CARTESIAN_POINT('Ctrl Pts',(-1.4047439120071,1.50846613462089,5.73291782711304));
#95645=CARTESIAN_POINT('Ctrl Pts',(-0.784943311216198,1.90594846094957,
5.69588061028457));
#95646=CARTESIAN_POINT('Ctrl Pts',(-0.139960769924853,1.95218999146749,
5.65884339345609));
#95647=CARTESIAN_POINT('Ctrl Pts',(0.505021771366483,1.99843152198542,5.62180617662761));
#95648=CARTESIAN_POINT('Ctrl Pts',(1.17518625315826,1.69343225669258,5.58476895979913));
#95649=CARTESIAN_POINT('Ctrl Pts',(1.56396070392606,1.17671648942254,5.54773174297065));
#95650=CARTESIAN_POINT('Ctrl Pts',(1.95273515469386,0.660000722152496,5.51069452614217));
#95651=CARTESIAN_POINT('Ctrl Pts',(2.06011957443768,-0.0684315470947738,
5.47365730931369));
#95652=CARTESIAN_POINT('Ctrl Pts',(1.83699012241942,-0.675353292756691,
5.43662009248521));
#95653=CARTESIAN_POINT('Ctrl Pts',(1.61386067040115,-1.28227503841861,5.39958287565673));
#95654=CARTESIAN_POINT('Ctrl Pts',(1.06021734662079,-1.76768626049519,5.36254565882826));
#95655=CARTESIAN_POINT('Ctrl Pts',(0.429328609649713,-1.90953180775813,
5.32550844199978));
#95656=CARTESIAN_POINT('Ctrl Pts',(-0.201560127321352,-2.05137735502108,
5.2884712251713));
#95657=CARTESIAN_POINT('Ctrl Pts',(-0.909694277483132,-1.84965722747041,
5.25143400834282));
#95658=CARTESIAN_POINT('Ctrl Pts',(-1.37113234823603,-1.39664987148696,
5.21439679151434));
#95659=CARTESIAN_POINT('Ctrl Pts',(-1.73877852911313,-1.03572077852157,
5.1848877583843));
#95660=CARTESIAN_POINT('Ctrl Pts',(-1.94982335358017,-0.515275892214865,
5.15537872525427));
#95661=CARTESIAN_POINT('Ctrl Pts',(-1.95458266482996,0.00173443779922018,
5.12586969212423));
#95662=CARTESIAN_POINT('Ctrl Pts',(-1.95491180920002,0.00168629508682236,
5.02413030787576));
#95663=CARTESIAN_POINT('Ctrl Pts',(-1.95010205227512,-0.526295513449078,
5.05427864266167));
#95664=CARTESIAN_POINT('Ctrl Pts',(-1.72879182329996,-1.05782955367232,
5.08442697744757));
#95665=CARTESIAN_POINT('Ctrl Pts',(-1.34689356786549,-1.42005289462677,
5.11457531223348));
#95666=CARTESIAN_POINT('Ctrl Pts',(-0.877416010060499,-1.86534356320495,
5.1516374521772));
#95667=CARTESIAN_POINT('Ctrl Pts',(-0.165250908911267,-2.05476460953673,
5.18869959212092));
#95668=CARTESIAN_POINT('Ctrl Pts',(0.463414671012952,-1.90155708549211,
5.22576173206464));
#95669=CARTESIAN_POINT('Ctrl Pts',(1.09208025093718,-1.74834956144749,5.26282387200837));
#95670=CARTESIAN_POINT('Ctrl Pts',(1.63724630963639,-1.25251346702646,5.29988601195209));
#95671=CARTESIAN_POINT('Ctrl Pts',(1.84921496651671,-0.641152489120857,
5.33694815189581));
#95672=CARTESIAN_POINT('Ctrl Pts',(2.06118362339704,-0.0297915112152539,
5.37401029183953));
#95673=CARTESIAN_POINT('Ctrl Pts',(1.93995487845847,0.697094350174917,5.41107243178325));
#95674=CARTESIAN_POINT('Ctrl Pts',(1.54105412656959,1.20657560296821,5.44813457172697));
#95675=CARTESIAN_POINT('Ctrl Pts',(1.14215337468071,1.71605685576151,5.48519671167069));
#95676=CARTESIAN_POINT('Ctrl Pts',(0.465580615841514,2.00813349995792,5.52225885161441));
#95677=CARTESIAN_POINT('Ctrl Pts',(-0.178779150223708,1.94902809680635,
5.55932099155813));
#95678=CARTESIAN_POINT('Ctrl Pts',(-0.823138916288934,1.88992269365477,
5.59638313150186));
#95679=CARTESIAN_POINT('Ctrl Pts',(-1.43528568958019,1.4796352431552,5.63344527144558));
#95680=CARTESIAN_POINT('Ctrl Pts',(-1.73484296927877,0.906086297567352,
5.6705074113893));
#95681=CARTESIAN_POINT('Ctrl Pts',(-1.87931321146693,0.629475576708828,
5.68838171021812));
#95682=CARTESIAN_POINT('Ctrl Pts',(-1.95107725773013,0.31489133949035,5.70625600904694));
#95683=CARTESIAN_POINT('Ctrl Pts',(-1.95080468396925,0.00018981806121043,
5.72413030787576));
#95684=CARTESIAN_POINT('Origin',(0.,0.,0.));
#95685=CARTESIAN_POINT('',(-1.95470932084261,-0.00171584046685047,6.52586969212424));
#95686=CARTESIAN_POINT('',(-1.95421427783755,-0.00177812761388513,6.42413030787576));
#95687=CARTESIAN_POINT('',(-1.954,-2.39295984553393E-16,0.));
#95688=CARTESIAN_POINT('Ctrl Pts',(-1.95470932084261,-0.00171584046685047,
6.52586969212424));
#95689=CARTESIAN_POINT('Ctrl Pts',(-1.94992946923152,0.519398730151351,
6.49612144370087));
#95690=CARTESIAN_POINT('Ctrl Pts',(-1.73506994162404,1.04399306729571,6.46637319527751));
#95691=CARTESIAN_POINT('Ctrl Pts',(-1.36210733975536,1.40545308526766,6.43662494685414));
#95692=CARTESIAN_POINT('Ctrl Pts',(-0.897760782010601,1.85547867567989,
6.39958773002566));
#95693=CARTESIAN_POINT('Ctrl Pts',(-0.188341937200331,2.05263315093338,
6.36255051319719));
#95694=CARTESIAN_POINT('Ctrl Pts',(0.441620008484366,1.90672665791667,6.32551329636871));
#95695=CARTESIAN_POINT('Ctrl Pts',(1.07158195416906,1.76082016489995,6.28847607954023));
#95696=CARTESIAN_POINT('Ctrl Pts',(1.62208700072817,1.27185270361303,6.25143886271175));
#95697=CARTESIAN_POINT('Ctrl Pts',(1.84130231899333,0.663506254660481,6.21440164588327));
#95698=CARTESIAN_POINT('Ctrl Pts',(2.0605176372585,0.0551598057079281,6.17736442905479));
#95699=CARTESIAN_POINT('Ctrl Pts',(1.94844322722972,-0.672565630910262,
6.14032721222632));
#95700=CARTESIAN_POINT('Ctrl Pts',(1.55634840229719,-1.18676637573315,6.10328999539784));
#95701=CARTESIAN_POINT('Ctrl Pts',(1.16425357736466,-1.70096712055603,6.06625277856936));
#95702=CARTESIAN_POINT('Ctrl Pts',(0.492138337528384,-2.00164317358361,
6.02921556174087));
#95703=CARTESIAN_POINT('Ctrl Pts',(-0.152532956197894,-1.95124792816734,
5.9921783449124));
#95704=CARTESIAN_POINT('Ctrl Pts',(-0.797204249924167,-1.90085268275106,
5.95514112808392));
#95705=CARTESIAN_POINT('Ctrl Pts',(-1.41443159754043,-1.49938613889095,
5.91810391125544));
#95706=CARTESIAN_POINT('Ctrl Pts',(-1.72185953262212,-0.930502299740384,
5.88106669442696));
#95707=CARTESIAN_POINT('Ctrl Pts',(-1.87458069522289,-0.647897528391999,
5.86266769365939));
#95708=CARTESIAN_POINT('Ctrl Pts',(-1.95084923717034,-0.323977343102287,
5.84426869289181));
#95709=CARTESIAN_POINT('Ctrl Pts',(-1.95079815420139,-3.45302974047446E-5,
5.82586969212423));
#95710=CARTESIAN_POINT('Ctrl Pts',(-1.95080468396925,0.00018981806121043,
5.72413030787576));
#95711=CARTESIAN_POINT('Ctrl Pts',(-1.95051207937167,-0.337638415069996,
5.74331814899066));
#95712=CARTESIAN_POINT('Ctrl Pts',(-1.86720620393942,-0.675601803708791,
5.76250599010555));
#95713=CARTESIAN_POINT('Ctrl Pts',(-1.70171536425399,-0.966869859783203,
5.78169383122045));
#95714=CARTESIAN_POINT('Ctrl Pts',(-1.38206269342473,-1.5294666308698,5.81875597116418));
#95715=CARTESIAN_POINT('Ctrl Pts',(-0.755789565660301,-1.91784973236686,
5.85581811110791));
#95716=CARTESIAN_POINT('Ctrl Pts',(-0.109742658556152,-1.95413127900566,
5.89288025105163));
#95717=CARTESIAN_POINT('Ctrl Pts',(0.536304248547996,-1.99041282564447,
5.92994239099535));
#95718=CARTESIAN_POINT('Ctrl Pts',(1.20212493499187,-1.674592817425,5.96700453093906));
#95719=CARTESIAN_POINT('Ctrl Pts',(1.58275908344154,-1.15132366886058,6.00406667088278));
#95720=CARTESIAN_POINT('Ctrl Pts',(1.9633932318912,-0.628054520296152,6.0411288108265));
#95721=CARTESIAN_POINT('Ctrl Pts',(2.05884084234667,0.102663768613233,6.07819095077022));
#95722=CARTESIAN_POINT('Ctrl Pts',(1.82538483877546,0.706146370849535,6.11525309071394));
#95723=CARTESIAN_POINT('Ctrl Pts',(1.59192883520425,1.30962897308584,6.15231523065767));
#95724=CARTESIAN_POINT('Ctrl Pts',(1.02956921760636,1.78587588864905,6.18937737060139));
#95725=CARTESIAN_POINT('Ctrl Pts',(0.395878889512919,1.91675569949154,6.22643951054511));
#95726=CARTESIAN_POINT('Ctrl Pts',(-0.237811438580523,2.04763551033402,
6.26350165048883));
#95727=CARTESIAN_POINT('Ctrl Pts',(-0.942832477169518,1.83314821645578,
6.30056379043255));
#95728=CARTESIAN_POINT('Ctrl Pts',(-1.39626929730598,1.37153365109863,6.33762593037627));
#95729=CARTESIAN_POINT('Ctrl Pts',(-1.7490486198241,1.01239194403086,6.3664607228761));
#95730=CARTESIAN_POINT('Ctrl Pts',(-1.94954331224527,0.503663409317413,
6.39529551537593));
#95731=CARTESIAN_POINT('Ctrl Pts',(-1.95421427783755,-0.00177812761388513,
6.42413030787576));
#95732=CARTESIAN_POINT('Origin',(0.,0.,0.));
#95733=CARTESIAN_POINT('',(-1.95636369417486,0.00113518110994186,7.22586969212423));
#95734=CARTESIAN_POINT('',(-1.95675615924934,0.000851174274233985,7.12413030787576));
#95735=CARTESIAN_POINT('',(-1.954,-2.39295984553393E-16,0.));
#95736=CARTESIAN_POINT('Ctrl Pts',(-1.95636369417486,0.00113518110994186,
7.22586969212423));
#95737=CARTESIAN_POINT('Ctrl Pts',(-1.95682546989371,0.0679235189129894,
7.22204862816689));
#95738=CARTESIAN_POINT('Ctrl Pts',(-1.95370156992351,0.134668159558925,
7.21822756420955));
#95739=CARTESIAN_POINT('Ctrl Pts',(-1.94684940168549,0.201027826582277,
7.2144065002522));
#95740=CARTESIAN_POINT('Ctrl Pts',(-1.88043197355288,0.844245894546327,
7.17736928342373));
#95741=CARTESIAN_POINT('Ctrl Pts',(-1.46373463610807,1.45129475044757,7.14033206659525));
#95742=CARTESIAN_POINT('Ctrl Pts',(-0.887378837876281,1.74447515831938,
7.10329484976677));
#95743=CARTESIAN_POINT('Ctrl Pts',(-0.31102303964449,2.03765556619118,7.06625763293829));
#95744=CARTESIAN_POINT('Ctrl Pts',(0.424991219374283,2.01696752603353,7.02922041610981));
#95745=CARTESIAN_POINT('Ctrl Pts',(0.983968473233738,1.69187494324663,6.99218319928133));
#95746=CARTESIAN_POINT('Ctrl Pts',(1.54294572709319,1.36678236045973,6.95514598245285));
#95747=CARTESIAN_POINT('Ctrl Pts',(1.92488597579333,0.737285235043576,6.91810876562437));
#95748=CARTESIAN_POINT('Ctrl Pts',(1.95506767226643,0.0913519390189264,
6.8810715487959));
#95749=CARTESIAN_POINT('Ctrl Pts',(1.98524936873952,-0.554581357005719,
6.84403433196742));
#95750=CARTESIAN_POINT('Ctrl Pts',(1.66367251298559,-1.21695082363886,6.80699711513894));
#95751=CARTESIAN_POINT('Ctrl Pts',(1.13744494695038,-1.59275037986524,6.76995989831046));
#95752=CARTESIAN_POINT('Ctrl Pts',(0.611217380915185,-1.96854993609162,
6.73292268148198));
#95753=CARTESIAN_POINT('Ctrl Pts',(-0.119660895401274,-2.05777958191125,
6.69588546465349));
#95754=CARTESIAN_POINT('Ctrl Pts',(-0.72084391141631,-1.81962051958034,
6.65884824782502));
#95755=CARTESIAN_POINT('Ctrl Pts',(-1.32202692743135,-1.58146145724943,
6.62181103099654));
#95756=CARTESIAN_POINT('Ctrl Pts',(-1.79351468314497,-1.01591368676797,
6.58477381416807));
#95757=CARTESIAN_POINT('Ctrl Pts',(-1.91962142566216,-0.381691448741754,
6.54773659733959));
#95758=CARTESIAN_POINT('Ctrl Pts',(-1.9444393828574,-0.256875756563692,
6.54044762893447));
#95759=CARTESIAN_POINT('Ctrl Pts',(-1.95588048853217,-0.129400253566584,
6.53315866052935));
#95760=CARTESIAN_POINT('Ctrl Pts',(-1.95470932084261,-0.00171584046685047,
6.52586969212424));
#95761=CARTESIAN_POINT('Ctrl Pts',(-1.95421427783755,-0.00177812761388513,
6.42413030787576));
#95762=CARTESIAN_POINT('Ctrl Pts',(-1.95554703085897,-0.145994290672205,
6.43235765531965));
#95763=CARTESIAN_POINT('Ctrl Pts',(-1.94093747105224,-0.289942854151266,
6.44058500276354));
#95764=CARTESIAN_POINT('Ctrl Pts',(-1.90937423221194,-0.430072724152966,
6.44881235020743));
#95765=CARTESIAN_POINT('Ctrl Pts',(-1.7671897452975,-1.06132269721135,6.48587449015115));
#95766=CARTESIAN_POINT('Ctrl Pts',(-1.28096816978468,-1.61508080649208,
6.52293663009487));
#95767=CARTESIAN_POINT('Ctrl Pts',(-0.67340953434779,-1.83771382585667,
6.55999877003859));
#95768=CARTESIAN_POINT('Ctrl Pts',(-0.0658508989108841,-2.06034684522128,
6.59706090998232));
#95769=CARTESIAN_POINT('Ctrl Pts',(0.663044796450101,-1.95185477466974,
6.63412304992604));
#95770=CARTESIAN_POINT('Ctrl Pts',(1.17942751209788,-1.56192933591821,6.67118518986976));
#95771=CARTESIAN_POINT('Ctrl Pts',(1.69581022774564,-1.17200389716668,6.70824732981348));
#95772=CARTESIAN_POINT('Ctrl Pts',(1.9996799636802,-0.500645090215166,6.7453094697572));
#95773=CARTESIAN_POINT('Ctrl Pts',(1.95185778931935,0.144650188277344,6.78237160970092));
#95774=CARTESIAN_POINT('Ctrl Pts',(1.90403561495849,0.789945466769872,6.81943374964464));
#95775=CARTESIAN_POINT('Ctrl Pts',(1.5045215303022,1.4091772168034,6.85649588958836));
#95776=CARTESIAN_POINT('Ctrl Pts',(0.936301652358751,1.71872386452436,6.89355802953208));
#95777=CARTESIAN_POINT('Ctrl Pts',(0.368081774415317,2.02827051224532,6.9306201694758));
#95778=CARTESIAN_POINT('Ctrl Pts',(-0.368843896815252,2.02813205765373,
6.96768230941953));
#95779=CARTESIAN_POINT('Ctrl Pts',(-0.936947418561655,1.71837191595589,
7.00474444936325));
#95780=CARTESIAN_POINT('Ctrl Pts',(-1.50505094030807,1.40861177425805,7.04180658930697));
#95781=CARTESIAN_POINT('Ctrl Pts',(-1.90433231257031,0.78922994545395,7.07886872925069));
#95782=CARTESIAN_POINT('Ctrl Pts',(-1.95191200566454,0.143916742729559,
7.11593086919441));
#95783=CARTESIAN_POINT('Ctrl Pts',(-1.95542076848464,0.0963281429343837,
7.11866401542153));
#95784=CARTESIAN_POINT('Ctrl Pts',(-1.95701686505733,0.0485985200318871,
7.12139716164864));
#95785=CARTESIAN_POINT('Ctrl Pts',(-1.95675615924934,0.000851174274233985,
7.12413030787576));
#95786=CARTESIAN_POINT('Origin',(0.,0.,0.));
#95787=CARTESIAN_POINT('',(-1.95128545551857,0.000980157954364874,7.92586969212424));
#95788=CARTESIAN_POINT('',(-1.95166123101285,0.00126544742759004,7.82413030787576));
#95789=CARTESIAN_POINT('',(-1.954,-2.39295984553393E-16,0.));
#95790=CARTESIAN_POINT('Ctrl Pts',(-1.95128545551857,0.000980157954364874,
7.92586969212424));
#95791=CARTESIAN_POINT('Ctrl Pts',(-1.95247914943593,0.263701155015296,
7.91093859580443));
#95792=CARTESIAN_POINT('Ctrl Pts',(-1.90313505751618,0.525992349613935,
7.89600749948463));
#95793=CARTESIAN_POINT('Ctrl Pts',(-1.80112460177197,0.765888339627252,
7.88107640316483));
#95794=CARTESIAN_POINT('Ctrl Pts',(-1.54808334564134,1.36096050365993,7.84403918633635));
#95795=CARTESIAN_POINT('Ctrl Pts',(-0.970981193167941,1.81823294990903,
7.80700196950786));
#95796=CARTESIAN_POINT('Ctrl Pts',(-0.333818027149729,1.92852282969788,
7.76996475267938));
#95797=CARTESIAN_POINT('Ctrl Pts',(0.303345138868501,2.03881270948674,7.73292753585091));
#95798=CARTESIAN_POINT('Ctrl Pts',(1.00056931843154,1.80212002281537,7.69589031902244));
#95799=CARTESIAN_POINT('Ctrl Pts',(1.43890387011628,1.32672168613705,7.65885310219396));
#95800=CARTESIAN_POINT('Ctrl Pts',(1.87723842180101,0.851323349458752,7.62181588536548));
#95801=CARTESIAN_POINT('Ctrl Pts',(2.05668334560742,0.13721936277351,7.58477866853699));
#95802=CARTESIAN_POINT('Ctrl Pts',(1.8951501609247,-0.488917833023672,7.54774145170851));
#95803=CARTESIAN_POINT('Ctrl Pts',(1.73361697624198,-1.11505502882086,7.51070423488003));
#95804=CARTESIAN_POINT('Ctrl Pts',(1.23110568307013,-1.65322543373001,7.47366701805156));
#95805=CARTESIAN_POINT('Ctrl Pts',(0.61749399359133,-1.85723879665063,7.43662980122308));
#95806=CARTESIAN_POINT('Ctrl Pts',(0.00388230411252383,-2.06125215957126,
7.3995925843946));
#95807=CARTESIAN_POINT('Ctrl Pts',(-0.72082978167322,-1.93110848050335,
7.36255536756612));
#95808=CARTESIAN_POINT('Ctrl Pts',(-1.22511706515588,-1.52634300095596,
7.32551815073764));
#95809=CARTESIAN_POINT('Ctrl Pts',(-1.6773779241913,-1.16333645789233,7.2923019978665));
#95810=CARTESIAN_POINT('Ctrl Pts',(-1.95234952088687,-0.579449614967985,
7.25908584499537));
#95811=CARTESIAN_POINT('Ctrl Pts',(-1.95636369417486,0.00113518110994186,
7.22586969212423));
#95812=CARTESIAN_POINT('Ctrl Pts',(-1.95675615924934,0.000851174274233985,
7.12413030787576));
#95813=CARTESIAN_POINT('Ctrl Pts',(-1.95348162971424,-0.598867317271105,
7.15845930159236));
#95814=CARTESIAN_POINT('Ctrl Pts',(-1.65727828481393,-1.20138176331325,
7.19278829530897));
#95815=CARTESIAN_POINT('Ctrl Pts',(-1.17884051406102,-1.56237241050387,
7.22711728902557));
#95816=CARTESIAN_POINT('Ctrl Pts',(-0.662311315437018,-1.95210378436822,
7.2641794289693));
#95817=CARTESIAN_POINT('Ctrl Pts',(0.0666250957372189,-2.06032195545224,
7.30124156891302));
#95818=CARTESIAN_POINT('Ctrl Pts',(0.674100031098693,-1.83746065393738,
7.33830370885674));
#95819=CARTESIAN_POINT('Ctrl Pts',(1.28157496646017,-1.61459935242253,7.37536584880046));
#95820=CARTESIAN_POINT('Ctrl Pts',(1.76758842600887,-1.0606585783088,7.41242798874417));
#95821=CARTESIAN_POINT('Ctrl Pts',(1.9095357026966,-0.429355222190436,7.44949012868789));
#95822=CARTESIAN_POINT('Ctrl Pts',(2.05148297938434,0.201948133927931,7.48655226863161));
#95823=CARTESIAN_POINT('Ctrl Pts',(1.84936407321109,0.910614072050953,7.52361440857534));
#95824=CARTESIAN_POINT('Ctrl Pts',(1.39575382755531,1.37205822017881,7.56067654851907));
#95825=CARTESIAN_POINT('Ctrl Pts',(0.942143581899539,1.83350236830666,7.59773868846279));
#95826=CARTESIAN_POINT('Ctrl Pts',(0.237041996761252,2.04772472643938,7.6348008284065));
#95827=CARTESIAN_POINT('Ctrl Pts',(-0.396599106844383,1.91660680765389,
7.67186296835022));
#95828=CARTESIAN_POINT('Ctrl Pts',(-1.03024021045003,1.78548888886839,7.70892510829394));
#95829=CARTESIAN_POINT('Ctrl Pts',(-1.59242083252301,1.30903069316467,7.74598724823766));
#95830=CARTESIAN_POINT('Ctrl Pts',(-1.82565005336597,0.705460409477194,
7.78304938818139));
#95831=CARTESIAN_POINT('Ctrl Pts',(-1.9118230851659,0.482454556858425,7.79674302807951));
#95832=CARTESIAN_POINT('Ctrl Pts',(-1.95308968355645,0.242096139413284,
7.81043666797764));
#95833=CARTESIAN_POINT('Ctrl Pts',(-1.95166123101285,0.00126544742759004,
7.82413030787576));
#95834=CARTESIAN_POINT('Origin',(0.,0.,0.));
#95835=CARTESIAN_POINT('',(-1.95279013340439,-0.00168009551267251,8.62586969212423));
#95836=CARTESIAN_POINT('',(-1.95215444869335,-0.00150235120299324,8.52413030787576));
#95837=CARTESIAN_POINT('',(-1.954,-2.39295984553393E-16,0.));
#95838=CARTESIAN_POINT('Ctrl Pts',(-1.95279013340439,-0.00168009551267251,
8.62586969212423));
#95839=CARTESIAN_POINT('Ctrl Pts',(-1.94903607268958,0.455640131522026,
8.59982856344197));
#95840=CARTESIAN_POINT('Ctrl Pts',(-1.78871895344458,0.915331173731693,
8.57378743475971));
#95841=CARTESIAN_POINT('Ctrl Pts',(-1.49539281844263,1.26270942713959,8.54774630607745));
#95842=CARTESIAN_POINT('Ctrl Pts',(-1.07820722729247,1.75677110357261,8.51070908924897));
#95843=CARTESIAN_POINT('Ctrl Pts',(-0.391968436807465,2.02364430724413,
8.47367187242049));
#95844=CARTESIAN_POINT('Ctrl Pts',(0.24939826400162,1.94124580780539,8.43663465559201));
#95845=CARTESIAN_POINT('Ctrl Pts',(0.890764964810705,1.85884730836666,8.39959743876353));
#95846=CARTESIAN_POINT('Ctrl Pts',(1.48725957594388,1.42717710581768,8.36256022193505));
#95847=CARTESIAN_POINT('Ctrl Pts',(1.76601098282085,0.843706103134459,8.32552300510657));
#95848=CARTESIAN_POINT('Ctrl Pts',(2.04476238969783,0.260235100451228,8.28848578827809));
#95849=CARTESIAN_POINT('Ctrl Pts',(2.00577059231861,-0.475036702366233,
8.25144857144961));
#95850=CARTESIAN_POINT('Ctrl Pts',(1.66687269277466,-1.02575348200379,8.21441135462113));
#95851=CARTESIAN_POINT('Ctrl Pts',(1.32797479323072,-1.57647026164133,8.17737413779266));
#95852=CARTESIAN_POINT('Ctrl Pts',(0.689170791522051,-1.94263201809897,
8.14033692096418));
#95853=CARTESIAN_POINT('Ctrl Pts',(0.0426865627857745,-1.95673519857469,
8.1032997041357));
#95854=CARTESIAN_POINT('Ctrl Pts',(-0.60379766595052,-1.97083837905041,
8.06626248730722));
#95855=CARTESIAN_POINT('Ctrl Pts',(-1.25796212171444,-1.6328829835442,8.02922527047874));
#95856=CARTESIAN_POINT('Ctrl Pts',(-1.62055416970245,-1.09746934488294,
7.99218805365026));
#95857=CARTESIAN_POINT('Ctrl Pts',(-1.83697171385623,-0.777901098892797,
7.97008193314158));
#95858=CARTESIAN_POINT('Ctrl Pts',(-1.94951814111497,-0.387989405753114,
7.94797581263291));
#95859=CARTESIAN_POINT('Ctrl Pts',(-1.95128545551857,0.000980157954364874,
7.92586969212424));
#95860=CARTESIAN_POINT('Ctrl Pts',(-1.95166123101285,0.00126544742759004,
7.82413030787576));
#95861=CARTESIAN_POINT('Ctrl Pts',(-1.94922354508138,-0.409717467160323,
7.84749880792136));
#95862=CARTESIAN_POINT('Ctrl Pts',(-1.82244856716882,-0.822075748123473,
7.87086730796695));
#95863=CARTESIAN_POINT('Ctrl Pts',(-1.58232634722073,-1.15191832939155,
7.89423580801255));
#95864=CARTESIAN_POINT('Ctrl Pts',(-1.20149560061961,-1.67504441290151,
7.93129794795627));
#95865=CARTESIAN_POINT('Ctrl Pts',(-0.535556287804454,-1.99061420825021,
7.96836008789999));
#95866=CARTESIAN_POINT('Ctrl Pts',(0.110476940437387,-1.95408990384897,
8.00542222784371));
#95867=CARTESIAN_POINT('Ctrl Pts',(0.756510168679237,-1.91756559944773,
8.04248436778743));
#95868=CARTESIAN_POINT('Ctrl Pts',(1.38263731234777,-1.52894719529654,8.07954650773116));
#95869=CARTESIAN_POINT('Ctrl Pts',(1.70207855773424,-0.966230350379699,
8.11660864767487));
#95870=CARTESIAN_POINT('Ctrl Pts',(2.02151980312072,-0.403513505462853,
8.1536707876186));
#95871=CARTESIAN_POINT('Ctrl Pts',(2.03427515022513,0.333301780219651,8.19073292756232));
#95872=CARTESIAN_POINT('Ctrl Pts',(1.73450237337761,0.906738122863988,8.22779506750604));
#95873=CARTESIAN_POINT('Ctrl Pts',(1.43472959653009,1.48017446550833,8.26485720744976));
#95874=CARTESIAN_POINT('Ctrl Pts',(0.822428695730641,1.89023186511451,8.30191934739348));
#95875=CARTESIAN_POINT('Ctrl Pts',(0.178046765554912,1.94909513773745,8.3389814873372));
#95876=CARTESIAN_POINT('Ctrl Pts',(-0.466335164620799,2.00795841036038,
8.37604362728092));
#95877=CARTESIAN_POINT('Ctrl Pts',(-1.14279812417278,1.71562755600011,8.41310576722464));
#95878=CARTESIAN_POINT('Ctrl Pts',(-1.54150740386038,1.20599644714809,8.45016790716836));
#95879=CARTESIAN_POINT('Ctrl Pts',(-1.80673309918174,0.866984359672774,
8.47482204073749));
#95880=CARTESIAN_POINT('Ctrl Pts',(-1.94905131081074,0.431815751432988,
8.49947617430663));
#95881=CARTESIAN_POINT('Ctrl Pts',(-1.95215444869335,-0.00150235120299324,
8.52413030787576));
#95882=CARTESIAN_POINT('Origin',(0.,0.,0.));
#95883=CARTESIAN_POINT('',(-1.95719986784682,3.71606954582295E-5,9.32586969212424));
#95884=CARTESIAN_POINT('',(-1.95707453392556,-0.000466568259871601,9.22413030787576));
#95885=CARTESIAN_POINT('',(-1.954,-2.39295984553393E-16,0.));
#95886=CARTESIAN_POINT('Ctrl Pts',(-1.95719986784682,3.71606954581456E-5,
9.32586969212423));
#95887=CARTESIAN_POINT('Ctrl Pts',(-1.95720042510874,0.00202653151786848,
9.32575574790799));
#95888=CARTESIAN_POINT('Ctrl Pts',(-1.95719765412071,0.00401590074103218,
9.32564180369175));
#95889=CARTESIAN_POINT('Ctrl Pts',(-1.95719155021855,0.00600525973720184,
9.32552785947551));
#95890=CARTESIAN_POINT('Ctrl Pts',(-1.95520749560565,0.65264027922361,9.28849064264703));
#95891=CARTESIAN_POINT('Ctrl Pts',(-1.60108272580438,1.29819476052309,9.25145342581855));
#95892=CARTESIAN_POINT('Ctrl Pts',(-1.0568144211536,1.64735485073218,9.21441620899007));
#95893=CARTESIAN_POINT('Ctrl Pts',(-0.512546116502833,1.99651494094127,
9.17737899216159));
#95894=CARTESIAN_POINT('Ctrl Pts',(0.221865722997436,2.04928064005996,9.14034177533311));
#95895=CARTESIAN_POINT('Ctrl Pts',(0.810458692323854,1.78151382429043,9.10330455850463));
#95896=CARTESIAN_POINT('Ctrl Pts',(1.39905166165026,1.51374700852089,9.06626734167615));
#95897=CARTESIAN_POINT('Ctrl Pts',(1.84182576080283,0.925447677863139,9.02923012484767));
#95898=CARTESIAN_POINT('Ctrl Pts',(1.93623051178265,0.285737974246437,8.99219290801919));
#95899=CARTESIAN_POINT('Ctrl Pts',(2.03063526276248,-0.353971729370283,
8.95515569119071));
#95900=CARTESIAN_POINT('Ctrl Pts',(1.77667066556955,-1.04509180594595,8.91811847436223));
#95901=CARTESIAN_POINT('Ctrl Pts',(1.29051481285208,-1.47146399547075,8.88108125753376));
#95902=CARTESIAN_POINT('Ctrl Pts',(0.804358960134614,-1.89783618499555,
8.84404404070528));
#95903=CARTESIAN_POINT('Ctrl Pts',(0.0860118518926114,-2.05946048746948,
8.8070068238768));
#95904=CARTESIAN_POINT('Ctrl Pts',(-0.535913025040727,-1.88240059832962,
8.76996960704832));
#95905=CARTESIAN_POINT('Ctrl Pts',(-1.15783790197406,-1.70534070918976,
8.73293239021984));
#95906=CARTESIAN_POINT('Ctrl Pts',(-1.68334054759872,-1.18959662843613,
8.69589517339136));
#95907=CARTESIAN_POINT('Ctrl Pts',(-1.87202567450341,-0.571099513462055,
8.65885795656288));
#95908=CARTESIAN_POINT('Ctrl Pts',(-1.92804495632289,-0.387472087407564,
8.64786186841667));
#95909=CARTESIAN_POINT('Ctrl Pts',(-1.95437531748109,-0.194787452297348,
8.63686578027045));
#95910=CARTESIAN_POINT('Ctrl Pts',(-1.95279013340439,-0.00168009551267234,
8.62586969212424));
#95911=CARTESIAN_POINT('Ctrl Pts',(-1.95215444869335,-0.00150235120299324,
8.52413030787576));
#95912=CARTESIAN_POINT('Ctrl Pts',(-1.95371620524508,-0.21958398707372,
8.53653831425035));
#95913=CARTESIAN_POINT('Ctrl Pts',(-1.92001564940553,-0.437196901383431,
8.54894632062494));
#95914=CARTESIAN_POINT('Ctrl Pts',(-1.84897391479539,-0.641847309864828,
8.56135432699953));
#95915=CARTESIAN_POINT('Ctrl Pts',(-1.63677554621959,-1.25312859468192,
8.59841646694325));
#95916=CARTESIAN_POINT('Ctrl Pts',(-1.0914232092448,-1.74875980097234,8.63547860688697));
#95917=CARTESIAN_POINT('Ctrl Pts',(-0.462700104058479,-1.90173108515756,
8.67254074683069));
#95918=CARTESIAN_POINT('Ctrl Pts',(0.166023001127845,-2.05470236934278,
8.70960288677441));
#95919=CARTESIAN_POINT('Ctrl Pts',(0.878116874525705,-1.86501373142281,
8.74666502671813));
#95920=CARTESIAN_POINT('Ctrl Pts',(1.34742707561642,-1.41954668207959,8.78372716666185));
#95921=CARTESIAN_POINT('Ctrl Pts',(1.81673727670714,-0.974079632736377,
8.82078930660557));
#95922=CARTESIAN_POINT('Ctrl Pts',(2.04326380549072,-0.272834171969915,
8.85785144654929));
#95923=CARTESIAN_POINT('Ctrl Pts',(1.92325259761237,0.363004067433246,8.89491358649301));
#95924=CARTESIAN_POINT('Ctrl Pts',(1.80324138973402,0.998842306836407,8.93197572643673));
#95925=CARTESIAN_POINT('Ctrl Pts',(1.33669244519374,1.56927332487627,8.96903786638045));
#95926=CARTESIAN_POINT('Ctrl Pts',(0.737295301650971,1.81302734225987,9.00610000632417));
#95927=CARTESIAN_POINT('Ctrl Pts',(0.137898158108199,2.05678135964346,9.0431621462679));
#95928=CARTESIAN_POINT('Ctrl Pts',(-0.59434718443707,1.9738583763708,9.08022428621162));
#95929=CARTESIAN_POINT('Ctrl Pts',(-1.12405647662483,1.60223891616111,9.11728642615534));
#95930=CARTESIAN_POINT('Ctrl Pts',(-1.63307724594775,1.24513356361944,9.15290105339548));
#95931=CARTESIAN_POINT('Ctrl Pts',(-1.95507366281261,0.621442230158499,
9.18851568063562));
#95932=CARTESIAN_POINT('Ctrl Pts',(-1.95707453392556,-0.000466568259871601,
9.22413030787576));
#95933=CARTESIAN_POINT('Origin',(0.,0.,0.));
#95934=CARTESIAN_POINT('',(-1.95268202714777,0.00165579016441021,10.0258696921242));
#95935=CARTESIAN_POINT('',(-1.9535343393295,0.00178280253715055,9.92413030787576));
#95936=CARTESIAN_POINT('',(-1.954,-2.39295984553393E-16,0.));
#95937=CARTESIAN_POINT('Ctrl Pts',(-1.95268202714777,0.00165579016441021,
10.0258696921242));
#95938=CARTESIAN_POINT('Ctrl Pts',(-1.9542709496717,0.198793394721131,10.0146457155455));
#95939=CARTESIAN_POINT('Ctrl Pts',(-1.92681564478375,0.395498739780043,
10.0034217389668));
#95940=CARTESIAN_POINT('Ctrl Pts',(-1.86848643290836,0.582577638715851,
9.99219776238813));
#95941=CARTESIAN_POINT('Ctrl Pts',(-1.67600993827966,1.1999062383733,9.95516054555966));
#95942=CARTESIAN_POINT('Ctrl Pts',(-1.14735119634562,1.71241362792136,9.91812332873117));
#95943=CARTESIAN_POINT('Ctrl Pts',(-0.524351231736321,1.8856531990772,9.88108611190269));
#95944=CARTESIAN_POINT('Ctrl Pts',(0.0986487328729629,2.05889277023303,
9.84404889507421));
#95945=CARTESIAN_POINT('Ctrl Pts',(0.815989920157508,1.89286452299667,9.80701167824573));
#95946=CARTESIAN_POINT('Ctrl Pts',(1.29952003507049,1.46351732792493,9.76997446141725));
#95947=CARTESIAN_POINT('Ctrl Pts',(1.78305014998348,1.03417013285319,9.73293724458878));
#95948=CARTESIAN_POINT('Ctrl Pts',(2.0327691925249,0.341503989946047,9.69590002776029));
#95949=CARTESIAN_POINT('Ctrl Pts',(1.9344406978275,-0.297614493697593,9.65886281093182));
#95950=CARTESIAN_POINT('Ctrl Pts',(1.8361122031301,-0.936732977341234,9.62182559410334));
#95951=CARTESIAN_POINT('Ctrl Pts',(1.38973617119388,-1.52230380172138,9.58478837727486));
#95952=CARTESIAN_POINT('Ctrl Pts',(0.799511084736072,-1.78645358874384,
9.54775116044638));
#95953=CARTESIAN_POINT('Ctrl Pts',(0.209285998278261,-2.0506033757663,9.5107139436179));
#95954=CARTESIAN_POINT('Ctrl Pts',(-0.524788142701144,-1.99333212543108,
9.47367672678942));
#95955=CARTESIAN_POINT('Ctrl Pts',(-1.06690354347858,-1.6408387214268,9.43663950996094));
#95956=CARTESIAN_POINT('Ctrl Pts',(-1.60735113766186,-1.28942975594381,
9.3997162373487));
#95957=CARTESIAN_POINT('Ctrl Pts',(-1.95701928883641,-0.644612332051665,
9.36279296473647));
#95958=CARTESIAN_POINT('Ctrl Pts',(-1.95719986784682,3.71606954582295E-5,
9.32586969212424));
#95959=CARTESIAN_POINT('Ctrl Pts',(-1.95707453392556,-0.000466568259871601,
9.22413030787576));
#95960=CARTESIAN_POINT('Ctrl Pts',(-1.95715585687005,-0.0257432861687418,
9.22557782057934));
#95961=CARTESIAN_POINT('Ctrl Pts',(-1.95670857405052,-0.0510170594794435,
9.22702533328292));
#95962=CARTESIAN_POINT('Ctrl Pts',(-1.95572375776859,-0.0762698699047084,
9.2284728459865));
#95963=CARTESIAN_POINT('Ctrl Pts',(-1.93050850489432,-0.722843258614067,
9.26553498593022));
#95964=CARTESIAN_POINT('Ctrl Pts',(-1.55290475731554,-1.35567409888606,
9.30259712587394));
#95965=CARTESIAN_POINT('Ctrl Pts',(-0.995863227266852,-1.68491214354887,
9.33965926581766));
#95966=CARTESIAN_POINT('Ctrl Pts',(-0.438821697218168,-2.01415018821168,
9.37672140576139));
#95967=CARTESIAN_POINT('Ctrl Pts',(0.297657615300397,-2.03979543726533,
9.4137835457051));
#95968=CARTESIAN_POINT('Ctrl Pts',(0.876251218790847,-1.75010180082627,
9.45084568564882));
#95969=CARTESIAN_POINT('Ctrl Pts',(1.45484482228131,-1.46040816438721,9.48790782559255));
#95970=CARTESIAN_POINT('Ctrl Pts',(1.87555271674363,-0.855375642455424,
9.52496996553627));
#95971=CARTESIAN_POINT('Ctrl Pts',(1.94568154283725,-0.21212227253196,9.56203210547999));
#95972=CARTESIAN_POINT('Ctrl Pts',(2.01581036893087,0.431131097391505,9.59909424542371));
#95973=CARTESIAN_POINT('Ctrl Pts',(1.73536012665579,1.11260531530666,9.63615638536743));
#95974=CARTESIAN_POINT('Ctrl Pts',(1.23278314419194,1.52017044141902,9.67321852531115));
#95975=CARTESIAN_POINT('Ctrl Pts',(0.730206161728088,1.92773556753138,9.71028066525487));
#95976=CARTESIAN_POINT('Ctrl Pts',(0.00550243907548716,2.06139160184095,
9.74734280519859));
#95977=CARTESIAN_POINT('Ctrl Pts',(-0.609398062732146,1.85992111567971,
9.78440494514231));
#95978=CARTESIAN_POINT('Ctrl Pts',(-1.22429856453979,1.65845062951848,9.82146708508603));
#95979=CARTESIAN_POINT('Ctrl Pts',(-1.72939584550245,1.12185362288641,9.85852922502976));
#95980=CARTESIAN_POINT('Ctrl Pts',(-1.89334427223443,0.495903289718102,
9.89559136497348));
#95981=CARTESIAN_POINT('Ctrl Pts',(-1.93542598326109,0.335236538822793,
9.90510434594091));
#95982=CARTESIAN_POINT('Ctrl Pts',(-1.95503184094814,0.168682937546108,
9.91461732690834));
#95983=CARTESIAN_POINT('Ctrl Pts',(-1.9535343393295,0.00178280253715055,
9.92413030787576));
#95984=CARTESIAN_POINT('Origin',(0.,0.,0.));
#95985=CARTESIAN_POINT('',(-1.95129684289216,-0.00113636086278679,10.7258696921242));
#95986=CARTESIAN_POINT('',(-1.95093054978418,-0.000550606481354719,10.6241303078758));
#95987=CARTESIAN_POINT('',(-1.954,-2.39295984553393E-16,0.));
#95988=CARTESIAN_POINT('Ctrl Pts',(-1.95129684289216,-0.00113636086278679,
10.7258696921242));
#95989=CARTESIAN_POINT('Ctrl Pts',(-1.94942963316978,0.391854106201406,
10.7035356831831));
#95990=CARTESIAN_POINT('Ctrl Pts',(-1.83442754086643,0.785903964976412,
10.6812016742419));
#95991=CARTESIAN_POINT('Ctrl Pts',(-1.61381630858742,1.10744756631717,10.6588676653008));
#95992=CARTESIAN_POINT('Ctrl Pts',(-1.24796949325566,1.64067382739912,10.6218304484723));
#95993=CARTESIAN_POINT('Ctrl Pts',(-0.591690439027595,1.97450300329055,
10.5847932316438));
#95994=CARTESIAN_POINT('Ctrl Pts',(0.0547076636758263,1.95640786233593,
10.5477560148153));
#95995=CARTESIAN_POINT('Ctrl Pts',(0.701105766379276,1.9383127213813,10.5107187979868));
#95996=CARTESIAN_POINT('Ctrl Pts',(1.33762291755807,1.56829326358058,10.4736815811584));
#95997=CARTESIAN_POINT('Ctrl Pts',(1.67312833478204,1.01552035674769,10.4366443643299));
#95998=CARTESIAN_POINT('Ctrl Pts',(2.00863375200599,0.462747449914819,10.3996071475014));
#95999=CARTESIAN_POINT('Ctrl Pts',(2.04312743527515,-0.272778905950186,
10.3625699306729));
#96000=CARTESIAN_POINT('Ctrl Pts',(1.7608042651717,-0.854535269464722,10.3255327138444));
#96001=CARTESIAN_POINT('Ctrl Pts',(1.47848109506825,-1.43629163297926,10.288495497016));
#96002=CARTESIAN_POINT('Ctrl Pts',(0.879341071592168,-1.86427800414334,
10.2514582801875));
#96003=CARTESIAN_POINT('Ctrl Pts',(0.237478981470821,-1.94273555725334,
10.214421063359));
#96004=CARTESIAN_POINT('Ctrl Pts',(-0.404383108650536,-2.02119311036335,
10.1773838465305));
#96005=CARTESIAN_POINT('Ctrl Pts',(-1.08896726541717,-1.75012184541928,
10.140346629702));
#96006=CARTESIAN_POINT('Ctrl Pts',(-1.5031122201388,-1.25351130806383,10.1033094128736));
#96007=CARTESIAN_POINT('Ctrl Pts',(-1.7917522457641,-0.907396556226723,
10.0774961726238));
#96008=CARTESIAN_POINT('Ctrl Pts',(-1.94902777514884,-0.451727225472274,
10.051682932374));
#96009=CARTESIAN_POINT('Ctrl Pts',(-1.95268202714777,0.00165579016441021,
10.0258696921242));
#96010=CARTESIAN_POINT('Ctrl Pts',(-1.9535343393295,0.00178280253715055,
9.92413030787576));
#96011=CARTESIAN_POINT('Ctrl Pts',(-1.94919764294582,-0.481552375812319,
9.95167946685205));
#96012=CARTESIAN_POINT('Ctrl Pts',(-1.76787653021499,-0.967793777264111,
9.97922862582834));
#96013=CARTESIAN_POINT('Ctrl Pts',(-1.44290486192301,-1.32238333502052,
10.0067777848046));
#96014=CARTESIAN_POINT('Ctrl Pts',(-1.00571745237828,-1.79941596688631,
10.0438399247484));
#96015=CARTESIAN_POINT('Ctrl Pts',(-0.308543060787511,-2.03817757091334,
10.0809020646921));
#96016=CARTESIAN_POINT('Ctrl Pts',(0.329297761185238,-1.92930969998698,
10.1179642046358));
#96017=CARTESIAN_POINT('Ctrl Pts',(0.967138583157977,-1.82044182906063,
10.1550263445795));
#96018=CARTESIAN_POINT('Ctrl Pts',(1.5456458355127,-1.36394448318089,10.1920884845232));
#96019=CARTESIAN_POINT('Ctrl Pts',(1.79984980484802,-0.76890421197536,10.229150624467));
#96020=CARTESIAN_POINT('Ctrl Pts',(2.05405377418334,-0.173863940769825,
10.2662127644107));
#96021=CARTESIAN_POINT('Ctrl Pts',(1.98395446049928,0.5597192557615,10.3032749043544));
#96022=CARTESIAN_POINT('Ctrl Pts',(1.62166047466929,1.09585000349956,10.3403370442981));
#96023=CARTESIAN_POINT('Ctrl Pts',(1.2593664888393,1.63198075123761,10.3773991842419));
#96024=CARTESIAN_POINT('Ctrl Pts',(0.604877830863377,1.9706590501824,10.4144613241856));
#96025=CARTESIAN_POINT('Ctrl Pts',(-0.042038551539475,1.95675976549601,
10.4515234641293));
#96026=CARTESIAN_POINT('Ctrl Pts',(-0.688954933942345,1.94286048080962,
10.488585604073));
#96027=CARTESIAN_POINT('Ctrl Pts',(-1.32829904077215,1.57638361249205,10.5256477440167));
#96028=CARTESIAN_POINT('Ctrl Pts',(-1.66723158702796,1.02518946943711,10.5627098839605));
#96029=CARTESIAN_POINT('Ctrl Pts',(-1.85446111291195,0.720704641366568,
10.5831833585989));
#96030=CARTESIAN_POINT('Ctrl Pts',(-1.95001820365716,0.359852200961074,
10.6036568332373));
#96031=CARTESIAN_POINT('Ctrl Pts',(-1.95093054978418,-0.000550606481354719,
10.6241303078758));
#96032=CARTESIAN_POINT('Origin',(0.,0.,-1.29405622560369));
#96033=CARTESIAN_POINT('',(-1.55334812646815,-0.000904610707407963,10.9559437743963));
#96034=CARTESIAN_POINT('',(-1.55659711405804,-0.00105088068675666,11.0940562256037));
#96035=CARTESIAN_POINT('',(-1.5555,-2.01987159101623E-13,-1.29405622560369));
#96036=CARTESIAN_POINT('',(0.499806597877791,1.47301514408978,11.4445));
#96037=CARTESIAN_POINT('Ctrl Pts',(-1.55334812646815,-0.000904610707408108,
10.9559437743963));
#96038=CARTESIAN_POINT('Ctrl Pts',(-1.55432667860164,-0.206859868644216,
10.9706469822836));
#96039=CARTESIAN_POINT('Ctrl Pts',(-1.42041322258558,-0.930327919713715,
11.0223874069994));
#96040=CARTESIAN_POINT('Ctrl Pts',(-0.324962964057439,-1.80887727526569,
11.1111650485437));
#96041=CARTESIAN_POINT('Ctrl Pts',(1.34445241673909,-1.25560970886474,11.2222766990291));
#96042=CARTESIAN_POINT('Ctrl Pts',(1.78171768593789,0.450698535437549,11.3333883495146));
#96043=CARTESIAN_POINT('Ctrl Pts',(0.989503531151977,1.30685679928735,11.4074627831715));
#96044=CARTESIAN_POINT('Ctrl Pts',(0.499806597877626,1.47301514408983,11.4445));
#96045=CARTESIAN_POINT('',(1.55548765964692,0.00619602180124784,11.4445));
#96046=CARTESIAN_POINT('Origin',(0.,0.,11.4445));
#96047=CARTESIAN_POINT('Ctrl Pts',(-1.55659711405804,-0.0010508806867568,
11.0940562256037));
#96048=CARTESIAN_POINT('Ctrl Pts',(-1.55726922058417,-0.079449137192624,
11.099684397238));
#96049=CARTESIAN_POINT('Ctrl Pts',(-1.51630179095532,-0.673453815214831,
11.142374708816));
#96050=CARTESIAN_POINT('Ctrl Pts',(-0.75277483453787,-1.67898453189698,
11.2221271603377));
#96051=CARTESIAN_POINT('Ctrl Pts',(1.00462758039806,-1.53944373403644,11.3333135801688));
#96052=CARTESIAN_POINT('Ctrl Pts',(1.55754888396286,-0.511266487217653,
11.4074378600563));
#96053=CARTESIAN_POINT('Ctrl Pts',(1.55548765964692,0.00619602180124784,
11.4445));
#96054=CARTESIAN_POINT('Origin',(0.,0.,-1.29405622560369));
#96055=CARTESIAN_POINT('',(-1.55445081536763,0.00131810726739325,10.2559437743963));
#96056=CARTESIAN_POINT('',(-1.55305653540906,-0.000438315446397164,10.3940562256037));
#96057=CARTESIAN_POINT('',(-1.5555,-2.01987159101623E-13,-1.29405622560369));
#96058=CARTESIAN_POINT('Ctrl Pts',(-1.55445081536763,0.00131810726739319,
10.2559437743963));
#96059=CARTESIAN_POINT('Ctrl Pts',(-1.55154181384031,-0.359601688445403,
10.2817570146461));
#96060=CARTESIAN_POINT('Ctrl Pts',(-1.24670140973274,-1.24280598265434,
10.3446074717243));
#96061=CARTESIAN_POINT('Ctrl Pts',(0.223056668548975,-1.82477852394609,
10.4444951456311));
#96062=CARTESIAN_POINT('Ctrl Pts',(1.65390974917898,-0.802670846854376,
10.5556067961165));
#96063=CARTESIAN_POINT('Ctrl Pts',(1.57153269033781,0.953897085409752,10.6667184466019));
#96064=CARTESIAN_POINT('Ctrl Pts',(0.0514163720288116,1.83756944970195,
10.7778300970874));
#96065=CARTESIAN_POINT('Ctrl Pts',(-1.30849536725084,1.14582374749785,10.8742385396855));
#96066=CARTESIAN_POINT('Ctrl Pts',(-1.55186171668149,0.311939131113674,
10.9336097654551));
#96067=CARTESIAN_POINT('Ctrl Pts',(-1.55334812646815,-0.000904610707408108,
10.9559437743963));
#96068=CARTESIAN_POINT('Ctrl Pts',(-1.55305653540906,-0.000438315446397077,
10.3940562256037));
#96069=CARTESIAN_POINT('Ctrl Pts',(-1.55364500629154,-0.232901140548306,
10.410644890909));
#96070=CARTESIAN_POINT('Ctrl Pts',(-1.39557528484751,-0.983968830408974,
10.464295696158));
#96071=CARTESIAN_POINT('Ctrl Pts',(-0.231259578302998,-1.82421227428175,
10.5550086413507));
#96072=CARTESIAN_POINT('Ctrl Pts',(1.40774638007895,-1.1829694620695,10.6661950611819));
#96073=CARTESIAN_POINT('Ctrl Pts',(1.75706993010233,0.541796064983141,10.7773814810131));
#96074=CARTESIAN_POINT('Ctrl Pts',(0.497080432048737,1.77049779856472,10.8885679008442));
#96075=CARTESIAN_POINT('Ctrl Pts',(-1.13185991314487,1.39680492671116,10.9941261490411));
#96076=CARTESIAN_POINT('Ctrl Pts',(-1.55284332390808,0.436812153822664,
11.0626222572943));
#96077=CARTESIAN_POINT('Ctrl Pts',(-1.55659711405804,-0.0010508806867568,
11.0940562256037));
#96078=CARTESIAN_POINT('Origin',(0.,0.,-1.29405622560369));
#96079=CARTESIAN_POINT('',(-1.55804728476752,2.95821195149996E-5,9.5559437743963));
#96080=CARTESIAN_POINT('',(-1.55512930646214,0.00141921665610299,9.69405622560371));
#96081=CARTESIAN_POINT('',(-1.5555,-2.01987159101623E-13,-1.29405622560369));
#96082=CARTESIAN_POINT('Ctrl Pts',(-1.55804728476752,2.95821195150548E-5,
9.5559437743963));
#96083=CARTESIAN_POINT('Ctrl Pts',(-1.55790353315504,-0.513149683984934,
9.59286704700854));
#96084=CARTESIAN_POINT('Ctrl Pts',(-1.00033131917675,-1.54135965233235,
9.66682753644926));
#96085=CARTESIAN_POINT('Ctrl Pts',(0.750970673805211,-1.67799333720618,
9.77782524271844));
#96086=CARTESIAN_POINT('Ctrl Pts',(1.81699613594968,-0.279545920640164,
9.88893689320389));
#96087=CARTESIAN_POINT('Ctrl Pts',(1.22062258834496,1.37466418983892,10.0000485436893));
#96088=CARTESIAN_POINT('Ctrl Pts',(-0.492515922639386,1.77116921324136,
10.1111601941748));
#96089=CARTESIAN_POINT('Ctrl Pts',(-1.46173837715872,0.831558022400444,
10.1964586044104));
#96090=CARTESIAN_POINT('Ctrl Pts',(-1.55571569202373,0.15825134364817,10.2447197978176));
#96091=CARTESIAN_POINT('Ctrl Pts',(-1.55445081536763,0.00131810726739319,
10.2559437743963));
#96092=CARTESIAN_POINT('Ctrl Pts',(-1.55512930646214,0.00141921665610296,
9.69405622560371));
#96093=CARTESIAN_POINT('Ctrl Pts',(-1.55167703869094,-0.383344278698275,
9.72160538457999));
#96094=CARTESIAN_POINT('Ctrl Pts',(-1.21314953523015,-1.29115961930375,
9.7862166835));
#96095=CARTESIAN_POINT('Ctrl Pts',(0.309373610575528,-1.81257875466721,
9.88789012236375));
#96096=CARTESIAN_POINT('Ctrl Pts',(1.69095195914933,-0.722381792257861,
9.99907654219489));
#96097=CARTESIAN_POINT('Ctrl Pts',(1.52354231364944,1.0295455294481,10.1102629620261));
#96098=CARTESIAN_POINT('Ctrl Pts',(-0.0394931635484403,1.83836962465064,
10.2214493818572));
#96099=CARTESIAN_POINT('Ctrl Pts',(-1.33855689695156,1.09373648628768,10.3160471363831));
#96100=CARTESIAN_POINT('Ctrl Pts',(-1.5523302537302,0.286463714736223,10.3735827509653));
#96101=CARTESIAN_POINT('Ctrl Pts',(-1.55305653540906,-0.000438315446397077,
10.3940562256037));
#96102=CARTESIAN_POINT('Origin',(0.,0.,-1.29405622560369));
#96103=CARTESIAN_POINT('',(-1.55453687436568,-0.00133745576774406,8.85594377439631));
#96104=CARTESIAN_POINT('',(-1.55794751152569,-0.000371416033132788,8.99405622560372));
#96105=CARTESIAN_POINT('',(-1.5555,-2.01987159101623E-13,-1.29405622560369));
#96106=CARTESIAN_POINT('Ctrl Pts',(-1.55453687436568,-0.00133745576774402,
8.85594377439631));
#96107=CARTESIAN_POINT('Ctrl Pts',(-1.55579877499581,-0.155062375664632,
8.86693986254252));
#96108=CARTESIAN_POINT('Ctrl Pts',(-1.46423861786649,-0.825096309536398,
8.91497316751722));
#96109=CARTESIAN_POINT('Ctrl Pts',(-0.503376402892206,-1.7681153483915,
9.00004368932038));
#96110=CARTESIAN_POINT('Ctrl Pts',(1.2121644264892,-1.38212772940753,9.11115533980582));
#96111=CARTESIAN_POINT('Ctrl Pts',(1.81867711471885,0.26839009932345,9.22226699029127));
#96112=CARTESIAN_POINT('Ctrl Pts',(0.761253709552246,1.67335367481701,9.33337864077668));
#96113=CARTESIAN_POINT('Ctrl Pts',(-0.99265255914171,1.54733978795034,9.44449029126215));
#96114=CARTESIAN_POINT('Ctrl Pts',(-1.55732851093913,0.517959404958592,
9.51867866913534));
#96115=CARTESIAN_POINT('Ctrl Pts',(-1.55804772838109,0.00161323939398619,
9.55582983018006));
#96116=CARTESIAN_POINT('Ctrl Pts',(-1.55804728476752,2.95821195150548E-5,
9.5559437743963));
#96117=CARTESIAN_POINT('Ctrl Pts',(-1.55794751152569,-0.000371416033132616,
8.99405622560372));
#96118=CARTESIAN_POINT('Ctrl Pts',(-1.55801224941728,-0.020493184051098,
8.99550373830729));
#96119=CARTESIAN_POINT('Ctrl Pts',(-1.54853952527048,-0.55575068168544,
9.03401339095459));
#96120=CARTESIAN_POINT('Ctrl Pts',(-0.935609375970031,-1.5829679799695,
9.1095851835456));
#96121=CARTESIAN_POINT('Ctrl Pts',(0.823234386500799,-1.64421340203127,
9.22077160337675));
#96122=CARTESIAN_POINT('Ctrl Pts',(1.82795976495949,-0.199287985657338,
9.33195802320793));
#96123=CARTESIAN_POINT('Ctrl Pts',(1.15819463928053,1.42819381470141,9.44314444303908));
#96124=CARTESIAN_POINT('Ctrl Pts',(-0.572526917402423,1.74738822826618,
9.55433086287024));
#96125=CARTESIAN_POINT('Ctrl Pts',(-1.47990815776177,0.783419353749631,
9.63796812372513));
#96126=CARTESIAN_POINT('Ctrl Pts',(-1.5563214066504,0.1342816322173,9.68454324463628));
#96127=CARTESIAN_POINT('Ctrl Pts',(-1.55512930646214,0.00141921665610296,
9.69405622560371));
#96128=CARTESIAN_POINT('Origin',(0.,0.,-1.29405622560369));
#96129=CARTESIAN_POINT('',(-1.55333906144275,0.000780263919018194,8.15594377439631));
#96130=CARTESIAN_POINT('',(-1.55403083159801,-0.00119596074553197,8.29405622560371));
#96131=CARTESIAN_POINT('',(-1.5555,-2.01987159101623E-13,-1.29405622560369));
#96132=CARTESIAN_POINT('Ctrl Pts',(-1.55333906144275,0.000780263919018167,
8.15594377439631));
#96133=CARTESIAN_POINT('Ctrl Pts',(-1.55193217426013,-0.308862600127516,
8.17804989490498));
#96134=CARTESIAN_POINT('Ctrl Pts',(-1.3122308335565,-1.13929638534857,8.23719323224213));
#96135=CARTESIAN_POINT('Ctrl Pts',(0.0400949547363229,-1.83793690702293,
8.33337378640777));
#96136=CARTESIAN_POINT('Ctrl Pts',(1.56567267939011,-0.963477420579929,
8.44448543689319));
#96137=CARTESIAN_POINT('Ctrl Pts',(1.65879203582308,0.792482593671729,8.55559708737864));
#96138=CARTESIAN_POINT('Ctrl Pts',(0.234256671005791,1.82338791618694,8.66670873786407));
#96139=CARTESIAN_POINT('Ctrl Pts',(-1.24241507899534,1.24912116508194,8.7668243002033));
#96140=CARTESIAN_POINT('Ctrl Pts',(-1.55154841917538,0.362716593952071,
8.82990264571404));
#96141=CARTESIAN_POINT('Ctrl Pts',(-1.55453687436568,-0.00133745576774402,
8.85594377439631));
#96142=CARTESIAN_POINT('Ctrl Pts',(-1.55403083159801,-0.00119596074553188,
8.29405622560371));
#96143=CARTESIAN_POINT('Ctrl Pts',(-1.55527408252746,-0.17480188940304,
8.30646423197829));
#96144=CARTESIAN_POINT('Ctrl Pts',(-1.4483135129372,-0.865473027753662,
8.3559343782966));
#96145=CARTESIAN_POINT('Ctrl Pts',(-0.434704832044991,-1.78666848096071,
8.44246666455862));
#96146=CARTESIAN_POINT('Ctrl Pts',(1.26590215885116,-1.33365823077974,8.55365308438979));
#96147=CARTESIAN_POINT('Ctrl Pts',(1.8068878531032,0.341040818691465,8.66483950422094));
#96148=CARTESIAN_POINT('Ctrl Pts',(0.69268588294083,1.70333168137465,8.77602592405212));
#96149=CARTESIAN_POINT('Ctrl Pts',(-1.03328002592178,1.50787500329959,8.88576483117969));
#96150=CARTESIAN_POINT('Ctrl Pts',(-1.55635469933735,0.494704907375218,
8.95844159836357));
#96151=CARTESIAN_POINT('Ctrl Pts',(-1.55794751152569,-0.000371416033132616,
8.99405622560372));
#96152=CARTESIAN_POINT('Origin',(0.,0.,-1.29405622560369));
#96153=CARTESIAN_POINT('',(-1.55738164088485,0.00090367155389158,7.45594377439631));
#96154=CARTESIAN_POINT('',(-1.55363820104426,0.00100737127591941,7.59405622560371));
#96155=CARTESIAN_POINT('',(-1.5555,-2.01987159101623E-13,-1.29405622560369));
#96156=CARTESIAN_POINT('Ctrl Pts',(-1.55738164088485,0.000903671553891608,
7.45594377439631));
#96157=CARTESIAN_POINT('Ctrl Pts',(-1.55418612064456,-0.461276292775272,
7.48915992726744));
#96158=CARTESIAN_POINT('Ctrl Pts',(-1.09121796390773,-1.44436334125619,
7.55941329696705));
#96159=CARTESIAN_POINT('Ctrl Pts',(0.580004387659595,-1.74448118065669,
7.66670388349515));
#96160=CARTESIAN_POINT('Ctrl Pts',(1.7800908511122,-0.459234407622611,7.77781553398057));
#96161=CARTESIAN_POINT('Ctrl Pts',(1.35154441460109,1.24617309179735,7.88892718446602));
#96162=CARTESIAN_POINT('Ctrl Pts',(-0.313551099181417,1.81143738163968,
8.00003883495145));
#96163=CARTESIAN_POINT('Ctrl Pts',(-1.41757073229054,0.936656796997624,
8.08904436492822));
#96164=CARTESIAN_POINT('Ctrl Pts',(-1.55428931266511,0.209921774117757,
8.1410126780765));
#96165=CARTESIAN_POINT('Ctrl Pts',(-1.55333906144275,0.000780263919018167,
8.15594377439631));
#96166=CARTESIAN_POINT('Ctrl Pts',(-1.55363820104426,0.00100737127591942,
7.59405622560371));
#96167=CARTESIAN_POINT('Ctrl Pts',(-1.55169765832855,-0.326159426902871,
7.6174247256493));
#96168=CARTESIAN_POINT('Ctrl Pts',(-1.29071878250434,-1.17503987929593,
7.67785536563862));
#96169=CARTESIAN_POINT('Ctrl Pts',(0.103792628149562,-1.8358593744105,7.77534814557165));
#96170=CARTESIAN_POINT('Ctrl Pts',(1.59909575810308,-0.907769413831382,
7.8865345654028));
#96171=CARTESIAN_POINT('Ctrl Pts',(1.62955779866738,0.851876712390422,7.99772098523398));
#96172=CARTESIAN_POINT('Ctrl Pts',(0.167274199086701,1.83116681231986,8.10890740506512));
#96173=CARTESIAN_POINT('Ctrl Pts',(-1.26795424285233,1.21093838634352,8.20768581852172));
#96174=CARTESIAN_POINT('Ctrl Pts',(-1.55156054962447,0.343750973057136,
8.26940209203457));
#96175=CARTESIAN_POINT('Ctrl Pts',(-1.55403083159801,-0.00119596074553188,
8.29405622560371));
#96176=CARTESIAN_POINT('Origin',(0.,0.,-1.29405622560369));
#96177=CARTESIAN_POINT('',(-1.55606466149984,-0.00136591087330588,6.7559437743963));
#96178=CARTESIAN_POINT('',(-1.55769406638298,0.000677585252333857,6.89405622560371));
#96179=CARTESIAN_POINT('',(-1.5555,-2.01987159101623E-13,-1.29405622560369));
#96180=CARTESIAN_POINT('Ctrl Pts',(-1.55606466149984,-0.00136591087330577,
6.7559437743963));
#96181=CARTESIAN_POINT('Ctrl Pts',(-1.55699698050756,-0.10301028373747,
6.76323274280142));
#96182=CARTESIAN_POINT('Ctrl Pts',(-1.50160999329305,-0.720125819190329,
6.80755892803501));
#96183=CARTESIAN_POINT('Ctrl Pts',(-0.677079673289082,-1.70914680334463,
6.8889223300971));
#96184=CARTESIAN_POINT('Ctrl Pts',(1.06838781720774,-1.49605051766532,7.00003398058251));
#96185=CARTESIAN_POINT('Ctrl Pts',(1.83637062036826,0.0858057341481814,
7.11114563106797));
#96186=CARTESIAN_POINT('Ctrl Pts',(0.924229284360448,1.589156980696,7.22225728155339));
#96187=CARTESIAN_POINT('Ctrl Pts',(-0.833503847528551,1.63856370505402,
7.33336893203883));
#96188=CARTESIAN_POINT('Ctrl Pts',(-1.53115801604342,0.622214122864029,
7.41126442965314));
#96189=CARTESIAN_POINT('Ctrl Pts',(-1.55774924177056,0.0540711533618156,
7.45212271043896));
#96190=CARTESIAN_POINT('Ctrl Pts',(-1.55738164088485,0.000903671553891608,
7.45594377439631));
#96191=CARTESIAN_POINT('Ctrl Pts',(-1.55769406638298,0.000677585252333878,
6.89405622560371));
#96192=CARTESIAN_POINT('Ctrl Pts',(-1.55508734647919,-0.476733936548398,
6.92838521932031));
#96193=CARTESIAN_POINT('Ctrl Pts',(-1.06472330039144,-1.47419539900055,
6.99977635298063));
#96194=CARTESIAN_POINT('Ctrl Pts',(0.633314188332071,-1.72628667698419,
7.10822962658467));
#96195=CARTESIAN_POINT('Ctrl Pts',(1.7940008868909,-0.403377453646542,7.21941604641583));
#96196=CARTESIAN_POINT('Ctrl Pts',(1.31130494233742,1.28904301731096,7.33060246624699));
#96197=CARTESIAN_POINT('Ctrl Pts',(-0.372603218894873,1.80064416072257,
7.44178888607816));
#96198=CARTESIAN_POINT('Ctrl Pts',(-1.43301362666466,0.901927254173143,
7.52960680586373));
#96199=CARTESIAN_POINT('Ctrl Pts',(-1.55477533406966,0.192722899107996,
7.58036258570558));
#96200=CARTESIAN_POINT('Ctrl Pts',(-1.55363820104426,0.00100737127591942,
7.59405622560371));
#96201=CARTESIAN_POINT('Origin',(0.,0.,-1.29405622560369));
#96202=CARTESIAN_POINT('',(-1.55295085115974,-2.74912889200857E-5,6.0559437743963));
#96203=CARTESIAN_POINT('',(-1.55567057787938,-0.00141549514015751,6.19405622560371));
#96204=CARTESIAN_POINT('',(-1.5555,-2.01987159101623E-13,-1.29405622560369));
#96205=CARTESIAN_POINT('Ctrl Pts',(-1.55295114066544,-2.74881667468134E-5,
6.0559437743963));
#96206=CARTESIAN_POINT('Ctrl Pts',(-1.55299180574127,-0.257905198155464,
6.07434277516388));
#96207=CARTESIAN_POINT('Ctrl Pts',(-1.37005956536857,-1.03483686203599,
6.12977899275993));
#96208=CARTESIAN_POINT('Ctrl Pts',(-0.143272298638598,-1.83278278249422,
6.22225242718446));
#96209=CARTESIAN_POINT('Ctrl Pts',(1.46185859526926,-1.11471481859797,6.33336407766989));
#96210=CARTESIAN_POINT('Ctrl Pts',(1.72951224644592,0.623223129190563,6.44447572815534));
#96211=CARTESIAN_POINT('Ctrl Pts',(0.414808152398764,1.79096450999678,6.55558737864077));
#96212=CARTESIAN_POINT('Ctrl Pts',(-1.1682689842466,1.35101180160119,6.6594100607211));
#96213=CARTESIAN_POINT('Ctrl Pts',(-1.55225961585962,0.413472223515983,
6.72619552597294));
#96214=CARTESIAN_POINT('Ctrl Pts',(-1.55606466149984,-0.00136591087330577,
6.7559437743963));
#96215=CARTESIAN_POINT('Ctrl Pts',(-1.55567057787938,-0.00141549514015748,
6.19405622560371));
#96216=CARTESIAN_POINT('Ctrl Pts',(-1.55673152840384,-0.11622012238534,
6.2022835730476));
#96217=CARTESIAN_POINT('Ctrl Pts',(-1.49271086742403,-0.747018195902368,
6.2475730604352));
#96218=CARTESIAN_POINT('Ctrl Pts',(-0.632665469493242,-1.72652453095426,
6.32992468776653));
#96219=CARTESIAN_POINT('Ctrl Pts',(1.10806726459172,-1.46742614445027,6.44111110759769));
#96220=CARTESIAN_POINT('Ctrl Pts',(1.83376231205259,0.135898253011021,6.55229752742886));
#96221=CARTESIAN_POINT('Ctrl Pts',(0.879651525947856,1.61473395492061,6.66348394726001));
#96222=CARTESIAN_POINT('Ctrl Pts',(-0.880258220622017,1.61440330069759,
6.77467036709119));
#96223=CARTESIAN_POINT('Ctrl Pts',(-1.53940153309356,0.591912849892102,
6.85152779320574));
#96224=CARTESIAN_POINT('Ctrl Pts',(-1.55790160368306,0.0386873070159844,
6.89132307937659));
#96225=CARTESIAN_POINT('Ctrl Pts',(-1.55769406638298,0.000677585252333878,
6.89405622560371));
#96226=CARTESIAN_POINT('Origin',(0.,0.,-1.29405622560369));
#96227=CARTESIAN_POINT('',(-1.55596383579478,0.00138071545366175,5.3559437743963));
#96228=CARTESIAN_POINT('',(-1.5529563387483,0.000151106445085702,5.49405622560371));
#96229=CARTESIAN_POINT('',(-1.5555,-2.01987159101623E-13,-1.29405622560369));
#96230=CARTESIAN_POINT('Ctrl Pts',(-1.55596383579478,0.00138071545366179,
5.3559437743963));
#96231=CARTESIAN_POINT('Ctrl Pts',(-1.55217514150148,-0.410190199764792,
5.38545280752634));
#96232=CARTESIAN_POINT('Ctrl Pts',(-1.17330640529453,-1.34449549172498,
5.45199905748485));
#96233=CARTESIAN_POINT('Ctrl Pts',(0.403262995152723,-1.79359935217008,
5.55558252427184));
#96234=CARTESIAN_POINT('Ctrl Pts',(1.72546185411942,-0.634350903950841,
5.66669417475728));
#96235=CARTESIAN_POINT('Ctrl Pts',(1.46900873501267,1.1052750860401,5.77780582524271));
#96236=CARTESIAN_POINT('Ctrl Pts',(-0.13146340126236,1.83366765077345,5.88891747572816));
#96237=CARTESIAN_POINT('Ctrl Pts',(-1.36655195880861,1.04159698732297,5.98163012544601));
#96238=CARTESIAN_POINT('Ctrl Pts',(-1.55290994688111,0.261203028467153,
6.0373055583354));
#96239=CARTESIAN_POINT('Ctrl Pts',(-1.55295114066544,-2.74881667468134E-5,
6.0559437743963));
#96240=CARTESIAN_POINT('Ctrl Pts',(-1.5529563387483,0.000151106445085633,
5.49405622560371));
#96241=CARTESIAN_POINT('Ctrl Pts',(-1.55272340811799,-0.268780222436924,
5.5132440667186));
#96242=CARTESIAN_POINT('Ctrl Pts',(-1.35831396530156,-1.05747938365068,
5.56949404777722));
#96243=CARTESIAN_POINT('Ctrl Pts',(-0.103102773360761,-1.83589824620028,
5.66280616877956));
#96244=CARTESIAN_POINT('Ctrl Pts',(1.4869956060099,-1.08166382022474,5.77399258861071));
#96245=CARTESIAN_POINT('Ctrl Pts',(1.71494149863546,0.663421591850831,5.88517900844189));
#96246=CARTESIAN_POINT('Ctrl Pts',(0.371926577693494,1.80078404398782,5.99636542827304));
#96247=CARTESIAN_POINT('Ctrl Pts',(-1.18720103315053,1.32645343006727,6.09932450066032));
#96248=CARTESIAN_POINT('Ctrl Pts',(-1.55195221197423,0.40094597399841,6.16522143310387));
#96249=CARTESIAN_POINT('Ctrl Pts',(-1.55567057787938,-0.00141549514015748,
6.19405622560371));
#96250=CARTESIAN_POINT('Origin',(0.,0.,-1.29405622560369));
#96251=CARTESIAN_POINT('',(-1.55745492001379,-0.000856371120316566,4.6559437743963));
#96252=CARTESIAN_POINT('',(-1.55622585425313,0.00134239099646036,4.79405622560371));
#96253=CARTESIAN_POINT('',(-1.5555,-2.01987159101623E-13,-1.29405622560369));
#96254=CARTESIAN_POINT('Ctrl Pts',(-1.55745492001379,-0.000856371120316864,
4.65594377439631));
#96255=CARTESIAN_POINT('Ctrl Pts',(-1.5577850741697,-0.0506891626144068,
4.65952562306032));
#96256=CARTESIAN_POINT('Ctrl Pts',(-1.53301192978291,-0.615473136307116,
4.70014468855281));
#96257=CARTESIAN_POINT('Ctrl Pts',(-0.844041411881997,-1.63316067010957,
4.77780097087378));
#96258=CARTESIAN_POINT('Ctrl Pts',(0.913973507436636,-1.59507746114991,
4.88891262135923));
#96259=CARTESIAN_POINT('Ctrl Pts',(1.83577980123458,-0.0976329900371924,
5.00002427184466));
#96260=CARTESIAN_POINT('Ctrl Pts',(1.0780025055099,1.48913742733129,5.1111359223301));
#96261=CARTESIAN_POINT('Ctrl Pts',(-0.666056105926533,1.7134727727987,5.22224757281553));
#96262=CARTESIAN_POINT('Ctrl Pts',(-1.49938299705611,0.726891414718789,
5.30385019017093));
#96263=CARTESIAN_POINT('Ctrl Pts',(-1.55693038683329,0.106378444150779,
5.34841559069786));
#96264=CARTESIAN_POINT('Ctrl Pts',(-1.55596383579478,0.00138071545366179,
5.3559437743963));
#96265=CARTESIAN_POINT('Ctrl Pts',(-1.55622585425313,0.00134239099646029,
4.79405622560371));
#96266=CARTESIAN_POINT('Ctrl Pts',(-1.55239700220769,-0.418962472451577,
4.82420456038961));
#96267=CARTESIAN_POINT('Ctrl Pts',(-1.15964303797854,-1.36226320639006,
4.89141503511923));
#96268=CARTESIAN_POINT('Ctrl Pts',(0.435376164803608,-1.7865050090601,4.99568764979258));
#96269=CARTESIAN_POINT('Ctrl Pts',(1.73732980498774,-0.602360109052031,
5.10687406962374));
#96270=CARTESIAN_POINT('Ctrl Pts',(1.44781397169404,1.13357278356683,5.21806048945491));
#96271=CARTESIAN_POINT('Ctrl Pts',(-0.167962271460079,1.83110382765203,
5.32924690928607));
#96272=CARTESIAN_POINT('Ctrl Pts',(-1.37758975876034,1.02035875886683,5.42124548800234));
#96273=CARTESIAN_POINT('Ctrl Pts',(-1.55317332364345,0.250672199885809,
5.47618192677488));
#96274=CARTESIAN_POINT('Ctrl Pts',(-1.5529563387483,0.000151106445085633,
5.49405622560371));
#96275=CARTESIAN_POINT('Origin',(0.,0.,-1.29405622560369));
#96276=CARTESIAN_POINT('',(-1.55339129538237,-0.00082587420025254,3.9559437743963));
#96277=CARTESIAN_POINT('',(-1.5573160577951,-0.00094952305265919,4.09405622560371));
#96278=CARTESIAN_POINT('',(-1.5555,-2.01987159101623E-13,-1.29405622560369));
#96279=CARTESIAN_POINT('Ctrl Pts',(-1.55339129538237,-0.000825874200252562,
3.9559437743963));
#96280=CARTESIAN_POINT('Ctrl Pts',(-1.55438295724494,-0.206599346759669,
3.97063565542278));
#96281=CARTESIAN_POINT('Ctrl Pts',(-1.42062281789543,-0.929876204718288,
4.02236475327773));
#96282=CARTESIAN_POINT('Ctrl Pts',(-0.325213021862407,-1.80938005122649,
4.11113106796117));
#96283=CARTESIAN_POINT('Ctrl Pts',(1.34348911316817,-1.25485325124609,4.2222427184466));
#96284=CARTESIAN_POINT('Ctrl Pts',(1.78301209192838,0.447758371671112,4.33335436893204));
#96285=CARTESIAN_POINT('Ctrl Pts',(0.591229481908682,1.74070887258225,4.44446601941748));
#96286=CARTESIAN_POINT('Ctrl Pts',(-1.0856218085317,1.45071736103991,4.55199582123889));
#96287=CARTESIAN_POINT('Ctrl Pts',(-1.55437119708937,0.464594445617744,
4.62248840623184));
#96288=CARTESIAN_POINT('Ctrl Pts',(-1.55745492001379,-0.000856371120316864,
4.65594377439631));
#96289=CARTESIAN_POINT('Ctrl Pts',(-1.5573160577951,-0.000949523052659442,
4.0940562256037));
#96290=CARTESIAN_POINT('Ctrl Pts',(-1.55772052747877,-0.0572626470532979,
4.0981029141169));
#96291=CARTESIAN_POINT('Ctrl Pts',(-1.52938259291224,-0.628915705084586,
4.13921174257381));
#96292=CARTESIAN_POINT('Ctrl Pts',(-0.822616502622442,-1.64452261823584,
4.21738271097444));
#96293=CARTESIAN_POINT('Ctrl Pts',(0.936204134582059,-1.58261630557358,
4.3285691308056));
#96294=CARTESIAN_POINT('Ctrl Pts',(1.83742116834086,-0.0709647969689106,
4.43975555063676));
#96295=CARTESIAN_POINT('Ctrl Pts',(1.0554806974386,1.50569354438759,4.55094197046793));
#96296=CARTESIAN_POINT('Ctrl Pts',(-0.693325883166112,1.70307127625589,
4.66212839029909));
#96297=CARTESIAN_POINT('Ctrl Pts',(-1.50503746143118,0.709862178387775,
4.74316647534435));
#96298=CARTESIAN_POINT('Ctrl Pts',(-1.55710391061042,0.0977293375193425,
4.78714242044589));
#96299=CARTESIAN_POINT('Ctrl Pts',(-1.55622585425313,0.00134239099646029,
4.79405622560371));
#96300=CARTESIAN_POINT('Origin',(0.,0.,-1.29405622560369));
#96301=CARTESIAN_POINT('',(-1.55444674488022,0.00131742778884735,3.2559437743963));
#96302=CARTESIAN_POINT('',(-1.5533186684889,-0.000770198572060954,3.39405622560371));
#96303=CARTESIAN_POINT('',(-1.5555,-2.01987159101623E-13,-1.29405622560369));
#96304=CARTESIAN_POINT('Ctrl Pts',(-1.55444674488022,0.00131742778884739,
3.2559437743963));
#96305=CARTESIAN_POINT('Ctrl Pts',(-1.55154236665719,-0.359445316439912,
3.28174568778523));
#96306=CARTESIAN_POINT('Ctrl Pts',(-1.24691611905359,-1.24248704432008,
3.34458481800264));
#96307=CARTESIAN_POINT('Ctrl Pts',(0.222506403513669,-1.8248590575151,3.44446116504855));
#96308=CARTESIAN_POINT('Ctrl Pts',(1.65365282072159,-0.803151310699741,
3.55557281553397));
#96309=CARTESIAN_POINT('Ctrl Pts',(1.57184646516792,0.953372104320743,3.66668446601942));
#96310=CARTESIAN_POINT('Ctrl Pts',(0.0519332482321354,1.83764050268212,
3.77779611650485));
#96311=CARTESIAN_POINT('Ctrl Pts',(-1.30823935507303,1.14600960175539,3.87421588596382));
#96312=CARTESIAN_POINT('Ctrl Pts',(-1.55188304621527,0.312141358191517,
3.9335984385943));
#96313=CARTESIAN_POINT('Ctrl Pts',(-1.55339129538237,-0.000825874200252562,
3.9559437743963));
#96314=CARTESIAN_POINT('Ctrl Pts',(-1.5533186684889,-0.000770198572060919,
3.39405622560371));
#96315=CARTESIAN_POINT('Ctrl Pts',(-1.5542597194186,-0.210984061911746,
3.4090634077879));
#96316=CARTESIAN_POINT('Ctrl Pts',(-1.41654850766895,-0.939166341982764,
3.46113272991582));
#96317=CARTESIAN_POINT('Ctrl Pts',(-0.308692884081366,-1.81269447386996,
3.55026419198746));
#96318=CARTESIAN_POINT('Ctrl Pts',(1.35606994996762,-1.24186426112907,3.66145061181863));
#96319=CARTESIAN_POINT('Ctrl Pts',(1.77861387826841,0.466567491694538,3.77263703164979));
#96320=CARTESIAN_POINT('Ctrl Pts',(0.571870330903418,1.74760318061885,3.88382345148095));
#96321=CARTESIAN_POINT('Ctrl Pts',(-1.09574509035902,1.43939945308724,3.99096318279893));
#96322=CARTESIAN_POINT('Ctrl Pts',(-1.55401613758806,0.458488658137791,
4.06104077417318));
#96323=CARTESIAN_POINT('Ctrl Pts',(-1.5573160577951,-0.000949523052659442,
4.0940562256037));
#96324=CARTESIAN_POINT('Origin',(0.,0.,-1.29405622560369));
#96325=CARTESIAN_POINT('',(-1.55804712705668,3.25009013604671E-5,2.5559437743963));
#96326=CARTESIAN_POINT('',(-1.55449947323643,0.00133480041304715,2.69405622560371));
#96327=CARTESIAN_POINT('',(-1.5555,-2.01987159101623E-13,-1.29405622560369));
#96328=CARTESIAN_POINT('Ctrl Pts',(-1.55804712705668,3.25009013604029E-5,
2.5559437743963));
#96329=CARTESIAN_POINT('Ctrl Pts',(-1.55788927539753,-0.512989453804214,
2.59285572014769));
#96330=CARTESIAN_POINT('Ctrl Pts',(-1.0006227616332,-1.54106832868198,2.66680488272757));
#96331=CARTESIAN_POINT('Ctrl Pts',(0.750458968510211,-1.67822257683237,
2.77779126213592));
#96332=CARTESIAN_POINT('Ctrl Pts',(1.81691053470019,-0.280099604209337,
2.88890291262136));
#96333=CARTESIAN_POINT('Ctrl Pts',(1.22104229764526,1.37429086670804,3.0000145631068));
#96334=CARTESIAN_POINT('Ctrl Pts',(-0.491976593161155,1.77132117679823,
3.11112621359223));
#96335=CARTESIAN_POINT('Ctrl Pts',(-1.46161229246342,0.831876851886141,
3.19643595068874));
#96336=CARTESIAN_POINT('Ctrl Pts',(-1.55571144064704,0.158409610837222,
3.24470847095676));
#96337=CARTESIAN_POINT('Ctrl Pts',(-1.55444674488022,0.00131742778884739,
3.2559437743963));
#96338=CARTESIAN_POINT('Ctrl Pts',(-1.55449947323643,0.00133480041304701,
2.69405622560371));
#96339=CARTESIAN_POINT('Ctrl Pts',(-1.55153406972295,-0.361714100102126,
2.72002390145891));
#96340=CARTESIAN_POINT('Ctrl Pts',(-1.2437032104418,-1.24745277135715,2.78305371725784));
#96341=CARTESIAN_POINT('Ctrl Pts',(0.231926238140432,-1.82410602009977,
2.88314567300049));
#96342=CARTESIAN_POINT('Ctrl Pts',(1.65866396469461,-0.793716828903688,
2.99433209283165));
#96343=CARTESIAN_POINT('Ctrl Pts',(1.56599354026699,0.96375141196464,3.10551851266282));
#96344=CARTESIAN_POINT('Ctrl Pts',(0.0388050940998321,1.83838154825996,
3.21670493249398));
#96345=CARTESIAN_POINT('Ctrl Pts',(-1.31300314367493,1.13822266482633,3.31288417014094));
#96346=CARTESIAN_POINT('Ctrl Pts',(-1.55193567478298,0.308165737536199,
3.37200126784418));
#96347=CARTESIAN_POINT('Ctrl Pts',(-1.5533186684889,-0.000770198572060919,
3.39405622560371));
#96348=CARTESIAN_POINT('Origin',(0.,0.,-1.29405622560369));
#96349=CARTESIAN_POINT('',(-1.55454118234884,-0.00133834695600709,1.8559437743963));
#96350=CARTESIAN_POINT('',(-1.55805467550008,3.4854191793785E-5,1.9940562256037));
#96351=CARTESIAN_POINT('',(-1.5555,-2.01987159101623E-13,-1.29405622560369));
#96352=CARTESIAN_POINT('Ctrl Pts',(-1.55454118234884,-0.00133834695600729,
1.8559437743963));
#96353=CARTESIAN_POINT('Ctrl Pts',(-1.55580288786201,-0.154903851691022,
1.86692853568168));
#96354=CARTESIAN_POINT('Ctrl Pts',(-1.46436232298065,-0.824775316270878,
1.91495051379553));
#96355=CARTESIAN_POINT('Ctrl Pts',(-0.503915664640746,-1.76796168665343,
2.00000970873786));
#96356=CARTESIAN_POINT('Ctrl Pts',(1.21174280763407,-1.38249741391359,2.1111213592233));
#96357=CARTESIAN_POINT('Ctrl Pts',(1.81875888824183,0.267835396201195,2.22223300970874));
#96358=CARTESIAN_POINT('Ctrl Pts',(0.761764071097843,1.67312138149853,2.33334466019417));
#96359=CARTESIAN_POINT('Ctrl Pts',(-0.992180579104728,1.54764252547341,
2.44445631067961));
#96360=CARTESIAN_POINT('Ctrl Pts',(-1.55725669913861,0.518277207581445,
2.51865601541365));
#96361=CARTESIAN_POINT('Ctrl Pts',(-1.55804766277071,0.0017735852989955,
2.55581850331921));
#96362=CARTESIAN_POINT('Ctrl Pts',(-1.55804712705668,3.25009013604029E-5,
2.5559437743963));
#96363=CARTESIAN_POINT('Ctrl Pts',(-1.55805467550008,3.48541917938314E-5,
1.9940562256037));
#96364=CARTESIAN_POINT('Ctrl Pts',(-1.55788564535512,-0.513206116891616,
2.03098439512992));
#96365=CARTESIAN_POINT('Ctrl Pts',(-1.00003893378143,-1.54186484140614,
2.10497470459985));
#96366=CARTESIAN_POINT('Ctrl Pts',(0.752488571272716,-1.67777039880966,
2.21602715401351));
#96367=CARTESIAN_POINT('Ctrl Pts',(1.81781810074028,-0.276929424335053,
2.32721357384467));
#96368=CARTESIAN_POINT('Ctrl Pts',(1.21794738393109,1.37759091140133,2.43839999367584));
#96369=CARTESIAN_POINT('Ctrl Pts',(-0.497615974795104,1.77017821004958,
2.549586413507));
#96370=CARTESIAN_POINT('Ctrl Pts',(-1.46313162187878,0.828233020270418,
2.63480515748296));
#96371=CARTESIAN_POINT('Ctrl Pts',(-1.55576641614544,0.156444291597347,
2.68296176151519));
#96372=CARTESIAN_POINT('Ctrl Pts',(-1.55449947323643,0.00133480041304701,
2.69405622560371));
#96373=CARTESIAN_POINT('Origin',(0.,0.,-1.29405622560369));
#96374=CARTESIAN_POINT('',(-1.55333634177863,0.000779921548230329,1.1559437743963));
#96375=CARTESIAN_POINT('',(-1.55460191805193,-0.00135568056800359,1.2940562256037));
#96376=CARTESIAN_POINT('',(-1.5555,-2.01987159101623E-13,-1.29405622560369));
#96377=CARTESIAN_POINT('Ctrl Pts',(-1.55333634177863,0.000779921548230561,
1.1559437743963));
#96378=CARTESIAN_POINT('Ctrl Pts',(-1.55193438638927,-0.308706275100063,
1.17803856804414));
#96379=CARTESIAN_POINT('Ctrl Pts',(-1.31241956589738,-1.1389814578602,1.23717057852045));
#96380=CARTESIAN_POINT('Ctrl Pts',(0.0395347168138628,-1.83794704008407,
1.33333980582524));
#96381=CARTESIAN_POINT('Ctrl Pts',(1.56537855283131,-0.963955976349113,
1.44445145631068));
#96382=CARTESIAN_POINT('Ctrl Pts',(1.65903376979378,0.791977165381959,1.55556310679611));
#96383=CARTESIAN_POINT('Ctrl Pts',(0.234812759114929,1.82331608910266,1.66667475728155));
#96384=CARTESIAN_POINT('Ctrl Pts',(-1.24220109658982,1.24943524423025,1.76680164648161));
#96385=CARTESIAN_POINT('Ctrl Pts',(-1.55154880719052,0.362871523529771,
1.8298913188532));
#96386=CARTESIAN_POINT('Ctrl Pts',(-1.55454118234884,-0.00133834695600729,
1.8559437743963));
#96387=CARTESIAN_POINT('Ctrl Pts',(-1.55460191805193,-0.00135568056800364,
1.2940562256037));
#96388=CARTESIAN_POINT('Ctrl Pts',(-1.5558637635503,-0.152693971168416,
1.30488274885721));
#96389=CARTESIAN_POINT('Ctrl Pts',(-1.46605510259419,-0.820638709603335,
1.35277141205443));
#96390=CARTESIAN_POINT('Ctrl Pts',(-0.510374815939226,-1.76654153931159,
1.43772221519537));
#96391=CARTESIAN_POINT('Ctrl Pts',(1.20797626960931,-1.38634273102519,1.54890863502654));
#96392=CARTESIAN_POINT('Ctrl Pts',(1.81976886629041,0.263806680570579,1.6600950548577));
#96393=CARTESIAN_POINT('Ctrl Pts',(0.764574137846417,1.67229745635935,1.77128147468886));
#96394=CARTESIAN_POINT('Ctrl Pts',(-0.991003621173195,1.54889135395602,
1.88246789452002));
#96395=CARTESIAN_POINT('Ctrl Pts',(-1.5572087700955,0.518861158146894,1.95672614482497));
#96396=CARTESIAN_POINT('Ctrl Pts',(-1.55805528871865,0.00189682319971778,
1.9939222551862));
#96397=CARTESIAN_POINT('Ctrl Pts',(-1.55805467550008,3.48541917938314E-5,
1.9940562256037));
#96398=CARTESIAN_POINT('Origin',(0.,0.,-1.29405622560369));
#96399=CARTESIAN_POINT('',(-1.55735926886437,0.00101346774827271,0.455943774396301));
#96400=CARTESIAN_POINT('',(-1.55326046963413,0.000729270061605516,0.594056225603705));
#96401=CARTESIAN_POINT('',(-1.5555,-2.01987159101623E-13,-1.29405622560369));
#96402=CARTESIAN_POINT('Ctrl Pts',(-1.55735926886437,0.00101346774827265,
0.455943774396301));
#96403=CARTESIAN_POINT('Ctrl Pts',(-1.5541538777776,-0.460983628495037,
0.489148600406595));
#96404=CARTESIAN_POINT('Ctrl Pts',(-1.09151218308356,-1.44423481489054,
0.559390643245367));
#96405=CARTESIAN_POINT('Ctrl Pts',(0.579488995883613,-1.74456230311225,
0.666669902912619));
#96406=CARTESIAN_POINT('Ctrl Pts',(1.77994191588978,-0.459827600750814,
0.777781553398056));
#96407=CARTESIAN_POINT('Ctrl Pts',(1.35192905881154,1.24578720765632,0.888893203883492));
#96408=CARTESIAN_POINT('Ctrl Pts',(-0.313001003158473,1.81151906168851,
1.00000485436893));
#96409=CARTESIAN_POINT('Ctrl Pts',(-1.41742497137191,0.93698092273704,1.08902171120653));
#96410=CARTESIAN_POINT('Ctrl Pts',(-1.55428446607623,0.210081433596544,
1.14100135121566));
#96411=CARTESIAN_POINT('Ctrl Pts',(-1.55333634177863,0.000779921548230561,
1.1559437743963));
#96412=CARTESIAN_POINT('Ctrl Pts',(-1.55326046963413,0.000729270061605551,
0.594056225603705));
#96413=CARTESIAN_POINT('Ctrl Pts',(-1.55199262831984,-0.304485333833814,
0.615843242528215));
#96414=CARTESIAN_POINT('Ctrl Pts',(-1.31743653601245,-1.13071739766558,
0.674692399396446));
#96415=CARTESIAN_POINT('Ctrl Pts',(0.0255447675030308,-1.83860034663711,
0.770603696208398));
#96416=CARTESIAN_POINT('Ctrl Pts',(1.55899683301632,-0.975032021788082,
0.881790116039561));
#96417=CARTESIAN_POINT('Ctrl Pts',(1.66434877052597,0.781732535368643,0.992976535870723));
#96418=CARTESIAN_POINT('Ctrl Pts',(0.245080507541896,1.82238325373942,1.10416295570189));
#96419=CARTESIAN_POINT('Ctrl Pts',(-1.23863138927055,1.25487925833816,1.20452285227955));
#96420=CARTESIAN_POINT('Ctrl Pts',(-1.55154412248428,0.365378245899198,
1.26782060891349));
#96421=CARTESIAN_POINT('Ctrl Pts',(-1.55460191805193,-0.00135568056800364,
1.2940562256037));
#96422=CARTESIAN_POINT('Origin',(0.,0.,11.5));
#96423=CARTESIAN_POINT('',(-1.77892626630995,-0.0012009523392913,11.2223275485995));
#96424=CARTESIAN_POINT('Ctrl Pts',(1.55548765964692,0.00619602180104861,
11.4445));
#96425=CARTESIAN_POINT('Ctrl Pts',(1.55843889773201,-0.053546881811892,
11.4417867591843));
#96426=CARTESIAN_POINT('Ctrl Pts',(1.55766805736304,-0.113278156040886,
11.439086160746));
#96427=CARTESIAN_POINT('Ctrl Pts',(1.55338999746751,-0.172741258360748,
11.4363936568093));
#96428=CARTESIAN_POINT('Ctrl Pts',(1.54917978268939,-0.231261344159722,
11.4337438528932));
#96429=CARTESIAN_POINT('Ctrl Pts',(1.54157226362346,-0.289522447371128,
11.4311018887755));
#96430=CARTESIAN_POINT('Ctrl Pts',(1.5307259163647,-0.347284232316321,11.4284634295395));
#96431=CARTESIAN_POINT('Ctrl Pts',(1.52490021612,-0.37830876404678,11.427046282158));
#96432=CARTESIAN_POINT('Ctrl Pts',(1.51813939227042,-0.409189253639797,
11.4256301458963));
#96433=CARTESIAN_POINT('Ctrl Pts',(1.51046300038634,-0.439887833717896,
11.4242143490555));
#96434=CARTESIAN_POINT('Ctrl Pts',(1.50749771858011,-0.451746261786366,
11.4236674467248));
#96435=CARTESIAN_POINT('Ctrl Pts',(1.50439653465153,-0.463574222421597,
11.4231207471528));
#96436=CARTESIAN_POINT('Ctrl Pts',(1.50116353235453,-0.47535996619676,11.4225746575513));
#96437=CARTESIAN_POINT('Ctrl Pts',(1.48455611813741,-0.535901441503565,
11.4197694828629));
#96438=CARTESIAN_POINT('Ctrl Pts',(1.46445634965142,-0.595403551134085,
11.4169769764437));
#96439=CARTESIAN_POINT('Ctrl Pts',(1.4410621824655,-0.653580209875647,11.414192092755));
#96440=CARTESIAN_POINT('Ctrl Pts',(1.41747802435967,-0.712229338392404,
11.4113845922059));
#96441=CARTESIAN_POINT('Ctrl Pts',(1.39054537943373,-0.769532412755046,
11.4085848387028));
#96442=CARTESIAN_POINT('Ctrl Pts',(1.36041578548535,-0.825184282227088,
11.4057876627772));
#96443=CARTESIAN_POINT('Ctrl Pts',(1.35261592294621,-0.839591277975912,
11.4050635379265));
#96444=CARTESIAN_POINT('Ctrl Pts',(1.34460155997405,-0.853887506909652,
11.4043395858183));
#96445=CARTESIAN_POINT('Ctrl Pts',(1.33637481784576,-0.868067413704247,
11.4036157167661));
#96446=CARTESIAN_POINT('Ctrl Pts',(1.33123141939554,-0.87693275912219,11.4031631503791));
#96447=CARTESIAN_POINT('Ctrl Pts',(1.32600576325494,-0.885751206456736,
11.4027106878625));
#96448=CARTESIAN_POINT('Ctrl Pts',(1.32070341258855,-0.894513477947337,
11.4022587210796));
#96449=CARTESIAN_POINT('Ctrl Pts',(1.28755838481391,-0.949286492822766,
11.3994334738427));
#96450=CARTESIAN_POINT('Ctrl Pts',(1.25136992677528,-1.00195372283142,11.3966231054397));
#96451=CARTESIAN_POINT('Ctrl Pts',(1.21232687524415,-1.05222079285711,11.3938225048748));
#96452=CARTESIAN_POINT('Ctrl Pts',(1.17352218779371,-1.10218097437215,11.3910390024248));
#96453=CARTESIAN_POINT('Ctrl Pts',(1.13189715922074,-1.14977118940024,11.3882651489085));
#96454=CARTESIAN_POINT('Ctrl Pts',(1.08759128036108,-1.19468014867466,11.3854959263702));
#96455=CARTESIAN_POINT('Ctrl Pts',(1.05692354853581,-1.22576532190738,11.3835791203762));
#96456=CARTESIAN_POINT('Ctrl Pts',(1.0249704261144,-1.25556541150052,11.3816645331574));
#96457=CARTESIAN_POINT('Ctrl Pts',(0.991767007145199,-1.28396712328559,
11.379750500582));
#96458=CARTESIAN_POINT('Ctrl Pts',(0.971829282858114,-1.30102155672743,
11.378601177562));
#96459=CARTESIAN_POINT('Ctrl Pts',(0.951440575196337,-1.31757160665078,
11.3774520545279));
#96460=CARTESIAN_POINT('Ctrl Pts',(0.930607078503626,-1.33359088746794,
11.3763027711782));
#96461=CARTESIAN_POINT('Ctrl Pts',(0.921822018225176,-1.34034589118487,
11.3758181418501));
#96462=CARTESIAN_POINT('Ctrl Pts',(0.912957575551233,-1.34700657088378,
11.3753334724466));
#96463=CARTESIAN_POINT('Ctrl Pts',(0.904026617991894,-1.35356212132308,
11.3748494000991));
#96464=CARTESIAN_POINT('Ctrl Pts',(0.898865665597572,-1.35735039189889,
11.3745696681303));
#96465=CARTESIAN_POINT('Ctrl Pts',(0.893681522170691,-1.36110432047063,
11.3742900812105));
#96466=CARTESIAN_POINT('Ctrl Pts',(0.888474357058895,-1.36482361432558,
11.3740106343829));
#96467=CARTESIAN_POINT('Ctrl Pts',(0.838811308516624,-1.4002961732508,11.3713454257582));
#96468=CARTESIAN_POINT('Ctrl Pts',(0.787057395286918,-1.43262124116857,
11.368692960317));
#96469=CARTESIAN_POINT('Ctrl Pts',(0.733560484100527,-1.46184200007972,
11.3660489378073));
#96470=CARTESIAN_POINT('Ctrl Pts',(0.677705393253366,-1.49235082960671,
11.3632883650152));
#96471=CARTESIAN_POINT('Ctrl Pts',(0.619949541746925,-1.51947609806138,
11.3605369959002));
#96472=CARTESIAN_POINT('Ctrl Pts',(0.560651932851881,-1.54322365588157,
11.3577899361005));
#96473=CARTESIAN_POINT('Ctrl Pts',(0.511114145446654,-1.56306259192994,
11.3554950161722));
#96474=CARTESIAN_POINT('Ctrl Pts',(0.460499386969577,-1.58054347420583,
11.3532031037542));
#96475=CARTESIAN_POINT('Ctrl Pts',(0.409004561176526,-1.5956447160272,11.3509113452381));
#96476=CARTESIAN_POINT('Ctrl Pts',(0.394571471762801,-1.59987732717035,
11.3502690058367));
#96477=CARTESIAN_POINT('Ctrl Pts',(0.38006920116156,-1.60392285642947,11.3496266785255));
#96478=CARTESIAN_POINT('Ctrl Pts',(0.365502000908426,-1.60778049339754,
11.3489843004725));
#96479=CARTESIAN_POINT('Ctrl Pts',(0.352945849497182,-1.61110557117631,
11.3484306047756));
#96480=CARTESIAN_POINT('Ctrl Pts',(0.340339686983491,-1.61429135213649,
11.3478767954507));
#96481=CARTESIAN_POINT('Ctrl Pts',(0.327707338901135,-1.61733252206154,
11.3473237518226));
#96482=CARTESIAN_POINT('Ctrl Pts',(0.26442068399392,-1.63256844418037,11.3445530649309));
#96483=CARTESIAN_POINT('Ctrl Pts',(0.200363163100888,-1.64421053384351,
11.3417964693365));
#96484=CARTESIAN_POINT('Ctrl Pts',(0.135902532141567,-1.65227549235515,
11.3390491503551));
#96485=CARTESIAN_POINT('Ctrl Pts',(0.0706504004584388,-1.66043947907059,
11.3362680975283));
#96486=CARTESIAN_POINT('Ctrl Pts',(0.00498413291330568,-1.6649382180869,
11.333496550525));
#96487=CARTESIAN_POINT('Ctrl Pts',(-0.0607337043444866,-1.66573959706564,
11.3307295151184));
#96488=CARTESIAN_POINT('Ctrl Pts',(-0.114943810254912,-1.66640064802417,
11.3284470102656));
#96489=CARTESIAN_POINT('Ctrl Pts',(-0.169189647051337,-1.66454499730668,
11.326167575313));
#96490=CARTESIAN_POINT('Ctrl Pts',(-0.223269283792523,-1.66012780789457,
11.3238884070273));
#96491=CARTESIAN_POINT('Ctrl Pts',(-0.242921115785065,-1.65852265909112,
11.3230601871106));
#96492=CARTESIAN_POINT('Ctrl Pts',(-0.262550978640708,-1.65657902103982,
11.3222320024074));
#96493=CARTESIAN_POINT('Ctrl Pts',(-0.282149042864747,-1.65429391513469,
11.3214037184036));
#96494=CARTESIAN_POINT('Ctrl Pts',(-0.293822649715497,-1.65293278948249,
11.3209103501959));
#96495=CARTESIAN_POINT('Ctrl Pts',(-0.305486007024825,-1.65145026241138,
11.3204169024293));
#96496=CARTESIAN_POINT('Ctrl Pts',(-0.317120120921591,-1.64984824722041,
11.3199240638241));
#96497=CARTESIAN_POINT('Ctrl Pts',(-0.382649500838262,-1.64082486451904,
11.3171481404934));
#96498=CARTESIAN_POINT('Ctrl Pts',(-0.447374851901241,-1.62800143931766,
11.3143862955204));
#96499=CARTESIAN_POINT('Ctrl Pts',(-0.510936115769287,-1.6113566500933,
11.3116336908415));
#96500=CARTESIAN_POINT('Ctrl Pts',(-0.573549739883189,-1.59496001930709,
11.3089221249567));
#96501=CARTESIAN_POINT('Ctrl Pts',(-0.635034780101342,-1.57485515271455,
11.3062195258916));
#96502=CARTESIAN_POINT('Ctrl Pts',(-0.695044280650932,-1.55097228857054,
11.3035212687658));
#96503=CARTESIAN_POINT('Ctrl Pts',(-0.755213263935446,-1.52702595273528,
11.3008158406849));
#96504=CARTESIAN_POINT('Ctrl Pts',(-0.813899721511821,-1.49928127162975,
11.2981147776525));
#96505=CARTESIAN_POINT('Ctrl Pts',(-0.870916818143125,-1.46801413582731,
11.2954134178164));
#96506=CARTESIAN_POINT('Ctrl Pts',(-0.88517189274549,-1.46019691292752,
11.2947380399339));
#96507=CARTESIAN_POINT('Ctrl Pts',(-0.8993225020166,-1.4521592870016,11.294062643499));
#96508=CARTESIAN_POINT('Ctrl Pts',(-0.913365468395192,-1.44390514150358,
11.2933871556582));
#96509=CARTESIAN_POINT('Ctrl Pts',(-0.922789553247202,-1.43836587255875,
11.2929338429778));
#96510=CARTESIAN_POINT('Ctrl Pts',(-0.932156968408698,-1.43273389293101,
11.2924808828034));
#96511=CARTESIAN_POINT('Ctrl Pts',(-0.941465939330546,-1.42701150822941,
11.2920283046203));
#96512=CARTESIAN_POINT('Ctrl Pts',(-0.997258564244995,-1.39271482109252,
11.2893158109378));
#96513=CARTESIAN_POINT('Ctrl Pts',(-1.05096555773083,-1.35516769400791,
11.2866164406656));
#96514=CARTESIAN_POINT('Ctrl Pts',(-1.10242222381511,-1.31470157532149,
11.2839256753843));
#96515=CARTESIAN_POINT('Ctrl Pts',(-1.15490559840975,-1.27342804116106,
11.2811812215953));
#96516=CARTESIAN_POINT('Ctrl Pts',(-1.20504870548191,-1.22911724367845,
11.2784457196118));
#96517=CARTESIAN_POINT('Ctrl Pts',(-1.25265335579406,-1.18207076364008,
11.2757143751156));
#96518=CARTESIAN_POINT('Ctrl Pts',(-1.28397500867159,-1.15111636092502,
11.2739172770666));
#96519=CARTESIAN_POINT('Ctrl Pts',(-1.31419725536704,-1.11897666094205,
11.2721219788063));
#96520=CARTESIAN_POINT('Ctrl Pts',(-1.34325581778868,-1.08572815742637,
11.2703271147686));
#96521=CARTESIAN_POINT('Ctrl Pts',(-1.36209363901681,-1.06417411919684,
11.2691635565932));
#96522=CARTESIAN_POINT('Ctrl Pts',(-1.38044228251278,-1.04215395727969,
11.2680001809021));
#96523=CARTESIAN_POINT('Ctrl Pts',(-1.39828252264694,-1.01968718394611,
11.2668366156616));
#96524=CARTESIAN_POINT('Ctrl Pts',(-1.40805056143521,-1.00738598666853,
11.2661995306046));
#96525=CARTESIAN_POINT('Ctrl Pts',(-1.41766921695113,-0.994946604236495,
11.2655621759649));
#96526=CARTESIAN_POINT('Ctrl Pts',(-1.42711662985222,-0.982397385607975,
11.264925758661));
#96527=CARTESIAN_POINT('Ctrl Pts',(-1.46820629310292,-0.927817028752221,
11.262157786839));
#96528=CARTESIAN_POINT('Ctrl Pts',(-1.50612185513061,-0.871087521735772,
11.2594035844773));
#96529=CARTESIAN_POINT('Ctrl Pts',(-1.54066769776793,-0.812525394359864,
11.2566583590267));
#96530=CARTESIAN_POINT('Ctrl Pts',(-1.57505516312501,-0.754231748217875,
11.2539257192103));
#96531=CARTESIAN_POINT('Ctrl Pts',(-1.60610442219133,-0.694121381542228,
11.2512019741836));
#96532=CARTESIAN_POINT('Ctrl Pts',(-1.63358497140864,-0.632471603998023,
11.2484823970106));
#96533=CARTESIAN_POINT('Ctrl Pts',(-1.65966108961598,-0.573972522557314,
11.2459018075444));
#96534=CARTESIAN_POINT('Ctrl Pts',(-1.68252420078453,-0.514086499095208,
11.2433249708101));
#96535=CARTESIAN_POINT('Ctrl Pts',(-1.70193725006908,-0.453031690747441,
11.2407478481942));
#96536=CARTESIAN_POINT('Ctrl Pts',(-1.70639988231082,-0.438996535720931,
11.2401554244947));
#96537=CARTESIAN_POINT('Ctrl Pts',(-1.71068001578898,-0.424899564800969,
11.239562985688));
#96538=CARTESIAN_POINT('Ctrl Pts',(-1.71477442803653,-0.410743347710776,
11.2389704827146));
#96539=CARTESIAN_POINT('Ctrl Pts',(-1.7181060933816,-0.399224288308597,
11.238488356953));
#96540=CARTESIAN_POINT('Ctrl Pts',(-1.72131496051192,-0.387664952239154,
11.2380061462914));
#96541=CARTESIAN_POINT('Ctrl Pts',(-1.72439513423882,-0.376083269559728,
11.2375245092466));
#96542=CARTESIAN_POINT('Ctrl Pts',(-1.73399637264737,-0.339981897872015,
11.2360231938976));
#96543=CARTESIAN_POINT('Ctrl Pts',(-1.74235845090443,-0.303626928305512,
11.234525913273));
#96544=CARTESIAN_POINT('Ctrl Pts',(-1.74944665354966,-0.267065873422436,
11.2330319031487));
#96545=CARTESIAN_POINT('Ctrl Pts',(-1.76197449586933,-0.202447076028902,
11.2303913574139));
#96546=CARTESIAN_POINT('Ctrl Pts',(-1.77052625497235,-0.137185361680741,
11.227761027999));
#96547=CARTESIAN_POINT('Ctrl Pts',(-1.77528061829343,-0.0715870718432795,
11.2251366955952));
#96548=CARTESIAN_POINT('Ctrl Pts',(-1.77697828156189,-0.0481635764959884,
11.2241996126621));
#96549=CARTESIAN_POINT('Ctrl Pts',(-1.7781912975682,-0.0246970169190114,
11.2232632943623));
#96550=CARTESIAN_POINT('Ctrl Pts',(-1.77892626630995,-0.00120095233929127,
11.2223275485995));
#96551=CARTESIAN_POINT('',(1.88128289424299,-0.51655738433239,11.046));
#96552=CARTESIAN_POINT('Ctrl Pts',(1.88079991776263,-0.516378774142054,
11.046));
#96553=CARTESIAN_POINT('Ctrl Pts',(1.89035995045861,-0.445151004206684,
11.0555631104642));
#96554=CARTESIAN_POINT('Ctrl Pts',(1.8961423315859,-0.373654493774377,11.0651669654983));
#96555=CARTESIAN_POINT('Ctrl Pts',(1.89809144951916,-0.302224012343752,
11.0748303404806));
#96556=CARTESIAN_POINT('Ctrl Pts',(1.89999077178002,-0.23261842246626,11.0842468375051));
#96557=CARTESIAN_POINT('Ctrl Pts',(1.89824990827702,-0.163074621232238,
11.0937198521185));
#96558=CARTESIAN_POINT('Ctrl Pts',(1.89277099599951,-0.0939167257851171,
11.1032667571406));
#96559=CARTESIAN_POINT('Ctrl Pts',(1.88910201129244,-0.0476047485319078,
11.1096598962807));
#96560=CARTESIAN_POINT('Ctrl Pts',(1.8837557967888,-0.00146614169388357,
11.1160861707414));
#96561=CARTESIAN_POINT('Ctrl Pts',(1.87669176161129,0.0443950771863014,
11.1225507975725));
#96562=CARTESIAN_POINT('Ctrl Pts',(1.87063241478827,0.0837336455737761,
11.1280959874063));
#96563=CARTESIAN_POINT('Ctrl Pts',(1.8633089856103,0.122868068816038,11.1336693960131));
#96564=CARTESIAN_POINT('Ctrl Pts',(1.85469071090361,0.161728394728602,11.1392743160301));
#96565=CARTESIAN_POINT('Ctrl Pts',(1.85223436103037,0.172804226014781,11.1408718103131));
#96566=CARTESIAN_POINT('Ctrl Pts',(1.84967323324123,0.183855475695868,11.142471538338));
#96567=CARTESIAN_POINT('Ctrl Pts',(1.84700939076218,0.19487013146115,11.1440720571876));
#96568=CARTESIAN_POINT('Ctrl Pts',(1.83137216521354,0.259528105007685,11.1534673853433));
#96569=CARTESIAN_POINT('Ctrl Pts',(1.81217652429567,0.323030635926077,11.1629048835303));
#96570=CARTESIAN_POINT('Ctrl Pts',(1.78934255453511,0.385087390709459,11.1724028038701));
#96571=CARTESIAN_POINT('Ctrl Pts',(1.78198218565347,0.405090947322401,11.1754643914102));
#96572=CARTESIAN_POINT('Ctrl Pts',(1.77424343060636,0.424944079046285,11.1785322571122));
#96573=CARTESIAN_POINT('Ctrl Pts',(1.76612263817241,0.444636415640588,11.181607012295));
#96574=CARTESIAN_POINT('Ctrl Pts',(1.73919119835162,0.509943216945239,11.1918039955137));
#96575=CARTESIAN_POINT('Ctrl Pts',(1.70806080167302,0.573485248201441,11.2020767507448));
#96576=CARTESIAN_POINT('Ctrl Pts',(1.67301702698032,0.634984575310704,11.2124475752393));
#96577=CARTESIAN_POINT('Ctrl Pts',(1.64235372412421,0.688796486531309,11.2215220466721));
#96578=CARTESIAN_POINT('Ctrl Pts',(1.60869302252863,0.741044106677185,11.2306716023846));
#96579=CARTESIAN_POINT('Ctrl Pts',(1.57220891785208,0.791506873950779,11.239911179793));
#96580=CARTESIAN_POINT('Ctrl Pts',(1.56528521292053,0.801083354276364,11.2416646038728));
#96581=CARTESIAN_POINT('Ctrl Pts',(1.55825911602623,0.81059620160376,11.2434214216921));
#96582=CARTESIAN_POINT('Ctrl Pts',(1.55114206425445,0.820030590825838,11.2451792455347));
#96583=CARTESIAN_POINT('Ctrl Pts',(1.51163333781795,0.872403499555923,11.254937412757));
#96584=CARTESIAN_POINT('Ctrl Pts',(1.46925448012712,0.922460374176763,11.2647444648472));
#96585=CARTESIAN_POINT('Ctrl Pts',(1.42425895086728,0.969999034377404,11.2746213834588));
#96586=CARTESIAN_POINT('Ctrl Pts',(1.37955552976012,1.01722907657888,11.2844341817346));
#96587=CARTESIAN_POINT('Ctrl Pts',(1.33226826113497,1.06197396880102,11.2943159423384));
#96588=CARTESIAN_POINT('Ctrl Pts',(1.28262305484525,1.10398985376236,11.3042872409362));
#96589=CARTESIAN_POINT('Ctrl Pts',(1.23402945162958,1.14511574274852,11.3140473238087));
#96590=CARTESIAN_POINT('Ctrl Pts',(1.18317581682196,1.18362727550242,11.3238931915966));
#96591=CARTESIAN_POINT('Ctrl Pts',(1.13026675802768,1.2192467284131,11.3338441399431));
#96592=CARTESIAN_POINT('Ctrl Pts',(1.11612186853279,1.22876935528969,11.3365044606506));
#96593=CARTESIAN_POINT('Ctrl Pts',(1.1018300740637,1.23808499004259,11.3391722917297));
#96594=CARTESIAN_POINT('Ctrl Pts',(1.0873953214649,1.24718768011963,11.3418480018757));
#96595=CARTESIAN_POINT('Ctrl Pts',(1.07843141524914,1.25284040326838,11.3435096039465));
#96596=CARTESIAN_POINT('Ctrl Pts',(1.06941317684967,1.25841040829158,11.3451740914355));
#96597=CARTESIAN_POINT('Ctrl Pts',(1.06035226952456,1.2638900735973,11.346839603865));
#96598=CARTESIAN_POINT('Ctrl Pts',(1.00742079701965,1.29590085828569,11.3565690958694));
#96599=CARTESIAN_POINT('Ctrl Pts',(0.952938092487177,1.32489391547385,11.3663514013733));
#96600=CARTESIAN_POINT('Ctrl Pts',(0.897108858642945,1.35066478023243,11.3762079140514));
#96601=CARTESIAN_POINT('Ctrl Pts',(0.842238965806958,1.37599281162795,11.3858950574554));
#96602=CARTESIAN_POINT('Ctrl Pts',(0.78606756226141,1.39820862213323,11.3956538796688));
#96603=CARTESIAN_POINT('Ctrl Pts',(0.72878604220227,1.41706842320411,11.4055046903548));
#96604=CARTESIAN_POINT('Ctrl Pts',(0.67317444208947,1.43537840719681,11.4150683217683));
#96605=CARTESIAN_POINT('Ctrl Pts',(0.616515828164059,1.45052520284418,11.4247186563809));
#96606=CARTESIAN_POINT('Ctrl Pts',(0.558993687390787,1.46223733220615,11.4344742788813));
#96607=CARTESIAN_POINT('Ctrl Pts',(0.539362537898783,1.46623444634835,11.4378036765901));
#96608=CARTESIAN_POINT('Ctrl Pts',(0.519630929867265,1.46983109384517,11.4411453373854));
#96609=CARTESIAN_POINT('Ctrl Pts',(0.499806597877626,1.47301514408983,11.4445));
#96610=CARTESIAN_POINT('',(1.56060797133591,1.17265290216009,11.046));
#96611=CARTESIAN_POINT('Origin',(0.,0.,11.046));
#96612=CARTESIAN_POINT('Ctrl Pts',(-1.77892626630995,-0.00120095233929127,
11.2223275485995));
#96613=CARTESIAN_POINT('Ctrl Pts',(-1.78091222637221,0.0622877965358305,
11.2197990686688));
#96614=CARTESIAN_POINT('Ctrl Pts',(-1.77941067542291,0.125992016111799,
11.2172747683064));
#96615=CARTESIAN_POINT('Ctrl Pts',(-1.77452381634337,0.189646102027163,
11.2147508586347));
#96616=CARTESIAN_POINT('Ctrl Pts',(-1.77287868795546,0.211074823838332,
11.2139012013432));
#96617=CARTESIAN_POINT('Ctrl Pts',(-1.7708495726434,0.232497857027148,11.2130515883281));
#96618=CARTESIAN_POINT('Ctrl Pts',(-1.76843936997923,0.253904972833394,
11.2122018750387));
#96619=CARTESIAN_POINT('Ctrl Pts',(-1.76712267121633,0.265599725029338,
11.2117376748892));
#96620=CARTESIAN_POINT('Ctrl Pts',(-1.76569197102713,0.277291668505868,
11.2112733675823));
#96621=CARTESIAN_POINT('Ctrl Pts',(-1.7641484990815,0.288972974548762,11.2108091738099));
#96622=CARTESIAN_POINT('Ctrl Pts',(-1.75515036560026,0.357072658062498,
11.2081030167356));
#96623=CARTESIAN_POINT('Ctrl Pts',(-1.74235696629666,0.42456963250346,11.2054102736121));
#96624=CARTESIAN_POINT('Ctrl Pts',(-1.72594903242932,0.491138664005795,
11.2027264834948));
#96625=CARTESIAN_POINT('Ctrl Pts',(-1.70928395222888,0.558750970212142,
11.2000006328234));
#96626=CARTESIAN_POINT('Ctrl Pts',(-1.68888999030711,0.625407040269523,
11.1972840179815));
#96627=CARTESIAN_POINT('Ctrl Pts',(-1.66490278446929,0.690766734877331,
11.1945719649831));
#96628=CARTESIAN_POINT('Ctrl Pts',(-1.64112198461878,0.755564019991226,
11.1918832487577));
#96629=CARTESIAN_POINT('Ctrl Pts',(-1.61380916520598,0.81908815011939,11.1891990162058));
#96630=CARTESIAN_POINT('Ctrl Pts',(-1.5830482712126,0.880993120829078,11.186514712963));
#96631=CARTESIAN_POINT('Ctrl Pts',(-1.57216641681974,0.902892382846704,
11.1855651242728));
#96632=CARTESIAN_POINT('Ctrl Pts',(-1.56085264019442,0.92458881232314,11.1846155267362));
#96633=CARTESIAN_POINT('Ctrl Pts',(-1.54910931637308,0.946066284278751,
11.1836657187303));
#96634=CARTESIAN_POINT('Ctrl Pts',(-1.54396572241992,0.955473450134084,
11.1832497013582));
#96635=CARTESIAN_POINT('Ctrl Pts',(-1.53874121405367,0.964835754579395,
11.1828337685169));
#96636=CARTESIAN_POINT('Ctrl Pts',(-1.5334404792476,0.974144495398925,11.18241823656));
#96637=CARTESIAN_POINT('Ctrl Pts',(-1.49854818334159,1.03541964895223,11.179682981066));
#96638=CARTESIAN_POINT('Ctrl Pts',(-1.46030493742689,1.09447092650475,11.1769608571821));
#96639=CARTESIAN_POINT('Ctrl Pts',(-1.41884997832206,1.15095727599886,11.1742472453603));
#96640=CARTESIAN_POINT('Ctrl Pts',(-1.37811238995456,1.20646613920276,11.1715805921112));
#96641=CARTESIAN_POINT('Ctrl Pts',(-1.33427285188376,1.25949901944966,11.1689221588738));
#96642=CARTESIAN_POINT('Ctrl Pts',(-1.28741864153,1.30971119589593,11.166267561795));
#96643=CARTESIAN_POINT('Ctrl Pts',(-1.26549062822221,1.33321075474058,11.1650251966024));
#96644=CARTESIAN_POINT('Ctrl Pts',(-1.24290170835111,1.35609210845284,11.1637836716393));
#96645=CARTESIAN_POINT('Ctrl Pts',(-1.21965775424868,1.37831740927343,11.1625425375316));
#96646=CARTESIAN_POINT('Ctrl Pts',(-1.19165584264812,1.40509215276722,11.1610473475387));
#96647=CARTESIAN_POINT('Ctrl Pts',(-1.16270333140537,1.43091488294274,11.1595527247918));
#96648=CARTESIAN_POINT('Ctrl Pts',(-1.13285929301872,1.45577404177113,11.1580578836196));
#96649=CARTESIAN_POINT('Ctrl Pts',(-1.12175109882477,1.46502682318719,11.1575014915585));
#96650=CARTESIAN_POINT('Ctrl Pts',(-1.11051936159011,1.47414607111053,11.156945069237));
#96651=CARTESIAN_POINT('Ctrl Pts',(-1.09916702235175,1.48313103947397,11.1563885761416));
#96652=CARTESIAN_POINT('Ctrl Pts',(-1.0900493418525,1.49034735578674,11.1559416262983));
#96653=CARTESIAN_POINT('Ctrl Pts',(-1.08085382696811,1.49747696130526,11.1554946319594));
#96654=CARTESIAN_POINT('Ctrl Pts',(-1.07159363370462,1.50451093778695,11.1550481251347));
#96655=CARTESIAN_POINT('Ctrl Pts',(-1.01611106549685,1.54665509923293,11.152372873695));
#96656=CARTESIAN_POINT('Ctrl Pts',(-0.958209601759993,1.58545013781557,
11.1497101571816));
#96657=CARTESIAN_POINT('Ctrl Pts',(-0.898278760372612,1.62088563165273,
11.1470556568828));
#96658=CARTESIAN_POINT('Ctrl Pts',(-0.837571419107242,1.65678024897295,
11.1443667632881));
#96659=CARTESIAN_POINT('Ctrl Pts',(-0.774780874239298,1.6892280755481,11.1416863001956));
#96660=CARTESIAN_POINT('Ctrl Pts',(-0.71027313016202,1.71817742298682,11.1390097788418));
#96661=CARTESIAN_POINT('Ctrl Pts',(-0.66261429365752,1.73956543207362,11.13703234349));
#96662=CARTESIAN_POINT('Ctrl Pts',(-0.614017264977652,1.75904301818697,
11.135057059686));
#96663=CARTESIAN_POINT('Ctrl Pts',(-0.56462073685077,1.77657345707156,11.1330821172509));
#96664=CARTESIAN_POINT('Ctrl Pts',(-0.539231747042784,1.78558380964183,
11.1320670298498));
#96665=CARTESIAN_POINT('Ctrl Pts',(-0.513631449727103,1.79407954038564,
11.1310520326313));
#96666=CARTESIAN_POINT('Ctrl Pts',(-0.487838223654543,1.802054170041,11.1300368798027));
#96667=CARTESIAN_POINT('Ctrl Pts',(-0.475799003301229,1.80577640018727,
11.1295630480858));
#96668=CARTESIAN_POINT('Ctrl Pts',(-0.463717747565173,1.80938508638487,
11.129089182467));
#96669=CARTESIAN_POINT('Ctrl Pts',(-0.451596312388482,1.81287949077367,
11.1286152579519));
#96670=CARTESIAN_POINT('Ctrl Pts',(-0.439480899976025,1.81637215890158,
11.1281415689151));
#96671=CARTESIAN_POINT('Ctrl Pts',(-0.427332434103985,1.81974856717366,
11.1276680985874));
#96672=CARTESIAN_POINT('Ctrl Pts',(-0.415160020480683,1.8230065701324,11.1271950974533));
#96673=CARTESIAN_POINT('Ctrl Pts',(-0.345659931193023,1.8416085913534,11.1244944316633));
#96674=CARTESIAN_POINT('Ctrl Pts',(-0.275309825422015,1.85637496302517,
11.1218062647546));
#96675=CARTESIAN_POINT('Ctrl Pts',(-0.204481476884407,1.86725830113956,
11.1191261497819));
#96676=CARTESIAN_POINT('Ctrl Pts',(-0.133579826115251,1.87815290272383,
11.1164432610836));
#96677=CARTESIAN_POINT('Ctrl Pts',(-0.0621979169225611,1.88515673586772,
11.1137684409964));
#96678=CARTESIAN_POINT('Ctrl Pts',(0.00930939936232982,1.88817434312463,
11.111097228754));
#96679=CARTESIAN_POINT('Ctrl Pts',(0.0795378313902503,1.89113798149254,
11.1084737902425));
#96680=CARTESIAN_POINT('Ctrl Pts',(0.149888204683991,1.89025686041538,11.1058538316796));
#96681=CARTESIAN_POINT('Ctrl Pts',(0.220026910137412,1.88539116319202,11.1032331273822));
#96682=CARTESIAN_POINT('Ctrl Pts',(0.236366392955163,1.88425765244837,11.1026226092302));
#96683=CARTESIAN_POINT('Ctrl Pts',(0.252694364144288,1.88290767750495,11.102012050607));
#96684=CARTESIAN_POINT('Ctrl Pts',(0.269006539233807,1.88133906123029,11.1014013980884));
#96685=CARTESIAN_POINT('Ctrl Pts',(0.280730896030037,1.88021162011471,11.1009624923038));
#96686=CARTESIAN_POINT('Ctrl Pts',(0.292446914187848,1.8789711508204,11.1005235443156));
#96687=CARTESIAN_POINT('Ctrl Pts',(0.304138944100939,1.87761870427971,11.1000850620809));
#96688=CARTESIAN_POINT('Ctrl Pts',(0.375822773838615,1.86932685519343,11.0973967277121));
#96689=CARTESIAN_POINT('Ctrl Pts',(0.446738242932316,1.85681796775178,11.0947208906731));
#96690=CARTESIAN_POINT('Ctrl Pts',(0.516529562716851,1.84000805096474,11.0920531719144));
#96691=CARTESIAN_POINT('Ctrl Pts',(0.584847521294231,1.82355300752536,11.0894417712386));
#96692=CARTESIAN_POINT('Ctrl Pts',(0.652089317501138,1.80297695165361,11.0868381496919));
#96693=CARTESIAN_POINT('Ctrl Pts',(0.718036401553849,1.77856692481578,11.084238199749));
#96694=CARTESIAN_POINT('Ctrl Pts',(0.785323202313169,1.75366100765569,11.0815854317561));
#96695=CARTESIAN_POINT('Ctrl Pts',(0.851262956271168,1.7247633139281,11.0789364860598));
#96696=CARTESIAN_POINT('Ctrl Pts',(0.915607648721953,1.6921267735849,11.0762869996812));
#96697=CARTESIAN_POINT('Ctrl Pts',(0.930631108062465,1.68450666199239,11.0756683868732));
#96698=CARTESIAN_POINT('Ctrl Pts',(0.945567515715628,1.67668252571399,11.0750497445899));
#96699=CARTESIAN_POINT('Ctrl Pts',(0.960413518624615,1.6686572293506,11.074431017298));
#96700=CARTESIAN_POINT('Ctrl Pts',(0.975205360081844,1.66066121101609,11.073814547258));
#96701=CARTESIAN_POINT('Ctrl Pts',(0.989912270604597,1.65246257743845,11.0731977870787));
#96702=CARTESIAN_POINT('Ctrl Pts',(1.00450295029956,1.6440805277344,11.0725818668126));
#96703=CARTESIAN_POINT('Ctrl Pts',(1.06739734574523,1.60794897253934,11.0699268888682));
#96704=CARTESIAN_POINT('Ctrl Pts',(1.12821828188749,1.56837054324493,11.0672840147147));
#96705=CARTESIAN_POINT('Ctrl Pts',(1.18673956352194,1.52565231730803,11.0646490274931));
#96706=CARTESIAN_POINT('Ctrl Pts',(1.24608357911593,1.48233352805146,11.0619769957398));
#96707=CARTESIAN_POINT('Ctrl Pts',(1.30306365724006,1.43578546725283,11.0593130742375));
#96708=CARTESIAN_POINT('Ctrl Pts',(1.35742307425591,1.38627866511896,11.056652865764));
#96709=CARTESIAN_POINT('Ctrl Pts',(1.41159294455999,1.3369444890372,11.0540019332135));
#96710=CARTESIAN_POINT('Ctrl Pts',(1.4631611896777,1.28467147000892,11.0513546878431));
#96711=CARTESIAN_POINT('Ctrl Pts',(1.51184108762766,1.22968809505141,11.0487067782687));
#96712=CARTESIAN_POINT('Ctrl Pts',(1.52842600119773,1.21095562929319,11.0478046532996));
#96713=CARTESIAN_POINT('Ctrl Pts',(1.54467532477781,1.19190827830405,11.0469024512351));
#96714=CARTESIAN_POINT('Ctrl Pts',(1.56057659382849,1.17255425406029,11.046));
#96715=CARTESIAN_POINT('',(-0.999999999999999,-1.22464679914735E-16,12.));
#96716=CARTESIAN_POINT('',(-1.5,-1.83697019872103E-16,11.5));
#96717=CARTESIAN_POINT('Origin',(0.,0.,12.));
#96718=CARTESIAN_POINT('Ctrl Pts',(1.13509973994371,-1.59049193030953,-0.230074082272069));
#96719=CARTESIAN_POINT('Ctrl Pts',(1.66385127640631,-1.21313337847033,-0.19303686544359));
#96720=CARTESIAN_POINT('Ctrl Pts',(2.30633516687349,0.103782615975306,-0.118962431786632));
#96721=CARTESIAN_POINT('Ctrl Pts',(1.16188988078006,1.99753850566951,-0.00785078130119459));
#96722=CARTESIAN_POINT('Ctrl Pts',(-1.04655428901899,2.05782953697956,0.103260869184242));
#96723=CARTESIAN_POINT('Ctrl Pts',(-2.29698075471667,0.238333788527267,
0.214372519669679));
#96724=CARTESIAN_POINT('Ctrl Pts',(-1.44613108848303,-1.80075271725216,
0.325484170155115));
#96725=CARTESIAN_POINT('Ctrl Pts',(0.727946961077783,-2.19149774367173,
0.436595820640553));
#96726=CARTESIAN_POINT('Ctrl Pts',(2.2359411788162,-0.57762978583554,0.547707471125989));
#96727=CARTESIAN_POINT('Ctrl Pts',(1.69827668332871,1.56494259322429,0.658819121611427));
#96728=CARTESIAN_POINT('Ctrl Pts',(-0.393188016825179,2.27560800163251,
0.769930772096863));
#96729=CARTESIAN_POINT('Ctrl Pts',(-2.12490816724285,0.90434536960108,0.881042422582301));
#96730=CARTESIAN_POINT('Ctrl Pts',(-1.9125222930514,-1.29434912039326,0.992154073067737));
#96731=CARTESIAN_POINT('Ctrl Pts',(0.0496630258143332,-2.30880650358359,
1.10326572355317));
#96732=CARTESIAN_POINT('Ctrl Pts',(1.96640931676781,-1.21090966106477,1.21437737403861));
#96733=CARTESIAN_POINT('Ctrl Pts',(2.08405785032279,0.994871990457256,1.32548902452405));
#96734=CARTESIAN_POINT('Ctrl Pts',(0.294968904732024,2.29042728261432,1.43660067500948));
#96735=CARTESIAN_POINT('Ctrl Pts',(-1.76399147035948,1.49043619583305,1.54771232549492));
#96736=CARTESIAN_POINT('Ctrl Pts',(-2.20904863824581,-0.673178902258552,
1.65882397598036));
#96737=CARTESIAN_POINT('Ctrl Pts',(-0.633012670336293,-2.22089176195486,
1.7699356264658));
#96738=CARTESIAN_POINT('Ctrl Pts',(1.52217643594786,-1.73667627565877,1.88104727695123));
#96739=CARTESIAN_POINT('Ctrl Pts',(2.28470258285089,0.336451535954383,1.99215892743667));
#96740=CARTESIAN_POINT('Ctrl Pts',(0.956918672404541,2.10175453516431,2.10327057792211));
#96741=CARTESIAN_POINT('Ctrl Pts',(-1.24636506047609,1.94412953698174,2.21438222840754));
#96742=CARTESIAN_POINT('Ctrl Pts',(-2.30932995110325,0.00779007092406014,
2.32549387889298));
#96743=CARTESIAN_POINT('Ctrl Pts',(-1.2594528285163,-1.93567664513544,2.43660552937842));
#96744=CARTESIAN_POINT('Ctrl Pts',(0.942717341349318,-2.1081625941051,2.54771717986386));
#96745=CARTESIAN_POINT('Ctrl Pts',(2.28238070382781,-0.351857683462,2.65882883034929));
#96746=CARTESIAN_POINT('Ctrl Pts',(1.53385834111148,1.72636731182735,2.76994048083473));
#96747=CARTESIAN_POINT('Ctrl Pts',(-0.618014955343493,2.22511191222357,
2.88105213132016));
#96748=CARTESIAN_POINT('Ctrl Pts',(-2.20445672440028,0.68806689849701,2.99216378180561));
#96749=CARTESIAN_POINT('Ctrl Pts',(-1.77400663329184,-1.47850125855229,
3.10327543229104));
#96750=CARTESIAN_POINT('Ctrl Pts',(0.279509811935462,-2.29236554058792,
3.21438708277648));
#96751=CARTESIAN_POINT('Ctrl Pts',(2.07729836817097,-1.00890881459812,3.32549873326191));
#96752=CARTESIAN_POINT('Ctrl Pts',(1.97453422882556,1.1976143309821,3.43661038374735));
#96753=CARTESIAN_POINT('Ctrl Pts',(0.0652379087403971,2.30842143506323,
3.54772203423278));
#96754=CARTESIAN_POINT('Ctrl Pts',(-1.90374559216213,1.30721774273047,3.65883368471823));
#96755=CARTESIAN_POINT('Ctrl Pts',(-2.13096254074055,-0.889979863001003,
3.76994533520366));
#96756=CARTESIAN_POINT('Ctrl Pts',(-0.408528604769679,-2.27292100295502,
3.8810569856891));
#96757=CARTESIAN_POINT('Ctrl Pts',(1.6876745272456,-1.57633124585981,3.99216863617453));
#96758=CARTESIAN_POINT('Ctrl Pts',(2.23979789625721,0.562468568463683,4.10328028665997));
#96759=CARTESIAN_POINT('Ctrl Pts',(0.742695215461042,2.18665711155622,4.21439193714541));
#96760=CARTESIAN_POINT('Ctrl Pts',(-1.43391090854028,1.81023893808443,4.32550358763085));
#96761=CARTESIAN_POINT('Ctrl Pts',(-2.29860956455329,-0.222395090620434,
4.43661523811628));
#96762=CARTESIAN_POINT('Ctrl Pts',(-1.06027445761331,-2.05155638019547,
4.54772688860172));
#96763=CARTESIAN_POINT('Ctrl Pts',(1.14812229735204,-2.00371672072451,4.65883853908716));
#96764=CARTESIAN_POINT('Ctrl Pts',(2.30608404475241,-0.122645363248325,
4.76995018957259));
#96765=CARTESIAN_POINT('Ctrl Pts',(1.35417351061808,1.87063615108022,4.88106184005803));
#96766=CARTESIAN_POINT('Ctrl Pts',(-0.83669150175529,2.1524434574405,4.99217349054346));
#96767=CARTESIAN_POINT('Ctrl Pts',(-2.26205440167697,0.464946653328952,
5.10328514102891));
#96768=CARTESIAN_POINT('Ctrl Pts',(-1.61782842764492,-1.64793709991974,
5.21439679151433));
#96769=CARTESIAN_POINT('Ctrl Pts',(0.506574022840452,-2.25309748257175,
5.32550844199978));
#96770=CARTESIAN_POINT('Ctrl Pts',(2.1675039941815,-0.796863816342033,5.43662009248521));
#96771=CARTESIAN_POINT('Ctrl Pts',(1.84535073495005,1.38843299139974,5.54773174297065));
#96772=CARTESIAN_POINT('Ctrl Pts',(-0.1651427104253,2.30343078727826,5.65884339345609));
#96773=CARTESIAN_POINT('Ctrl Pts',(-2.024544512798,1.1109838082922,5.76995504394152));
#96774=CARTESIAN_POINT('Ctrl Pts',(-2.03165894515671,-1.09791959503082,
5.88106669442697));
#96775=CARTESIAN_POINT('Ctrl Pts',(-0.179976902307884,-2.30231922661119,
5.99217834491239));
#96776=CARTESIAN_POINT('Ctrl Pts',(1.83636881720094,-1.40029106752845,6.10328999539785));
#96777=CARTESIAN_POINT('Ctrl Pts',(2.17259204728728,0.782885242326115,6.21440164588326));
#96778=CARTESIAN_POINT('Ctrl Pts',(0.521076907609949,2.24978762618687,6.32551329636872));
#96779=CARTESIAN_POINT('Ctrl Pts',(-1.60717962682088,1.6583242004264,6.43662494685413));
#96780=CARTESIAN_POINT('Ctrl Pts',(-2.26500243885858,-0.450365916286509,
6.5477365973396));
#96781=CARTESIAN_POINT('Ctrl Pts',(-0.850539171717745,-2.14700922773088,
6.65884824782501));
#96782=CARTESIAN_POINT('Ctrl Pts',(1.34209565723166,-1.87932029027199,6.76995989831046));
#96783=CARTESIAN_POINT('Ctrl Pts',(2.30682622449346,0.107788109627418,6.8810715487959));
#96784=CARTESIAN_POINT('Ctrl Pts',(1.16100547839306,1.99627948587589,6.99218319928133));
#96785=CARTESIAN_POINT('Ctrl Pts',(-1.04703729866327,2.05834360634882,7.10329484976677));
#96786=CARTESIAN_POINT('Ctrl Pts',(-2.29712931099768,0.237197038645086,
7.21440650025221));
#96787=CARTESIAN_POINT('Ctrl Pts',(-1.44554186745893,-1.80096480143545,
7.32551815073763));
#96788=CARTESIAN_POINT('Ctrl Pts',(0.72859438989827,-2.19139583863915,7.43662980122308));
#96789=CARTESIAN_POINT('Ctrl Pts',(2.23612826941383,-0.576884623911715,
7.5477414517085));
#96790=CARTESIAN_POINT('Ctrl Pts',(1.6977934979946,1.56542733614398,7.65885310219396));
#96791=CARTESIAN_POINT('Ctrl Pts',(-0.393879040694563,2.27550539615811,
7.76996475267938));
#96792=CARTESIAN_POINT('Ctrl Pts',(-2.12518549811472,0.903688057410859,
7.88107640316484));
#96793=CARTESIAN_POINT('Ctrl Pts',(-1.91212657747833,-1.29492758803799,
7.99218805365025));
#96794=CARTESIAN_POINT('Ctrl Pts',(0.0503667898133586,-2.30879377455661,
8.1032997041357));
#96795=CARTESIAN_POINT('Ctrl Pts',(1.96677879493939,-1.21030850518371,8.21441135462113));
#96796=CARTESIAN_POINT('Ctrl Pts',(2.08375418707704,0.995506903268707,8.32552300510658));
#96797=CARTESIAN_POINT('Ctrl Pts',(0.294270353677539,2.29051751091564,8.436634655592));
#96798=CARTESIAN_POINT('Ctrl Pts',(-1.76444601777748,1.4898978999011,8.54774630607746));
#96799=CARTESIAN_POINT('Ctrl Pts',(-2.2088431932234,-0.673852547682493,
8.65885795656288));
#96800=CARTESIAN_POINT('Ctrl Pts',(-0.632335256349382,-2.2210847899434,
8.76996960704833));
#96801=CARTESIAN_POINT('Ctrl Pts',(1.52270606837662,-1.73621188252162,8.88108125753376));
#96802=CARTESIAN_POINT('Ctrl Pts',(2.28459985995541,0.337148347205355,8.99219290801919));
#96803=CARTESIAN_POINT('Ctrl Pts',(0.956277562497704,2.10204633917866,9.10330455850463));
#96804=CARTESIAN_POINT('Ctrl Pts',(-1.2469579560031,1.94374924182257,9.21441620899007));
#96805=CARTESIAN_POINT('Ctrl Pts',(-2.30933226540692,0.00708579792413808,
9.32552785947551));
#96806=CARTESIAN_POINT('Ctrl Pts',(-1.25886228368054,-1.93606087509586,
9.43663950996094));
#96807=CARTESIAN_POINT('Ctrl Pts',(0.943360139257667,-2.10787462610152,
9.54775116044639));
#96808=CARTESIAN_POINT('Ctrl Pts',(2.28248823506631,-0.351162152961091,
9.65886281093181));
#96809=CARTESIAN_POINT('Ctrl Pts',(1.53333110744206,1.72683627576032,9.76997446141726));
#96810=CARTESIAN_POINT('Ctrl Pts',(-0.618692454411617,2.22492101746939,
9.88108611190268));
#96811=CARTESIAN_POINT('Ctrl Pts',(-2.20466868021367,0.687398848825245,
9.99219776238814));
#96812=CARTESIAN_POINT('Ctrl Pts',(-1.7735514221838,-1.47905058047522,10.1033094128735));
#96813=CARTESIAN_POINT('Ctrl Pts',(0.280201048116106,-2.29226437530741,
10.214421063359));
#96814=CARTESIAN_POINT('Ctrl Pts',(2.07762111854432,-1.0083052618152,10.3255327138444));
#96815=CARTESIAN_POINT('Ctrl Pts',(1.97414006873683,1.19827380577986,10.4366443643299));
#96816=CARTESIAN_POINT('Ctrl Pts',(0.0645886152005097,2.30833217918201,
10.5477560148153));
#96817=CARTESIAN_POINT('Ctrl Pts',(-1.90424854748374,1.30684465150768,10.6588676653008));
#96818=CARTESIAN_POINT('Ctrl Pts',(-2.13049227679005,-0.891025387309722,
10.7699793157862));
#96819=CARTESIAN_POINT('Ctrl Pts',(-0.408214485225542,-2.27228942196666,
10.8810909662716));
#96820=CARTESIAN_POINT('Ctrl Pts',(1.68888461736298,-1.5772814986318,10.9922026167571));
#96821=CARTESIAN_POINT('Ctrl Pts',(2.23817187934597,0.566161966084782,11.1033142672425));
#96822=CARTESIAN_POINT('Ctrl Pts',(1.24300218570944,1.64165746435707,11.1773887008995));
#96823=CARTESIAN_POINT('Ctrl Pts',(0.627850911123727,1.850383536838,11.2144259177279));
#96824=CARTESIAN_POINT('Ctrl Pts',(1.05793541951254,-1.4823699524473,-0.153382721514713));
#96825=CARTESIAN_POINT('Ctrl Pts',(1.55074231467859,-1.13066431478549,-0.116345504686234));
#96826=CARTESIAN_POINT('Ctrl Pts',(2.14955001436596,0.0967274517879858,
-0.0422710710292769));
#96827=CARTESIAN_POINT('Ctrl Pts',(1.08290436090784,1.86174541551099,0.0688405794561606));
#96828=CARTESIAN_POINT('Ctrl Pts',(-0.975409307071879,1.91793784975909,
0.179952229941597));
#96829=CARTESIAN_POINT('Ctrl Pts',(-2.14083151712633,0.22213180716797,0.291063880427034));
#96830=CARTESIAN_POINT('Ctrl Pts',(-1.34782279118508,-1.67833716661673,
0.402175530912471));
#96831=CARTESIAN_POINT('Ctrl Pts',(0.678460972679723,-2.04251926348523,
0.513287181397908));
#96832=CARTESIAN_POINT('Ctrl Pts',(2.08394142450739,-0.538362390807298,
0.624398831883346));
#96833=CARTESIAN_POINT('Ctrl Pts',(1.58282747515632,1.45855746470163,0.735510482368781));
#96834=CARTESIAN_POINT('Ctrl Pts',(-0.366459012269607,2.12091168831785,
0.84662213285422));
#96835=CARTESIAN_POINT('Ctrl Pts',(-1.98045646054783,0.842867780077688,
0.957733783339656));
#96836=CARTESIAN_POINT('Ctrl Pts',(-1.78250862301028,-1.20635899339281,
1.06884543382509));
#96837=CARTESIAN_POINT('Ctrl Pts',(0.0462869228141735,-2.15185334908375,
1.17995708431053));
#96838=CARTESIAN_POINT('Ctrl Pts',(1.83273239545565,-1.12859176615955,1.29106873479597));
#96839=CARTESIAN_POINT('Ctrl Pts',(1.94238315681312,0.927240382098824,1.4021803852814));
#96840=CARTESIAN_POINT('Ctrl Pts',(0.274916856192995,2.13472355144377,1.51329203576684));
#96841=CARTESIAN_POINT('Ctrl Pts',(-1.64407495706399,1.38911602796551,1.62440368625228));
#96842=CARTESIAN_POINT('Ctrl Pts',(-2.0588770445336,-0.62741605808422,1.73551533673771));
#96843=CARTESIAN_POINT('Ctrl Pts',(-0.589980335104445,-2.06991507018771,
1.84662698722315));
#96844=CARTESIAN_POINT('Ctrl Pts',(1.41869855984326,-1.61861665507704,1.95773863770859));
#96845=CARTESIAN_POINT('Ctrl Pts',(2.1293880179812,0.313579489369987,2.06885028819403));
#96846=CARTESIAN_POINT('Ctrl Pts',(0.891867138635642,1.95887681727571,2.17996193867946));
#96847=CARTESIAN_POINT('Ctrl Pts',(-1.16163690001897,1.8119671998123,2.2910735891649));
#96848=CARTESIAN_POINT('Ctrl Pts',(-2.1523412125303,0.0072605002547781,
2.40218523965033));
#96849=CARTESIAN_POINT('Ctrl Pts',(-1.1738349588193,-1.80408893734178,2.51329689013577));
#96850=CARTESIAN_POINT('Ctrl Pts',(0.878631217069615,-1.96484925501419,
2.62440854062121));
#96851=CARTESIAN_POINT('Ctrl Pts',(2.12722398078527,-0.327938323711113,
2.73552019110664));
#96852=CARTESIAN_POINT('Ctrl Pts',(1.42958632662274,1.60900849678758,2.84663184159209));
#96853=CARTESIAN_POINT('Ctrl Pts',(-0.57600216794938,2.07384833374845,2.95774349207752));
#96854=CARTESIAN_POINT('Ctrl Pts',(-2.05459728996263,0.641291965189069,
3.06885514256296));
#96855=CARTESIAN_POINT('Ctrl Pts',(-1.65340928710165,-1.37799243024573,
3.17996679304839));
#96856=CARTESIAN_POINT('Ctrl Pts',(0.260508675794864,-2.13653004623031,
3.29107844353384));
#96857=CARTESIAN_POINT('Ctrl Pts',(1.93608318568785,-0.940322979965331,
3.40219009401926));
#96858=CARTESIAN_POINT('Ctrl Pts',(1.84030497427301,1.11620025542831,3.51330174450471));
#96859=CARTESIAN_POINT('Ctrl Pts',(0.0608030219043116,2.15149445760286,
3.62441339499014));
#96860=CARTESIAN_POINT('Ctrl Pts',(-1.77432856410404,1.21835280406139,3.73552504547559));
#96861=CARTESIAN_POINT('Ctrl Pts',(-1.98609925645444,-0.829478843655077,
3.84663669596101));
#96862=CARTESIAN_POINT('Ctrl Pts',(-0.380756743800589,-2.11840735237885,
3.95774834644646));
#96863=CARTESIAN_POINT('Ctrl Pts',(1.57294605588646,-1.4691719143219,4.06885999693188));
#96864=CARTESIAN_POINT('Ctrl Pts',(2.08753596148093,0.524231836199493,4.17997164741733));
#96865=CARTESIAN_POINT('Ctrl Pts',(0.692206637610257,2.03800769856489,4.29108329790276));
#96866=CARTESIAN_POINT('Ctrl Pts',(-1.33643334165982,1.68717851215016,4.4021949483882));
#96867=CARTESIAN_POINT('Ctrl Pts',(-2.1423496001257,-0.207276625316418,
4.51330659887364));
#96868=CARTESIAN_POINT('Ctrl Pts',(-0.988196775702872,-1.91209114350017,
4.62441824935908));
#96869=CARTESIAN_POINT('Ctrl Pts',(1.07007270071357,-1.86750363419964,4.73552989984451));
#96870=CARTESIAN_POINT('Ctrl Pts',(2.1493159635798,-0.11430790551128,4.84664155032995));
#96871=CARTESIAN_POINT('Ctrl Pts',(1.26211650891535,1.74346990983058,4.95775320081538));
#96872=CARTESIAN_POINT('Ctrl Pts',(-0.779813036479037,2.00611989589323,
5.06886485130082));
#96873=CARTESIAN_POINT('Ctrl Pts',(-2.1082794649543,0.433339481484583,5.17997650178626));
#96874=CARTESIAN_POINT('Ctrl Pts',(-1.50784810891129,-1.53590998727594,
5.29108815227169));
#96875=CARTESIAN_POINT('Ctrl Pts',(0.472137013611209,-2.09993143910453,
5.40219980275713));
#96876=CARTESIAN_POINT('Ctrl Pts',(2.02015661416081,-0.742692845544967,
5.51331145324257));
#96877=CARTESIAN_POINT('Ctrl Pts',(1.71990340163759,1.29404702294652,5.62442310372801));
#96878=CARTESIAN_POINT('Ctrl Pts',(-0.153916274037652,2.14684307510999,
5.73553475421344));
#96879=CARTESIAN_POINT('Ctrl Pts',(-1.88691554856225,1.03545889399597,5.84664640469888));
#96880=CARTESIAN_POINT('Ctrl Pts',(-1.89354634030427,-1.02328278871562,
5.95775805518432));
#96881=CARTESIAN_POINT('Ctrl Pts',(-0.167742034418123,-2.1458070785722,
6.06886970566975));
#96882=CARTESIAN_POINT('Ctrl Pts',(1.71153207655705,-1.30509898455162,6.1799813561552));
#96883=CARTESIAN_POINT('Ctrl Pts',(2.02489878034016,0.729664537947597,6.29109300664062));
#96884=CARTESIAN_POINT('Ctrl Pts',(0.485653989206222,2.09684658745684,6.40220465712607));
#96885=CARTESIAN_POINT('Ctrl Pts',(-1.49792321581985,1.54559097049293,6.5133163076115));
#96886=CARTESIAN_POINT('Ctrl Pts',(-2.11102709394471,-0.41974994603061,
6.62442795809694));
#96887=CARTESIAN_POINT('Ctrl Pts',(-0.79271933890819,-2.0010550862688,6.73553960858237));
#96888=CARTESIAN_POINT('Ctrl Pts',(1.25085971055702,-1.7515636994031,6.84665125906781));
#96889=CARTESIAN_POINT('Ctrl Pts',(2.15000768978506,0.100460651134341,6.95776290955325));
#96890=CARTESIAN_POINT('Ctrl Pts',(1.08208008038219,1.86057198414926,7.06887456003868));
#96891=CARTESIAN_POINT('Ctrl Pts',(-0.975859481618359,1.91841697258389,
7.17998621052413));
#96892=CARTESIAN_POINT('Ctrl Pts',(-2.14096997451993,0.221072333783236,
7.29109786100956));
#96893=CARTESIAN_POINT('Ctrl Pts',(-1.34727362553083,-1.67853483327237,
7.402209511495));
#96894=CARTESIAN_POINT('Ctrl Pts',(0.679064389152043,-2.04242428597833,
7.51332116198043));
#96895=CARTESIAN_POINT('Ctrl Pts',(2.08411579664662,-0.537667885148679,
7.62443281246587));
#96896=CARTESIAN_POINT('Ctrl Pts',(1.58237713686343,1.4590092546951,7.73554446295131));
#96897=CARTESIAN_POINT('Ctrl Pts',(-0.367103060190181,2.1208160579853,7.84665611343674));
#96898=CARTESIAN_POINT('Ctrl Pts',(-1.98071493840836,0.842255152109201,
7.95776776392219));
#96899=CARTESIAN_POINT('Ctrl Pts',(-1.78213980826558,-1.20689813668469,
8.0688794144076));
#96900=CARTESIAN_POINT('Ctrl Pts',(0.0469428447876819,-2.15184148537872,
8.17999106489306));
#96901=CARTESIAN_POINT('Ctrl Pts',(1.83307675642296,-1.12803147698245,8.29110271537848));
#96902=CARTESIAN_POINT('Ctrl Pts',(1.94210013665906,0.927832133403047,8.40221436586394));
#96903=CARTESIAN_POINT('Ctrl Pts',(0.274265792786954,2.13480764600607,8.51332601634936));
#96904=CARTESIAN_POINT('Ctrl Pts',(-1.64449860425235,1.38861432550488,8.6244376668348));
#96905=CARTESIAN_POINT('Ctrl Pts',(-2.05868556570727,-0.628043908949741,
8.73554931732024));
#96906=CARTESIAN_POINT('Ctrl Pts',(-0.589348971863656,-2.07009497609277,
8.84666096780567));
#96907=CARTESIAN_POINT('Ctrl Pts',(1.41919218774748,-1.61818383148359,8.95777261829112));
#96908=CARTESIAN_POINT('Ctrl Pts',(2.12929227820989,0.314228931244718,9.06888426877654));
#96909=CARTESIAN_POINT('Ctrl Pts',(0.891269611515884,1.95914878439144,9.179995919262));
#96910=CARTESIAN_POINT('Ctrl Pts',(-1.16218949038264,1.81161275719849,9.29110756974741));
#96911=CARTESIAN_POINT('Ctrl Pts',(-2.15234336950711,0.00660410388236847,
9.40221922023287));
#96912=CARTESIAN_POINT('Ctrl Pts',(-1.17328455934639,-1.80444704726821,
9.51333087071829));
#96913=CARTESIAN_POINT('Ctrl Pts',(0.879230317440182,-1.96458086313641,
9.62444252120374));
#96914=CARTESIAN_POINT('Ctrl Pts',(2.12732420202743,-0.327290075520782,
9.73555417168917));
#96915=CARTESIAN_POINT('Ctrl Pts',(1.42909493440969,1.60944558045319,9.8466658221746));
#96916=CARTESIAN_POINT('Ctrl Pts',(-0.576633610487541,2.07367041606005,
9.95777747266004));
#96917=CARTESIAN_POINT('Ctrl Pts',(-2.05479483697499,0.640669329675303,
10.0688891231455));
#96918=CARTESIAN_POINT('Ctrl Pts',(-1.65298502134104,-1.37850440914814,
10.1800007736309));
#96919=CARTESIAN_POINT('Ctrl Pts',(0.26115292159373,-2.13643575818697,10.2911124241164));
#96920=CARTESIAN_POINT('Ctrl Pts',(1.93638399542254,-0.939760456828254,
10.4022240746018));
#96921=CARTESIAN_POINT('Ctrl Pts',(1.83993760927049,1.11681489898982,10.5133357250872));
#96922=CARTESIAN_POINT('Ctrl Pts',(0.0601978674766102,2.15141126935532,
10.6244473755726));
#96923=CARTESIAN_POINT('Ctrl Pts',(-1.77479732841649,1.21800507565884,10.7355590260581));
#96924=CARTESIAN_POINT('Ctrl Pts',(-1.98566096114678,-0.830453293000129,
10.8466706765435));
#96925=CARTESIAN_POINT('Ctrl Pts',(-0.380463978169507,-2.11781870639967,
10.957782327029));
#96926=CARTESIAN_POINT('Ctrl Pts',(1.57407388382168,-1.47005756870945,11.0688939775144));
#96927=CARTESIAN_POINT('Ctrl Pts',(2.08602048154327,0.527674155869038,11.1800056279999));
#96928=CARTESIAN_POINT('Ctrl Pts',(1.15850263419028,1.53005724266717,11.2540800616568));
#96929=CARTESIAN_POINT('Ctrl Pts',(0.585169473375027,1.72459407258861,11.2911172784853));
#96930=CARTESIAN_POINT('Ctrl Pts',(0.980771099081375,-1.37424797458507,
-0.0766913607573581));
#96931=CARTESIAN_POINT('Ctrl Pts',(1.43763335295088,-1.04819525110066,-0.0396541439288791));
#96932=CARTESIAN_POINT('Ctrl Pts',(1.99276486185844,0.089672287600667,0.0344202897280782));
#96933=CARTESIAN_POINT('Ctrl Pts',(1.00391884103562,1.72595232535247,0.145531940213516));
#96934=CARTESIAN_POINT('Ctrl Pts',(-0.904264325124765,1.77804616253862,
0.256643590698952));
#96935=CARTESIAN_POINT('Ctrl Pts',(-1.98468227953599,0.20592982580867,0.36775524118439));
#96936=CARTESIAN_POINT('Ctrl Pts',(-1.24951449388714,-1.55592161598129,
0.478866891669827));
#96937=CARTESIAN_POINT('Ctrl Pts',(0.628974984281669,-1.89354078329874,
0.589978542155263));
#96938=CARTESIAN_POINT('Ctrl Pts',(1.93194167019859,-0.499094995779056,
0.7010901926407));
#96939=CARTESIAN_POINT('Ctrl Pts',(1.46737826698393,1.35217233617898,0.812201843126137));
#96940=CARTESIAN_POINT('Ctrl Pts',(-0.339730007714042,1.96621537500318,
0.923313493611574));
#96941=CARTESIAN_POINT('Ctrl Pts',(-1.8360047538528,0.7813901905543,1.03442514409701));
#96942=CARTESIAN_POINT('Ctrl Pts',(-1.65249495296916,-1.11836886639236,
1.14553679458245));
#96943=CARTESIAN_POINT('Ctrl Pts',(0.0429108198140191,-1.99490019458391,
1.25664844506789));
#96944=CARTESIAN_POINT('Ctrl Pts',(1.69905547414348,-1.04627387125433,1.36776009555332));
#96945=CARTESIAN_POINT('Ctrl Pts',(1.80070846330345,0.859608773740392,1.47887174603876));
#96946=CARTESIAN_POINT('Ctrl Pts',(0.254864807653961,1.97901982027321,1.5899833965242));
#96947=CARTESIAN_POINT('Ctrl Pts',(-1.52415844376849,1.28779586009797,1.70109504700963));
#96948=CARTESIAN_POINT('Ctrl Pts',(-1.90870545082139,-0.581653213909888,
1.81220669749507));
#96949=CARTESIAN_POINT('Ctrl Pts',(-0.546947999872595,-1.91893837842057,
1.92331834798051));
#96950=CARTESIAN_POINT('Ctrl Pts',(1.31522068373867,-1.50055703449532,2.03442999846594));
#96951=CARTESIAN_POINT('Ctrl Pts',(1.97407345311151,0.290707442785592,2.14554164895138));
#96952=CARTESIAN_POINT('Ctrl Pts',(0.826815604866742,1.81599909938712,2.25665329943681));
#96953=CARTESIAN_POINT('Ctrl Pts',(-1.07690873956185,1.67980486264285,2.36776494992226));
#96954=CARTESIAN_POINT('Ctrl Pts',(-1.99535247395734,0.00673092958549589,
2.47887660040769));
#96955=CARTESIAN_POINT('Ctrl Pts',(-1.0882170891223,-1.67250122954812,2.58998825089313));
#96956=CARTESIAN_POINT('Ctrl Pts',(0.814545092789914,-1.82153591592328,
2.70109990137857));
#96957=CARTESIAN_POINT('Ctrl Pts',(1.97206725774273,-0.304018963960226,
2.812211551864));
#96958=CARTESIAN_POINT('Ctrl Pts',(1.325314312134,1.49164968174781,2.92332320234944));
#96959=CARTESIAN_POINT('Ctrl Pts',(-0.533989380555266,1.92258475527334,
3.03443485283487));
#96960=CARTESIAN_POINT('Ctrl Pts',(-1.90473785552499,0.594517031881129,
3.14554650332031));
#96961=CARTESIAN_POINT('Ctrl Pts',(-1.53281194091147,-1.27748360193918,
3.25665815380575));
#96962=CARTESIAN_POINT('Ctrl Pts',(0.241507539654265,-1.98069455187271,
3.36776980429119));
#96963=CARTESIAN_POINT('Ctrl Pts',(1.79486800320472,-0.871737145332536,
3.47888145477662));
#96964=CARTESIAN_POINT('Ctrl Pts',(1.70607571972046,1.03478617987453,3.58999310526206));
#96965=CARTESIAN_POINT('Ctrl Pts',(0.0563681350682242,1.99456748014249,
3.7011047557475));
#96966=CARTESIAN_POINT('Ctrl Pts',(-1.64491153604594,1.1294878653923,3.81221640623293));
#96967=CARTESIAN_POINT('Ctrl Pts',(-1.84123597216834,-0.768977824309152,
3.92332805671837));
#96968=CARTESIAN_POINT('Ctrl Pts',(-0.352984882831497,-1.96389370180267,
4.03443970720381));
#96969=CARTESIAN_POINT('Ctrl Pts',(1.45821758452731,-1.36201258278399,4.14555135768924));
#96970=CARTESIAN_POINT('Ctrl Pts',(1.93527402670466,0.485995103935303,4.25666300817468));
#96971=CARTESIAN_POINT('Ctrl Pts',(0.641718059759468,1.88935828557357,4.36777465866012));
#96972=CARTESIAN_POINT('Ctrl Pts',(-1.23895577477937,1.56411808621589,4.47888630914555));
#96973=CARTESIAN_POINT('Ctrl Pts',(-1.98608963569812,-0.1921581600124,4.58999795963099));
#96974=CARTESIAN_POINT('Ctrl Pts',(-0.916119093792434,-1.77262590680487,
4.70110961011643));
#96975=CARTESIAN_POINT('Ctrl Pts',(0.992023104075105,-1.73129054767478,
4.81222126060186));
#96976=CARTESIAN_POINT('Ctrl Pts',(1.99254788240719,-0.105970447774237,
4.9233329110873));
#96977=CARTESIAN_POINT('Ctrl Pts',(1.17005950721263,1.61630366858093,5.03444456157274));
#96978=CARTESIAN_POINT('Ctrl Pts',(-0.722934571202785,1.85979633434597,
5.14555621205818));
#96979=CARTESIAN_POINT('Ctrl Pts',(-1.95450452823164,0.401732309640217,
5.25666786254361));
#96980=CARTESIAN_POINT('Ctrl Pts',(-1.39786779017765,-1.42388287463214,
5.36777951302905));
#96981=CARTESIAN_POINT('Ctrl Pts',(0.437700004381964,-1.9467653956373,5.47889116351449));
#96982=CARTESIAN_POINT('Ctrl Pts',(1.87280923414012,-0.688521874747905,
5.59000281399993));
#96983=CARTESIAN_POINT('Ctrl Pts',(1.59445606832513,1.19966105449332,5.70111446448536));
#96984=CARTESIAN_POINT('Ctrl Pts',(-0.142689837650004,1.99025536294172,
5.81222611497081));
#96985=CARTESIAN_POINT('Ctrl Pts',(-1.74928658432651,0.959933979699734,
5.92333776545623));
#96986=CARTESIAN_POINT('Ctrl Pts',(-1.75543373545183,-0.948645982400418,
6.03444941594168));
#96987=CARTESIAN_POINT('Ctrl Pts',(-0.155507166528361,-1.98929493053321,
6.1455610664271));
#96988=CARTESIAN_POINT('Ctrl Pts',(1.58669533591315,-1.20990690157479,6.25667271691256));
#96989=CARTESIAN_POINT('Ctrl Pts',(1.87720551339304,0.676443833569079,6.36778436739797));
#96990=CARTESIAN_POINT('Ctrl Pts',(0.450231070802491,1.94390554872681,6.47889601788343));
#96991=CARTESIAN_POINT('Ctrl Pts',(-1.38866680481881,1.43285774055946,6.59000766836885));
#96992=CARTESIAN_POINT('Ctrl Pts',(-1.95705174903083,-0.38913397577471,
6.7011193188543));
#96993=CARTESIAN_POINT('Ctrl Pts',(-0.734899506098636,-1.85510094480672,
6.81223096933973));
#96994=CARTESIAN_POINT('Ctrl Pts',(1.15962376388238,-1.62380710853421,6.92334261982516));
#96995=CARTESIAN_POINT('Ctrl Pts',(1.99318915507666,0.0931331926412601,
7.03445427031061));
#96996=CARTESIAN_POINT('Ctrl Pts',(1.00315468237132,1.72486448242263,7.14556592079604));
#96997=CARTESIAN_POINT('Ctrl Pts',(-0.904681664573454,1.77849033881895,
7.25667757128148));
#96998=CARTESIAN_POINT('Ctrl Pts',(-1.98481063804218,0.204947628921387,
7.36778922176691));
#96999=CARTESIAN_POINT('Ctrl Pts',(-1.24900538360275,-1.55610486510929,
7.47890087225236));
#97000=CARTESIAN_POINT('Ctrl Pts',(0.629534388405818,-1.89345273331751,
7.59001252273779));
#97001=CARTESIAN_POINT('Ctrl Pts',(1.93210332387941,-0.498451146385645,
7.70112417322323));
#97002=CARTESIAN_POINT('Ctrl Pts',(1.46696077573226,1.35259117324623,7.81223582370866));
#97003=CARTESIAN_POINT('Ctrl Pts',(-0.340327079685797,1.96612671981249,
7.9233474741941));
#97004=CARTESIAN_POINT('Ctrl Pts',(-1.836244378702,0.780822246807544,8.03445912467955));
#97005=CARTESIAN_POINT('Ctrl Pts',(-1.65215303905282,-1.11886868533138,
8.14557077516496));
#97006=CARTESIAN_POINT('Ctrl Pts',(0.0435188997620014,-1.99488919620082,
8.25668242565042));
#97007=CARTESIAN_POINT('Ctrl Pts',(1.69937471790653,-1.04575444878119,8.36779407613584));
#97008=CARTESIAN_POINT('Ctrl Pts',(1.80044608624107,0.860157363537389,8.47890572662129));
#97009=CARTESIAN_POINT('Ctrl Pts',(0.254261231896373,1.97909778109651,8.59001737710672));
#97010=CARTESIAN_POINT('Ctrl Pts',(-1.52455119072723,1.28733075110866,8.70112902759215));
#97011=CARTESIAN_POINT('Ctrl Pts',(-1.90852793819114,-0.58223527021699,
8.8122406780776));
#97012=CARTESIAN_POINT('Ctrl Pts',(-0.546362687377931,-1.91910516224214,
8.92335232856302));
#97013=CARTESIAN_POINT('Ctrl Pts',(1.31567830711834,-1.50015578044556,9.03446397904849));
#97014=CARTESIAN_POINT('Ctrl Pts',(1.97398469646436,0.291309515284085,9.14557562953389));
#97015=CARTESIAN_POINT('Ctrl Pts',(0.826261660534066,1.81625122960423,9.25668728001935));
#97016=CARTESIAN_POINT('Ctrl Pts',(-1.07742102476217,1.67947627257441,9.36779893050478));
#97017=CARTESIAN_POINT('Ctrl Pts',(-1.99535447360731,0.00612240984059651,
9.47891058099021));
#97018=CARTESIAN_POINT('Ctrl Pts',(-1.08770683501224,-1.67283321944057,
9.59002223147566));
#97019=CARTESIAN_POINT('Ctrl Pts',(0.815100495622697,-1.82128710017129,
9.70113388196108));
#97020=CARTESIAN_POINT('Ctrl Pts',(1.97216016898856,-0.303417998080474,
9.81224553244654));
#97021=CARTESIAN_POINT('Ctrl Pts',(1.32485876137733,1.49205488514605,9.92335718293196));
#97022=CARTESIAN_POINT('Ctrl Pts',(-0.534574766563464,1.9224198146507,10.0344688334174));
#97023=CARTESIAN_POINT('Ctrl Pts',(-1.90492099373632,0.593939810525364,
10.1455804839028));
#97024=CARTESIAN_POINT('Ctrl Pts',(-1.53241862049827,-1.27795823782107,
10.2566921343883));
#97025=CARTESIAN_POINT('Ctrl Pts',(0.242104795071353,-1.98060714106653,
10.3678037848737));
#97026=CARTESIAN_POINT('Ctrl Pts',(1.79514687230076,-0.871215651841315,
10.4789154353591));
#97027=CARTESIAN_POINT('Ctrl Pts',(1.70573514980415,1.03535599219979,10.5900270858446));
#97028=CARTESIAN_POINT('Ctrl Pts',(0.055807119752709,1.99449035952863,10.70113873633));
#97029=CARTESIAN_POINT('Ctrl Pts',(-1.64534610934924,1.12916549981001,10.8122503868155));
#97030=CARTESIAN_POINT('Ctrl Pts',(-1.84082964550351,-0.769881198690536,
10.9233620373009));
#97031=CARTESIAN_POINT('Ctrl Pts',(-0.352713471113472,-1.96334799083268,
11.0344736877863));
#97032=CARTESIAN_POINT('Ctrl Pts',(1.45926315028039,-1.36283363878709,11.1455853382718));
#97033=CARTESIAN_POINT('Ctrl Pts',(1.93386908374058,0.489186345653294,11.2566969887572));
#97034=CARTESIAN_POINT('Ctrl Pts',(1.07400308267113,1.41845702097726,11.3307714224142));
#97035=CARTESIAN_POINT('Ctrl Pts',(0.542488035626326,1.59880460833922,11.3678086392426));
#97036=CARTESIAN_POINT('Ctrl Pts',(0.903606778650208,-1.26612599672284,
-2.77555756156289E-15));
#97037=CARTESIAN_POINT('Ctrl Pts',(1.32452439122316,-0.965726187415828,
0.0370372168284762));
#97038=CARTESIAN_POINT('Ctrl Pts',(1.83597970935092,0.0826171234133487,
0.111111650485434));
#97039=CARTESIAN_POINT('Ctrl Pts',(0.924933321163406,1.59015923519395,0.222223300970871));
#97040=CARTESIAN_POINT('Ctrl Pts',(-0.833119343177651,1.63815447531815,
0.333334951456308));
#97041=CARTESIAN_POINT('Ctrl Pts',(-1.82853304194564,0.18972784444937,0.444446601941745));
#97042=CARTESIAN_POINT('Ctrl Pts',(-1.15120619658919,-1.43350606534586,
0.555558252427182));
#97043=CARTESIAN_POINT('Ctrl Pts',(0.579488995883613,-1.74456230311225,
0.666669902912619));
#97044=CARTESIAN_POINT('Ctrl Pts',(1.77994191588978,-0.459827600750814,
0.777781553398056));
#97045=CARTESIAN_POINT('Ctrl Pts',(1.35192905881154,1.24578720765632,0.888893203883492));
#97046=CARTESIAN_POINT('Ctrl Pts',(-0.313001003158473,1.81151906168851,
1.00000485436893));
#97047=CARTESIAN_POINT('Ctrl Pts',(-1.69155304715778,0.719912601030908,
1.11111650485437));
#97048=CARTESIAN_POINT('Ctrl Pts',(-1.52248128292804,-1.03037873939191,
1.2222281553398));
#97049=CARTESIAN_POINT('Ctrl Pts',(0.0395347168138628,-1.83794704008407,
1.33333980582524));
#97050=CARTESIAN_POINT('Ctrl Pts',(1.56537855283131,-0.963955976349113,
1.44445145631068));
#97051=CARTESIAN_POINT('Ctrl Pts',(1.65903376979378,0.791977165381959,1.55556310679611));
#97052=CARTESIAN_POINT('Ctrl Pts',(0.234812759114929,1.82331608910266,1.66667475728155));
#97053=CARTESIAN_POINT('Ctrl Pts',(-1.404241930473,1.18647569223042,1.77778640776699));
#97054=CARTESIAN_POINT('Ctrl Pts',(-1.75853385710917,-0.535890369735552,
1.88889805825242));
#97055=CARTESIAN_POINT('Ctrl Pts',(-0.503915664640746,-1.76796168665343,
2.00000970873786));
#97056=CARTESIAN_POINT('Ctrl Pts',(1.21174280763407,-1.38249741391359,2.1111213592233));
#97057=CARTESIAN_POINT('Ctrl Pts',(1.81875888824183,0.267835396201195,2.22223300970874));
#97058=CARTESIAN_POINT('Ctrl Pts',(0.761764071097843,1.67312138149853,2.33334466019417));
#97059=CARTESIAN_POINT('Ctrl Pts',(-0.992180579104728,1.54764252547341,
2.44445631067961));
#97060=CARTESIAN_POINT('Ctrl Pts',(-1.83836373538439,0.00620135891621234,
2.55556796116504));
#97061=CARTESIAN_POINT('Ctrl Pts',(-1.0025992194253,-1.54091352175446,2.66667961165049));
#97062=CARTESIAN_POINT('Ctrl Pts',(0.750458968510211,-1.67822257683237,
2.77779126213592));
#97063=CARTESIAN_POINT('Ctrl Pts',(1.81691053470019,-0.280099604209337,
2.88890291262136));
#97064=CARTESIAN_POINT('Ctrl Pts',(1.22104229764526,1.37429086670804,3.0000145631068));
#97065=CARTESIAN_POINT('Ctrl Pts',(-0.491976593161155,1.77132117679823,
3.11112621359223));
#97066=CARTESIAN_POINT('Ctrl Pts',(-1.75487842108734,0.547742098573187,
3.22223786407767));
#97067=CARTESIAN_POINT('Ctrl Pts',(-1.41221459472129,-1.17697477363263,
3.3333495145631));
#97068=CARTESIAN_POINT('Ctrl Pts',(0.222506403513669,-1.8248590575151,3.44446116504855));
#97069=CARTESIAN_POINT('Ctrl Pts',(1.65365282072159,-0.803151310699741,
3.55557281553397));
#97070=CARTESIAN_POINT('Ctrl Pts',(1.57184646516792,0.953372104320743,3.66668446601942));
#97071=CARTESIAN_POINT('Ctrl Pts',(0.0519332482321354,1.83764050268212,
3.77779611650485));
#97072=CARTESIAN_POINT('Ctrl Pts',(-1.51549450798785,1.04062292672322,3.88890776699029));
#97073=CARTESIAN_POINT('Ctrl Pts',(-1.69637268788223,-0.708476804963227,
4.00001941747572));
#97074=CARTESIAN_POINT('Ctrl Pts',(-0.325213021862407,-1.80938005122649,
4.11113106796117));
#97075=CARTESIAN_POINT('Ctrl Pts',(1.34348911316817,-1.25485325124609,4.2222427184466));
#97076=CARTESIAN_POINT('Ctrl Pts',(1.78301209192838,0.447758371671112,4.33335436893204));
#97077=CARTESIAN_POINT('Ctrl Pts',(0.591229481908682,1.74070887258225,4.44446601941748));
#97078=CARTESIAN_POINT('Ctrl Pts',(-1.14147820789891,1.44105766028162,4.55557766990291));
#97079=CARTESIAN_POINT('Ctrl Pts',(-1.82982967127054,-0.177039694708382,
4.66668932038835));
#97080=CARTESIAN_POINT('Ctrl Pts',(-0.844041411881997,-1.63316067010957,
4.77780097087378));
#97081=CARTESIAN_POINT('Ctrl Pts',(0.913973507436636,-1.59507746114991,
4.88891262135923));
#97082=CARTESIAN_POINT('Ctrl Pts',(1.83577980123458,-0.0976329900371924,
5.00002427184466));
#97083=CARTESIAN_POINT('Ctrl Pts',(1.0780025055099,1.48913742733129,5.1111359223301));
#97084=CARTESIAN_POINT('Ctrl Pts',(-0.666056105926533,1.7134727727987,5.22224757281553));
#97085=CARTESIAN_POINT('Ctrl Pts',(-1.80072959150898,0.37012513779585,5.33335922330097));
#97086=CARTESIAN_POINT('Ctrl Pts',(-1.28788747144402,-1.31185576198834,
5.44447087378641));
#97087=CARTESIAN_POINT('Ctrl Pts',(0.403262995152723,-1.79359935217008,
5.55558252427184));
#97088=CARTESIAN_POINT('Ctrl Pts',(1.72546185411942,-0.634350903950841,
5.66669417475728));
#97089=CARTESIAN_POINT('Ctrl Pts',(1.46900873501267,1.1052750860401,5.77780582524271));
#97090=CARTESIAN_POINT('Ctrl Pts',(-0.13146340126236,1.83366765077345,5.88891747572816));
#97091=CARTESIAN_POINT('Ctrl Pts',(-1.61165762009075,0.884409065403499,
6.00002912621358));
#97092=CARTESIAN_POINT('Ctrl Pts',(-1.6173211305994,-0.87400917608522,6.11114077669903));
#97093=CARTESIAN_POINT('Ctrl Pts',(-0.143272298638598,-1.83278278249422,
6.22225242718446));
#97094=CARTESIAN_POINT('Ctrl Pts',(1.46185859526926,-1.11471481859797,6.33336407766989));
#97095=CARTESIAN_POINT('Ctrl Pts',(1.72951224644592,0.623223129190563,6.44447572815534));
#97096=CARTESIAN_POINT('Ctrl Pts',(0.414808152398764,1.79096450999678,6.55558737864077));
#97097=CARTESIAN_POINT('Ctrl Pts',(-1.27941039381778,1.320124510626,6.66669902912621));
#97098=CARTESIAN_POINT('Ctrl Pts',(-1.80307640411694,-0.358518005518811,
6.77781067961165));
#97099=CARTESIAN_POINT('Ctrl Pts',(-0.677079673289082,-1.70914680334463,
6.8889223300971));
#97100=CARTESIAN_POINT('Ctrl Pts',(1.06838781720774,-1.49605051766532,7.00003398058251));
#97101=CARTESIAN_POINT('Ctrl Pts',(1.83637062036826,0.0858057341481814,
7.11114563106797));
#97102=CARTESIAN_POINT('Ctrl Pts',(0.924229284360448,1.589156980696,7.22225728155339));
#97103=CARTESIAN_POINT('Ctrl Pts',(-0.833503847528551,1.63856370505402,
7.33336893203883));
#97104=CARTESIAN_POINT('Ctrl Pts',(-1.82865130156443,0.188822924059537,
7.44448058252428));
#97105=CARTESIAN_POINT('Ctrl Pts',(-1.15073714167466,-1.43367489694622,
7.5555922330097));
#97106=CARTESIAN_POINT('Ctrl Pts',(0.580004387659595,-1.74448118065669,
7.66670388349515));
#97107=CARTESIAN_POINT('Ctrl Pts',(1.7800908511122,-0.459234407622611,7.77781553398057));
#97108=CARTESIAN_POINT('Ctrl Pts',(1.35154441460109,1.24617309179735,7.88892718446602));
#97109=CARTESIAN_POINT('Ctrl Pts',(-0.313551099181417,1.81143738163968,
8.00003883495145));
#97110=CARTESIAN_POINT('Ctrl Pts',(-1.69177381899564,0.719389341505889,
8.11115048543689));
#97111=CARTESIAN_POINT('Ctrl Pts',(-1.52216626984007,-1.03083923397808,
8.22226213592232));
#97112=CARTESIAN_POINT('Ctrl Pts',(0.0400949547363229,-1.83793690702293,
8.33337378640777));
#97113=CARTESIAN_POINT('Ctrl Pts',(1.56567267939011,-0.963477420579929,
8.44448543689319));
#97114=CARTESIAN_POINT('Ctrl Pts',(1.65879203582308,0.792482593671729,8.55559708737864));
#97115=CARTESIAN_POINT('Ctrl Pts',(0.234256671005791,1.82338791618694,8.66670873786407));
#97116=CARTESIAN_POINT('Ctrl Pts',(-1.40460377720211,1.18604717671243,8.77782038834951));
#97117=CARTESIAN_POINT('Ctrl Pts',(-1.75837031067501,-0.536426631484242,
8.88893203883495));
#97118=CARTESIAN_POINT('Ctrl Pts',(-0.503376402892206,-1.7681153483915,
9.00004368932038));
#97119=CARTESIAN_POINT('Ctrl Pts',(1.2121644264892,-1.38212772940753,9.11115533980582));
#97120=CARTESIAN_POINT('Ctrl Pts',(1.81867711471885,0.26839009932345,9.22226699029127));
#97121=CARTESIAN_POINT('Ctrl Pts',(0.761253709552246,1.67335367481701,9.33337864077668));
#97122=CARTESIAN_POINT('Ctrl Pts',(-0.99265255914171,1.54733978795034,9.44449029126215));
#97123=CARTESIAN_POINT('Ctrl Pts',(-1.8383655777075,0.00564071579882353,
9.55560194174756));
#97124=CARTESIAN_POINT('Ctrl Pts',(-1.00212911067809,-1.54121939161292,
9.66671359223301));
#97125=CARTESIAN_POINT('Ctrl Pts',(0.750970673805211,-1.67799333720618,
9.77782524271844));
#97126=CARTESIAN_POINT('Ctrl Pts',(1.81699613594968,-0.279545920640164,
9.88893689320389));
#97127=CARTESIAN_POINT('Ctrl Pts',(1.22062258834496,1.37466418983892,10.0000485436893));
#97128=CARTESIAN_POINT('Ctrl Pts',(-0.492515922639386,1.77116921324136,
10.1111601941748));
#97129=CARTESIAN_POINT('Ctrl Pts',(-1.75504715049764,0.547210291375423,
10.2222718446602));
#97130=CARTESIAN_POINT('Ctrl Pts',(-1.4118522196555,-1.177412066494,10.3333834951456));
#97131=CARTESIAN_POINT('Ctrl Pts',(0.223056668548975,-1.82477852394609,
10.4444951456311));
#97132=CARTESIAN_POINT('Ctrl Pts',(1.65390974917898,-0.802670846854376,
10.5556067961165));
#97133=CARTESIAN_POINT('Ctrl Pts',(1.57153269033781,0.953897085409752,10.6667184466019));
#97134=CARTESIAN_POINT('Ctrl Pts',(0.0514163720288116,1.83756944970195,
10.7778300970874));
#97135=CARTESIAN_POINT('Ctrl Pts',(-1.51589489028199,1.04032592396117,10.8889417475728));
#97136=CARTESIAN_POINT('Ctrl Pts',(-1.69599832986023,-0.709309104380943,
11.0000533980583));
#97137=CARTESIAN_POINT('Ctrl Pts',(-0.324962964057439,-1.80887727526569,
11.1111650485437));
#97138=CARTESIAN_POINT('Ctrl Pts',(1.34445241673909,-1.25560970886474,11.2222766990291));
#97139=CARTESIAN_POINT('Ctrl Pts',(1.78171768593789,0.450698535437549,11.3333883495146));
#97140=CARTESIAN_POINT('Ctrl Pts',(0.989503531151977,1.30685679928735,11.4074627831715));
#97141=CARTESIAN_POINT('Ctrl Pts',(0.499806597877626,1.47301514408983,11.4445));
#97142=CARTESIAN_POINT('',(0.903606778650206,-1.26612599672284,0.));
#97143=CARTESIAN_POINT('Ctrl Pts',(0.903606778650208,-1.26612599672284,
-2.77555756156289E-15));
#97144=CARTESIAN_POINT('Ctrl Pts',(1.32452439122316,-0.965726187415828,
0.0370372168284762));
#97145=CARTESIAN_POINT('Ctrl Pts',(1.83597970935092,0.0826171234133487,
0.111111650485434));
#97146=CARTESIAN_POINT('Ctrl Pts',(0.924933321163406,1.59015923519395,0.222223300970871));
#97147=CARTESIAN_POINT('Ctrl Pts',(-0.833119343177651,1.63815447531815,
0.333334951456308));
#97148=CARTESIAN_POINT('Ctrl Pts',(-1.5310616378989,0.622578531632503,0.411241775931451));
#97149=CARTESIAN_POINT('Ctrl Pts',(-1.55772922446558,0.0543356393242454,
0.452111383578116));
#97150=CARTESIAN_POINT('Ctrl Pts',(-1.55735926886437,0.00101346774827265,
0.455943774396301));
#97151=CARTESIAN_POINT('Ctrl Pts',(0.863567639152676,1.75641488315944,2.28983498828939E-16));
#97152=CARTESIAN_POINT('Ctrl Pts',(0.902605506355985,1.73244147111074,2.48310810971475E-16));
#97153=CARTESIAN_POINT('Ctrl Pts',(0.940681517855526,1.70703362163956,1.53446104133306E-16));
#97154=CARTESIAN_POINT('Ctrl Pts',(0.977705169885396,1.68018661523996,1.12757025938492E-16));
#97155=CARTESIAN_POINT('Ctrl Pts',(1.0358643592122,1.63801357064694,3.49621561433049E-17));
#97156=CARTESIAN_POINT('Ctrl Pts',(1.09142895154027,1.59229038852923,-3.14041157591089E-18));
#97157=CARTESIAN_POINT('Ctrl Pts',(1.14423757319707,1.54335784953327,-1.00613961606655E-16));
#97158=CARTESIAN_POINT('Ctrl Pts',(1.16947625472704,1.51997165369202,-1.47199231391008E-16));
#97159=CARTESIAN_POINT('Ctrl Pts',(1.19408480623982,1.49585194230134,-1.44940981238328E-16));
#97160=CARTESIAN_POINT('Ctrl Pts',(1.21804196717247,1.47103398018765,-1.04083408558608E-16));
#97161=CARTESIAN_POINT('Ctrl Pts',(1.23020142841566,1.45843761915368,-8.33461403619852E-17));
#97162=CARTESIAN_POINT('Ctrl Pts',(1.24219304748387,1.44566136836505,-3.17714931440926E-16));
#97163=CARTESIAN_POINT('Ctrl Pts',(1.25401379483509,1.43270976178997,-3.05311331771918E-16));
#97164=CARTESIAN_POINT('Ctrl Pts',(1.26389181876557,1.42188673377951,-2.94946246493115E-16));
#97165=CARTESIAN_POINT('Ctrl Pts',(1.27364380619492,1.41094858444086,-5.46603369369435E-16));
#97166=CARTESIAN_POINT('Ctrl Pts',(1.28326720497828,1.3998998522991,-5.34294830600857E-16));
#97167=CARTESIAN_POINT('Ctrl Pts',(1.330154786252,1.3460676940429,-4.74324582576826E-16));
#97168=CARTESIAN_POINT('Ctrl Pts',(1.37400431756963,1.2896005558432,-2.78813144032988E-17));
#97169=CARTESIAN_POINT('Ctrl Pts',(1.41465239664765,1.2308327382907,1.45716771982052E-16));
#97170=CARTESIAN_POINT('Ctrl Pts',(1.44369336478921,1.18884614615641,2.69743702909727E-16));
#97171=CARTESIAN_POINT('Ctrl Pts',(1.47109927736379,1.14568453076923,1.23340209484872E-16));
#97172=CARTESIAN_POINT('Ctrl Pts',(1.4967949674738,1.10146499100096,1.52655665885959E-16));
#97173=CARTESIAN_POINT('Ctrl Pts',(1.51164370962241,1.07591189080641,1.69596158676961E-16));
#97174=CARTESIAN_POINT('Ctrl Pts',(1.5259211042574,1.05000546373499,-2.47389032972511E-16));
#97175=CARTESIAN_POINT('Ctrl Pts',(1.53961051084784,1.0237681518455,-2.63677968348475E-16));
#97176=CARTESIAN_POINT('Ctrl Pts',(1.5453767175419,1.01271655786648,-2.70539139983884E-16));
#97177=CARTESIAN_POINT('Ctrl Pts',(1.55103417937643,1.00161467257822,6.72528652799515E-17));
#97178=CARTESIAN_POINT('Ctrl Pts',(1.55658137030158,0.990465869694384,6.24500451351651E-17));
#97179=CARTESIAN_POINT('Ctrl Pts',(1.58759523113096,0.928133884781808,3.5597896440648E-17));
#97180=CARTESIAN_POINT('Ctrl Pts',(1.61517455934254,0.864320573166324,-1.32844578099872E-16));
#97181=CARTESIAN_POINT('Ctrl Pts',(1.639165272121,0.799334213601843,-1.80411241501588E-16));
#97182=CARTESIAN_POINT('Ctrl Pts',(1.66256479067373,0.735949288762567,-2.26805737281603E-16));
#97183=CARTESIAN_POINT('Ctrl Pts',(1.68255047093124,0.671447445488438,-3.92048207771591E-16));
#97184=CARTESIAN_POINT('Ctrl Pts',(1.69893099532196,0.606109731061441,-4.30211422042248E-16));
#97185=CARTESIAN_POINT('Ctrl Pts',(1.70969999791506,0.563154939181291,-4.55300957861645E-16));
#97186=CARTESIAN_POINT('Ctrl Pts',(1.71890982821634,0.519838805550124,-3.77882014063636E-16));
#97187=CARTESIAN_POINT('Ctrl Pts',(1.72649398406889,0.476242912678102,-4.71844785465692E-16));
#97188=CARTESIAN_POINT('Ctrl Pts',(1.73287054571603,0.439588616027976,-5.50846247992205E-16));
#97189=CARTESIAN_POINT('Ctrl Pts',(1.73809775889755,0.402736552578244,-9.42921937940892E-17));
#97190=CARTESIAN_POINT('Ctrl Pts',(1.74213052178609,0.36573694696249,-1.2490009027033E-16));
#97191=CARTESIAN_POINT('Ctrl Pts',(1.74338539139703,0.354223827548557,-1.34424309820125E-16));
#97192=CARTESIAN_POINT('Ctrl Pts',(1.74452450777523,0.342696049837886,-3.03274465566551E-16));
#97193=CARTESIAN_POINT('Ctrl Pts',(1.74554535151306,0.331170337018761,-2.91433543964104E-16));
#97194=CARTESIAN_POINT('Ctrl Pts',(1.75129431083391,0.266262406759456,-2.24750491415529E-16));
#97195=CARTESIAN_POINT('Ctrl Pts',(1.75331011127704,0.201301920292928,9.80627071070611E-17));
#97196=CARTESIAN_POINT('Ctrl Pts',(1.75142561531544,0.136549272921142,2.77555756156289E-17));
#97197=CARTESIAN_POINT('Ctrl Pts',(1.75088296778463,0.11790351037964,7.510378979319E-18));
#97198=CARTESIAN_POINT('Ctrl Pts',(1.75001659332986,0.099275023041261,-5.08054903583662E-16));
#97199=CARTESIAN_POINT('Ctrl Pts',(1.74882170147482,0.0806701752180915,
-4.85722573273506E-16));
#97200=CARTESIAN_POINT('Ctrl Pts',(1.74442082328573,0.0121470962041962,
-4.16579971360731E-16));
#97201=CARTESIAN_POINT('Ctrl Pts',(1.73556771390717,-0.056057442313777,
-1.52368272571946E-16));
#97202=CARTESIAN_POINT('Ctrl Pts',(1.72245534586321,-0.123606275893366,
-5.55111512312578E-17));
#97203=CARTESIAN_POINT('Ctrl Pts',(1.71065390208195,-0.184401836184713,
3.16625666268892E-17));
#97204=CARTESIAN_POINT('Ctrl Pts',(1.69540107690307,-0.244666544752314,
-5.10914177950054E-16));
#97205=CARTESIAN_POINT('Ctrl Pts',(1.67680493801022,-0.304129401844208,
-5.82867087928207E-16));
#97206=CARTESIAN_POINT('Ctrl Pts',(1.67349552259788,-0.314711560692091,
-5.95672007842828E-16));
#97207=CARTESIAN_POINT('Ctrl Pts',(1.67008173945308,-0.325263020743978,
-2.82234476894323E-16));
#97208=CARTESIAN_POINT('Ctrl Pts',(1.66656691458475,-0.335775244456298,
-2.77555756156289E-16));
#97209=CARTESIAN_POINT('Ctrl Pts',(1.64601434320315,-0.39724437487395,-2.5019742521657E-16));
#97210=CARTESIAN_POINT('Ctrl Pts',(1.6219871213203,-0.457449913435399,-1.49651752513019E-16));
#97211=CARTESIAN_POINT('Ctrl Pts',(1.59467186427628,-0.5161179062652,-1.94289029309402E-16));
#97212=CARTESIAN_POINT('Ctrl Pts',(1.56746479951959,-0.57455352257637,-2.38749503483388E-16));
#97213=CARTESIAN_POINT('Ctrl Pts',(1.53699493854014,-0.631464584970275,
-4.11608014004163E-16));
#97214=CARTESIAN_POINT('Ctrl Pts',(1.50340708769257,-0.686547887629179,
-4.71844785465692E-16));
#97215=CARTESIAN_POINT('Ctrl Pts',(1.47050686756616,-0.740503491725204,
-5.30848353445754E-16));
#97216=CARTESIAN_POINT('Ctrl Pts',(1.43461427022078,-0.792706028859038,
8.26037042042841E-17));
#97217=CARTESIAN_POINT('Ctrl Pts',(1.39583852741916,-0.842828743497358,
1.94289029309402E-16));
#97218=CARTESIAN_POINT('Ctrl Pts',(1.38891448399703,-0.851778974428235,
2.14232271779286E-16));
#97219=CARTESIAN_POINT('Ctrl Pts',(1.38189845475662,-0.860662765012678,
1.05754276149716E-16));
#97220=CARTESIAN_POINT('Ctrl Pts',(1.3747909965488,-0.869478087839508,1.11022302462516E-16));
#97221=CARTESIAN_POINT('Ctrl Pts',(1.36801000346398,-0.877888498619479,
1.1604835382339E-16));
#97222=CARTESIAN_POINT('Ctrl Pts',(1.36114891147745,-0.8862326313589,4.78426519390645E-16));
#97223=CARTESIAN_POINT('Ctrl Pts',(1.35421355798306,-0.894502968665375,
4.71844785465692E-16));
#97224=CARTESIAN_POINT('Ctrl Pts',(1.3143417576089,-0.942049678199007,4.34005967100638E-16));
#97225=CARTESIAN_POINT('Ctrl Pts',(1.27196760499602,-0.987223303029092,
-4.84873724376989E-16));
#97226=CARTESIAN_POINT('Ctrl Pts',(1.22722986402911,-1.02975664627632,-3.05311331771918E-16));
#97227=CARTESIAN_POINT('Ctrl Pts',(1.18329662429212,-1.07152512911229,-1.2897793916942E-16));
#97228=CARTESIAN_POINT('Ctrl Pts',(1.13708333146208,-1.1107479710078,1.42267300457324E-16));
#97229=CARTESIAN_POINT('Ctrl Pts',(1.08869802628341,-1.14712822354107,1.94289029309402E-16));
#97230=CARTESIAN_POINT('Ctrl Pts',(1.04185702701945,-1.1823473334721,2.44650389103912E-16));
#97231=CARTESIAN_POINT('Ctrl Pts',(0.99297984330778,-1.21490270865201,1.66616011326585E-16));
#97232=CARTESIAN_POINT('Ctrl Pts',(0.942151955941521,-1.24447758118399,
1.11022302462516E-16));
#97233=CARTESIAN_POINT('Ctrl Pts',(0.929425469464971,-1.25188265416315,
9.71025308430195E-17));
#97234=CARTESIAN_POINT('Ctrl Pts',(0.916576650468056,-1.25910062269163,
1.9641793555709E-16));
#97235=CARTESIAN_POINT('Ctrl Pts',(0.903606778650242,-1.26612599672281,
1.94289029309402E-16));
#97236=CARTESIAN_POINT('Ctrl Pts',(1.88079991776263,-0.516378774142081,
11.046));
#97237=CARTESIAN_POINT('Ctrl Pts',(1.79754570390634,-0.821182550519846,
11.028067538919));
#97238=CARTESIAN_POINT('Ctrl Pts',(1.64446793279769,-1.10682480125595,11.010135077838));
#97239=CARTESIAN_POINT('Ctrl Pts',(1.43091597726206,-1.33587557506818,10.9922026167571));
#97240=CARTESIAN_POINT('Ctrl Pts',(0.9898515831668,-1.80895080641009,10.9551653999286));
#97241=CARTESIAN_POINT('Ctrl Pts',(0.290818548970629,-2.04062011418838,
10.9181281831001));
#97242=CARTESIAN_POINT('Ctrl Pts',(-0.345744266721549,-1.9262440956347,
10.8810909662716));
#97243=CARTESIAN_POINT('Ctrl Pts',(-0.982307082413709,-1.81186807708102,
10.8440537494431));
#97244=CARTESIAN_POINT('Ctrl Pts',(-1.55639967960188,-1.35144673219537,
10.8070165326147));
#97245=CARTESIAN_POINT('Ctrl Pts',(-1.80573868997825,-0.754924386616321,
10.7699793157862));
#97246=CARTESIAN_POINT('Ctrl Pts',(-1.90472245868201,-0.518114150655666,
10.7552761078989));
#97247=CARTESIAN_POINT('Ctrl Pts',(-1.95252608806662,-0.259854826956367,
10.7405729000116));
#97248=CARTESIAN_POINT('Ctrl Pts',(-1.95129684289216,-0.00113636086278679,
10.7258696921242));
#97249=CARTESIAN_POINT('Origin',(0.,0.,-1.29405622560369));
#97250=CARTESIAN_POINT('',(-0.903606778650172,-1.26612599672286,0.));
#97251=CARTESIAN_POINT('Ctrl Pts',(-0.905549614304886,-1.26792015305981,
1.24276674021151E-15));
#97252=CARTESIAN_POINT('Ctrl Pts',(-0.513706458239086,-1.54472437079514,
0.0344950590738082));
#97253=CARTESIAN_POINT('Ctrl Pts',(0.587535178885047,-1.72169358136003,
0.106052258091336));
#97254=CARTESIAN_POINT('Ctrl Pts',(1.77508460417327,-0.479721809770191,
0.214671597052585));
#97255=CARTESIAN_POINT('Ctrl Pts',(1.3650560094313,1.23222299189869,0.325858016883748));
#97256=CARTESIAN_POINT('Ctrl Pts',(-0.295638381403906,1.81478253869214,
0.43704443671491));
#97257=CARTESIAN_POINT('Ctrl Pts',(-1.41307745535963,0.946781319192958,
0.526443839621562));
#97258=CARTESIAN_POINT('Ctrl Pts',(-1.55414936746312,0.214718667413076,
0.578781102584494));
#97259=CARTESIAN_POINT('Ctrl Pts',(-1.55326046963413,0.000729270061605551,
0.594056225603705));
#97260=CARTESIAN_POINT('Origin',(0.,0.,0.));
#97261=CARTESIAN_POINT('Ctrl Pts',(-0.685825729128748,1.39614588036674,
-0.230074082272066));
#97262=CARTESIAN_POINT('Ctrl Pts',(-1.15028016933624,1.16799292759742,-0.193011942328345));
#97263=CARTESIAN_POINT('Ctrl Pts',(-1.82555218707277,0.215691441263552,
-0.118887662440903));
#97264=CARTESIAN_POINT('Ctrl Pts',(-1.16942936218886,-1.42059634545264,
-0.00770124260974049));
#97265=CARTESIAN_POINT('Ctrl Pts',(0.559468948314244,-1.75104601534012,
0.103485177221422));
#97266=CARTESIAN_POINT('Ctrl Pts',(1.77508460417327,-0.479721809770191,
0.214671597052585));
#97267=CARTESIAN_POINT('Ctrl Pts',(1.3650560094313,1.23222299189869,0.325858016883748));
#97268=CARTESIAN_POINT('Ctrl Pts',(-0.295638381403906,1.81478253869214,
0.43704443671491));
#97269=CARTESIAN_POINT('Ctrl Pts',(-1.68540213790592,0.735245708832444,
0.548230856546073));
#97270=CARTESIAN_POINT('Ctrl Pts',(-1.53132379752993,-1.01797781965797,
0.659417276377235));
#97271=CARTESIAN_POINT('Ctrl Pts',(0.0255447675030308,-1.83860034663711,
0.770603696208398));
#97272=CARTESIAN_POINT('Ctrl Pts',(1.55899683301632,-0.975032021788082,
0.881790116039561));
#97273=CARTESIAN_POINT('Ctrl Pts',(1.66434877052597,0.781732535368643,0.992976535870723));
#97274=CARTESIAN_POINT('Ctrl Pts',(0.245080507541896,1.82238325373942,1.10416295570189));
#97275=CARTESIAN_POINT('Ctrl Pts',(-1.39868975820189,1.19365863723167,1.21534937553305));
#97276=CARTESIAN_POINT('Ctrl Pts',(-1.76120077222934,-0.528512641939849,
1.32653579536421));
#97277=CARTESIAN_POINT('Ctrl Pts',(-0.510374815939226,-1.76654153931159,
1.43772221519537));
#97278=CARTESIAN_POINT('Ctrl Pts',(1.20797626960931,-1.38634273102519,1.54890863502654));
#97279=CARTESIAN_POINT('Ctrl Pts',(1.81976886629041,0.263806680570579,1.6600950548577));
#97280=CARTESIAN_POINT('Ctrl Pts',(0.764574137846417,1.67229745635935,1.77128147468886));
#97281=CARTESIAN_POINT('Ctrl Pts',(-0.991003621173195,1.54889135395602,
1.88246789452002));
#97282=CARTESIAN_POINT('Ctrl Pts',(-1.83877909581896,0.00663349951290586,
1.99365431435119));
#97283=CARTESIAN_POINT('Ctrl Pts',(-1.00215313155719,-1.54170088892816,
2.10484073418235));
#97284=CARTESIAN_POINT('Ctrl Pts',(0.752488571272716,-1.67777039880966,
2.21602715401351));
#97285=CARTESIAN_POINT('Ctrl Pts',(1.81781810074028,-0.276929424335053,
2.32721357384467));
#97286=CARTESIAN_POINT('Ctrl Pts',(1.21794738393109,1.37759091140133,2.43839999367584));
#97287=CARTESIAN_POINT('Ctrl Pts',(-0.497615974795104,1.77017821004958,
2.549586413507));
#97288=CARTESIAN_POINT('Ctrl Pts',(-1.75734151264734,0.541205469518692,
2.66077283333817));
#97289=CARTESIAN_POINT('Ctrl Pts',(-1.40726598433086,-1.1835349598584,2.77195925316932));
#97290=CARTESIAN_POINT('Ctrl Pts',(0.231926238140432,-1.82410602009977,
2.88314567300049));
#97291=CARTESIAN_POINT('Ctrl Pts',(1.65866396469461,-0.793716828903688,
2.99433209283165));
#97292=CARTESIAN_POINT('Ctrl Pts',(1.56599354026699,0.96375141196464,3.10551851266282));
#97293=CARTESIAN_POINT('Ctrl Pts',(0.0388050940998321,1.83838154825996,
3.21670493249398));
#97294=CARTESIAN_POINT('Ctrl Pts',(-1.52393050178991,1.02897443019027,3.32789135232514));
#97295=CARTESIAN_POINT('Ctrl Pts',(-1.69067964401488,-0.723017906820314,
3.4390777721563));
#97296=CARTESIAN_POINT('Ctrl Pts',(-0.308692884081366,-1.81269447386996,
3.55026419198746));
#97297=CARTESIAN_POINT('Ctrl Pts',(1.35606994996762,-1.24186426112907,3.66145061181863));
#97298=CARTESIAN_POINT('Ctrl Pts',(1.77861387826841,0.466567491694538,3.77263703164979));
#97299=CARTESIAN_POINT('Ctrl Pts',(0.571870330903418,1.74760318061885,3.88382345148095));
#97300=CARTESIAN_POINT('Ctrl Pts',(-1.15873124952358,1.42775853828764,3.99500987131212));
#97301=CARTESIAN_POINT('Ctrl Pts',(-1.82788473512851,-0.199974866820836,
4.10619629114327));
#97302=CARTESIAN_POINT('Ctrl Pts',(-0.822616502622442,-1.64452261823584,
4.21738271097444));
#97303=CARTESIAN_POINT('Ctrl Pts',(0.936204134582059,-1.58261630557358,
4.3285691308056));
#97304=CARTESIAN_POINT('Ctrl Pts',(1.83742116834086,-0.0709647969689106,
4.43975555063676));
#97305=CARTESIAN_POINT('Ctrl Pts',(1.0554806974386,1.50569354438759,4.55094197046793));
#97306=CARTESIAN_POINT('Ctrl Pts',(-0.693325883166112,1.70307127625589,
4.66212839029909));
#97307=CARTESIAN_POINT('Ctrl Pts',(-1.80701587562324,0.340361833232659,
4.77331481013025));
#97308=CARTESIAN_POINT('Ctrl Pts',(-1.26540093064824,-1.33413381524886,
4.88450122996142));
#97309=CARTESIAN_POINT('Ctrl Pts',(0.435376164803608,-1.7865050090601,4.99568764979258));
#97310=CARTESIAN_POINT('Ctrl Pts',(1.73732980498774,-0.602360109052031,
5.10687406962374));
#97311=CARTESIAN_POINT('Ctrl Pts',(1.44781397169404,1.13357278356683,5.21806048945491));
#97312=CARTESIAN_POINT('Ctrl Pts',(-0.167962271460079,1.83110382765203,
5.32924690928607));
#97313=CARTESIAN_POINT('Ctrl Pts',(-1.62987778710162,0.851264325217889,
5.44043332911723));
#97314=CARTESIAN_POINT('Ctrl Pts',(-1.59875453933454,-0.908370230265797,
5.55161974894839));
#97315=CARTESIAN_POINT('Ctrl Pts',(-0.103102773360761,-1.83589824620028,
5.66280616877956));
#97316=CARTESIAN_POINT('Ctrl Pts',(1.4869956060099,-1.08166382022474,5.77399258861071));
#97317=CARTESIAN_POINT('Ctrl Pts',(1.71494149863546,0.663421591850831,5.88517900844189));
#97318=CARTESIAN_POINT('Ctrl Pts',(0.371926577693494,1.80078404398782,5.99636542827304));
#97319=CARTESIAN_POINT('Ctrl Pts',(-1.311789224034,1.28855018683177,6.10755184810421));
#97320=CARTESIAN_POINT('Ctrl Pts',(-1.79384918603911,-0.404051543769803,
6.21873826793537));
#97321=CARTESIAN_POINT('Ctrl Pts',(-0.632665469493242,-1.72652453095426,
6.32992468776653));
#97322=CARTESIAN_POINT('Ctrl Pts',(1.10806726459172,-1.46742614445027,6.44111110759769));
#97323=CARTESIAN_POINT('Ctrl Pts',(1.83376231205259,0.135898253011021,6.55229752742886));
#97324=CARTESIAN_POINT('Ctrl Pts',(0.879651525947856,1.61473395492061,6.66348394726001));
#97325=CARTESIAN_POINT('Ctrl Pts',(-0.880258220622017,1.61440330069759,
6.77467036709119));
#97326=CARTESIAN_POINT('Ctrl Pts',(-1.83381324808445,0.13520918395534,6.88585678692234));
#97327=CARTESIAN_POINT('Ctrl Pts',(-1.1075157823663,-1.46784241118916,6.99704320675351));
#97328=CARTESIAN_POINT('Ctrl Pts',(0.633314188332071,-1.72628667698419,
7.10822962658467));
#97329=CARTESIAN_POINT('Ctrl Pts',(1.7940008868909,-0.403377453646542,7.21941604641583));
#97330=CARTESIAN_POINT('Ctrl Pts',(1.31130494233742,1.28904301731096,7.33060246624699));
#97331=CARTESIAN_POINT('Ctrl Pts',(-0.372603218894873,1.80064416072257,
7.44178888607816));
#97332=CARTESIAN_POINT('Ctrl Pts',(-1.71519066664489,0.662777133981789,
7.55297530590932));
#97333=CARTESIAN_POINT('Ctrl Pts',(-1.48658905212271,-1.08222250133236,
7.66416172574049));
#97334=CARTESIAN_POINT('Ctrl Pts',(0.103792628149562,-1.8358593744105,7.77534814557165));
#97335=CARTESIAN_POINT('Ctrl Pts',(1.59909575810308,-0.907769413831382,
7.8865345654028));
#97336=CARTESIAN_POINT('Ctrl Pts',(1.62955779866738,0.851876712390422,7.99772098523398));
#97337=CARTESIAN_POINT('Ctrl Pts',(0.167274199086701,1.83116681231986,8.10890740506512));
#97338=CARTESIAN_POINT('Ctrl Pts',(-1.44823982381472,1.1330286690894,8.2200938248963));
#97339=CARTESIAN_POINT('Ctrl Pts',(-1.73710333792674,-0.603012890298399,
8.33128024472746));
#97340=CARTESIAN_POINT('Ctrl Pts',(-0.434704832044991,-1.78666848096071,
8.44246666455862));
#97341=CARTESIAN_POINT('Ctrl Pts',(1.26590215885116,-1.33365823077974,8.55365308438979));
#97342=CARTESIAN_POINT('Ctrl Pts',(1.8068878531032,0.341040818691465,8.66483950422094));
#97343=CARTESIAN_POINT('Ctrl Pts',(0.69268588294083,1.70333168137465,8.77602592405212));
#97344=CARTESIAN_POINT('Ctrl Pts',(-1.05604640517969,1.5052968290502,8.88721234388326));
#97345=CARTESIAN_POINT('Ctrl Pts',(-1.83739437498563,-0.0716552286239433,
8.99839876371444));
#97346=CARTESIAN_POINT('Ctrl Pts',(-0.935609375970031,-1.5829679799695,
9.1095851835456));
#97347=CARTESIAN_POINT('Ctrl Pts',(0.823234386500799,-1.64421340203127,
9.22077160337675));
#97348=CARTESIAN_POINT('Ctrl Pts',(1.82795976495949,-0.199287985657338,
9.33195802320793));
#97349=CARTESIAN_POINT('Ctrl Pts',(1.15819463928053,1.42819381470141,9.44314444303908));
#97350=CARTESIAN_POINT('Ctrl Pts',(-0.572526917402423,1.74738822826618,
9.55433086287024));
#97351=CARTESIAN_POINT('Ctrl Pts',(-1.77878918025408,0.46589901053406,9.66551728270142));
#97352=CARTESIAN_POINT('Ctrl Pts',(-1.35560300066214,-1.24237352171324,
9.77670370253256));
#97353=CARTESIAN_POINT('Ctrl Pts',(0.309373610575528,-1.81257875466721,
9.88789012236375));
#97354=CARTESIAN_POINT('Ctrl Pts',(1.69095195914933,-0.722381792257861,
9.99907654219489));
#97355=CARTESIAN_POINT('Ctrl Pts',(1.52354231364944,1.0295455294481,10.1102629620261));
#97356=CARTESIAN_POINT('Ctrl Pts',(-0.0394931635484403,1.83836962465064,
10.2214493818572));
#97357=CARTESIAN_POINT('Ctrl Pts',(-1.56636075542215,0.963157594965877,
10.3326358016884));
#97358=CARTESIAN_POINT('Ctrl Pts',(-1.65835572967195,-0.794329933758677,
10.4438222215196));
#97359=CARTESIAN_POINT('Ctrl Pts',(-0.231259578302998,-1.82421227428175,
10.5550086413507));
#97360=CARTESIAN_POINT('Ctrl Pts',(1.40774638007895,-1.1829694620695,10.6661950611819));
#97361=CARTESIAN_POINT('Ctrl Pts',(1.75706993010233,0.541796064983141,10.7773814810131));
#97362=CARTESIAN_POINT('Ctrl Pts',(0.497080432048737,1.77049779856472,10.8885679008442));
#97363=CARTESIAN_POINT('Ctrl Pts',(-1.21871201614337,1.37688031013954,10.9997543206754));
#97364=CARTESIAN_POINT('Ctrl Pts',(-1.81724153253684,-0.27712968875509,
11.1109407405065));
#97365=CARTESIAN_POINT('Ctrl Pts',(-0.75277483453787,-1.67898453189698,
11.2221271603377));
#97366=CARTESIAN_POINT('Ctrl Pts',(1.00462758039806,-1.53944373403644,11.3333135801688));
#97367=CARTESIAN_POINT('Ctrl Pts',(1.55754888396286,-0.511266487217653,
11.4074378600563));
#97368=CARTESIAN_POINT('Ctrl Pts',(1.55548765964692,0.00619602180124784,
11.4445));
#97369=CARTESIAN_POINT('Ctrl Pts',(-0.74439243930934,1.51537102412034,-0.153382721514711));
#97370=CARTESIAN_POINT('Ctrl Pts',(-1.24850938769699,1.26773474301532,-0.11632058157099));
#97371=CARTESIAN_POINT('Ctrl Pts',(-1.98144687185762,0.234110607521693,
-0.042196301683548));
#97372=CARTESIAN_POINT('Ctrl Pts',(-1.26929384324154,-1.54190945884872,
0.0689901181476148));
#97373=CARTESIAN_POINT('Ctrl Pts',(0.607245306591998,-1.90057817801302,
0.180176537978778));
#97374=CARTESIAN_POINT('Ctrl Pts',(1.92666956394248,-0.520688088821623,
0.29136295780994));
#97375=CARTESIAN_POINT('Ctrl Pts',(1.48162620545796,1.33744979191402,0.402549377641103));
#97376=CARTESIAN_POINT('Ctrl Pts',(-0.320884689126903,1.9697575395855,0.513735797472264));
#97377=CARTESIAN_POINT('Ctrl Pts',(-1.82932858212653,0.798032683003624,
0.624922217303428));
#97378=CARTESIAN_POINT('Ctrl Pts',(-1.66209258212561,-1.10490895887015,
0.736108637134591));
#97379=CARTESIAN_POINT('Ctrl Pts',(0.0277261860929502,-1.99560929084259,
0.847295056965753));
#97380=CARTESIAN_POINT('Ctrl Pts',(1.69212878157669,-1.0582957656395,0.958481476796916));
#97381=CARTESIAN_POINT('Ctrl Pts',(1.80647734334385,0.848489294255244,1.06966789662808));
#97382=CARTESIAN_POINT('Ctrl Pts',(0.266009379770665,1.97800732458805,1.18085431645924));
#97383=CARTESIAN_POINT('Ctrl Pts',(-1.51813213871049,1.2955921992025,1.29204073629041));
#97384=CARTESIAN_POINT('Ctrl Pts',(-1.91160010957712,-0.573645458357494,
1.40322715612156));
#97385=CARTESIAN_POINT('Ctrl Pts',(-0.553958736254638,-1.91739695630841,
1.51441357595273));
#97386=CARTESIAN_POINT('Ctrl Pts',(1.31113249878304,-1.50473072594935,1.62559999578389));
#97387=CARTESIAN_POINT('Ctrl Pts',(1.9751696791516,0.286334691329668,1.73678641561505));
#97388=CARTESIAN_POINT('Ctrl Pts',(0.829865639814035,1.81510481441338,1.84797283544622));
#97389=CARTESIAN_POINT('Ctrl Pts',(-1.07563127424026,1.68116033596642,1.95915925527738));
#97390=CARTESIAN_POINT('Ctrl Pts',(-1.99580330447296,0.00719997322039096,
2.07034567510854));
#97391=CARTESIAN_POINT('Ctrl Pts',(-1.08773290717609,-1.67335583465575,
2.18153209493971));
#97392=CARTESIAN_POINT('Ctrl Pts',(0.816748015321165,-1.82104512374819,
2.29271851477087));
#97393=CARTESIAN_POINT('Ctrl Pts',(1.97305232620797,-0.300578063700233,
2.40390493460203));
#97394=CARTESIAN_POINT('Ctrl Pts',(1.32195510545613,1.49523153675082,2.51509135443319));
#97395=CARTESIAN_POINT('Ctrl Pts',(-0.54011034229875,1.92134418384253,2.62627777426435));
#97396=CARTESIAN_POINT('Ctrl Pts',(-1.90741128502276,0.587422201459822,
2.73746419409552));
#97397=CARTESIAN_POINT('Ctrl Pts',(-1.52744073944838,-1.28460400121777,
2.84865061392668));
#97398=CARTESIAN_POINT('Ctrl Pts',(0.251731789602741,-1.9798772081443,2.95983703375785));
#97399=CARTESIAN_POINT('Ctrl Pts',(1.80030707836241,-0.861496997406464,
3.071023453589));
#97400=CARTESIAN_POINT('Ctrl Pts',(1.69972297898904,1.04605183790867,3.18220987342017));
#97401=CARTESIAN_POINT('Ctrl Pts',(0.0421188903066005,1.99537180797957,
3.29339629325133));
#97402=CARTESIAN_POINT('Ctrl Pts',(-1.65406792919015,1.11684463493277,3.4045827130825));
#97403=CARTESIAN_POINT('Ctrl Pts',(-1.83505676565636,-0.784760676748056,
3.51576913291366));
#97404=CARTESIAN_POINT('Ctrl Pts',(-0.335053992900935,-1.96749116257395,
3.62695555274482));
#97405=CARTESIAN_POINT('Ctrl Pts',(1.47187277329603,-1.34791438607496,3.73814197257599));
#97406=CARTESIAN_POINT('Ctrl Pts',(1.93050022360002,0.506410445822938,3.84932839240714));
#97407=CARTESIAN_POINT('Ctrl Pts',(0.620705716495424,1.89684133929807,3.96051481223831));
#97408=CARTESIAN_POINT('Ctrl Pts',(-1.25768215554202,1.54968327363698,4.07170123206947));
#97409=CARTESIAN_POINT('Ctrl Pts',(-1.9839786099702,-0.217051901949521,
4.18288765190064));
#97410=CARTESIAN_POINT('Ctrl Pts',(-0.892864584974339,-1.78495811879663,
4.29407407173179));
#97411=CARTESIAN_POINT('Ctrl Pts',(1.01615213578872,-1.71776526041577,4.40526049156296));
#97412=CARTESIAN_POINT('Ctrl Pts',(1.99432941554622,-0.0770249001709277,
4.51644691139412));
#97413=CARTESIAN_POINT('Ctrl Pts',(1.14561442891388,1.6342736102696,4.62763333122529));
#97414=CARTESIAN_POINT('Ctrl Pts',(-0.752533075803338,1.84850659257176,
4.73881975105645));
#97415=CARTESIAN_POINT('Ctrl Pts',(-1.96132763527948,0.369427340688636,
4.85000617088761));
#97416=CARTESIAN_POINT('Ctrl Pts',(-1.3734609908354,-1.44806338245697,4.96119259071877));
#97417=CARTESIAN_POINT('Ctrl Pts',(0.472555507281729,-1.9390652246629,5.07237901054994));
#97418=CARTESIAN_POINT('Ctrl Pts',(1.88569065943703,-0.653799196903168,
5.1835654303811));
#97419=CARTESIAN_POINT('Ctrl Pts',(1.57145135896933,1.23037525956625,5.29475185021226));
#97420=CARTESIAN_POINT('Ctrl Pts',(-0.182305561972616,1.98747259981946,
5.40593827004342));
#97421=CARTESIAN_POINT('Ctrl Pts',(-1.76906267902489,0.923958814363803,
5.51712468987459));
#97422=CARTESIAN_POINT('Ctrl Pts',(-1.73528163328608,-0.985941329968107,
5.62831110970574));
#97423=CARTESIAN_POINT('Ctrl Pts',(-0.111907328205795,-1.99267644208816,
5.73949752953692));
#97424=CARTESIAN_POINT('Ctrl Pts',(1.61397894448518,-1.17403348321834,5.85068394936807));
#97425=CARTESIAN_POINT('Ctrl Pts',(1.86139048335769,0.720075080408093,5.96187036919923));
#97426=CARTESIAN_POINT('Ctrl Pts',(0.403687585131819,1.9545636307293,6.0730567890304));
#97427=CARTESIAN_POINT('Ctrl Pts',(-1.42381065460884,1.39858709874703,6.18424320886156));
#97428=CARTESIAN_POINT('Ctrl Pts',(-1.94703656429618,-0.438555891823412,
6.29542962869273));
#97429=CARTESIAN_POINT('Ctrl Pts',(-0.686692511086116,-1.87396265922711,
6.40661604852388));
#97430=CARTESIAN_POINT('Ctrl Pts',(1.20269167366484,-1.59273833100625,6.51780246835505));
#97431=CARTESIAN_POINT('Ctrl Pts',(1.99035810790665,0.147503407586138,6.62898888818621));
#97432=CARTESIAN_POINT('Ctrl Pts',(0.954770165847204,1.75262562555938,6.74017530801738));
#97433=CARTESIAN_POINT('Ctrl Pts',(-0.9554286697633,1.7522667348191,6.85136172784854));
#97434=CARTESIAN_POINT('Ctrl Pts',(-1.99041339366714,0.146755494853507,
6.9625481476797));
#97435=CARTESIAN_POINT('Ctrl Pts',(-1.20209309711463,-1.59319014522084,
7.07373456751086));
#97436=CARTESIAN_POINT('Ctrl Pts',(0.687396627858533,-1.87370449350154,
7.18492098734203));
#97437=CARTESIAN_POINT('Ctrl Pts',(1.94720121977979,-0.437824237162718,
7.29610740717318));
#97438=CARTESIAN_POINT('Ctrl Pts',(1.42328501723757,1.39912201493195,7.40729382700435));
#97439=CARTESIAN_POINT('Ctrl Pts',(-0.404422008722263,1.95441180200575,
7.51848024683551));
#97440=CARTESIAN_POINT('Ctrl Pts',(-1.86166092929526,0.719375588474842,
7.62966666666667));
#97441=CARTESIAN_POINT('Ctrl Pts',(-1.61353767256008,-1.17463987340584,
7.74085308649784));
#97442=CARTESIAN_POINT('Ctrl Pts',(0.112656093769942,-1.99263425080664,
7.852039506329));
#97443=CARTESIAN_POINT('Ctrl Pts',(1.73565199074082,-0.985289206269375,
7.96322592616017));
#97444=CARTESIAN_POINT('Ctrl Pts',(1.76871536488809,0.924623496894334,8.07441234599133));
#97445=CARTESIAN_POINT('Ctrl Pts',(0.181558731034875,1.98754096312013,8.18559876582249));
#97446=CARTESIAN_POINT('Ctrl Pts',(-1.57191357711808,1.22978467993954,8.29678518565365));
#97447=CARTESIAN_POINT('Ctrl Pts',(-1.88544485301595,-0.6545077229961,8.40797160548482));
#97448=CARTESIAN_POINT('Ctrl Pts',(-0.471826845453332,-1.93924265639472,
8.51915802531597));
#97449=CARTESIAN_POINT('Ctrl Pts',(1.37400502187529,-1.44754718502077,8.63034444514714));
#97450=CARTESIAN_POINT('Ctrl Pts',(1.96118868016023,0.370164308726493,8.7415308649783));
#97451=CARTESIAN_POINT('Ctrl Pts',(0.751838422178375,1.84878923522181,8.85271728480947));
#97452=CARTESIAN_POINT('Ctrl Pts',(-1.14622844578058,1.63384301706618,8.96390370464062));
#97453=CARTESIAN_POINT('Ctrl Pts',(-1.99430033414812,-0.077774291863319,
9.0750901244718));
#97454=CARTESIAN_POINT('Ctrl Pts',(-1.01550658722561,-1.71814696636568,
9.18627654430294));
#97455=CARTESIAN_POINT('Ctrl Pts',(0.893535233606871,-1.78462249679383,
9.29746296413412));
#97456=CARTESIAN_POINT('Ctrl Pts',(1.98406004704164,-0.216306363946107,
9.40864938396527));
#97457=CARTESIAN_POINT('Ctrl Pts',(1.2570997209806,1.55015572087487,9.51983580379645));
#97458=CARTESIAN_POINT('Ctrl Pts',(-0.621418372793996,1.8966080308943,9.63102222362759));
#97459=CARTESIAN_POINT('Ctrl Pts',(-1.93069049565776,0.50568487910749,9.74220864345877));
#97460=CARTESIAN_POINT('Ctrl Pts',(-1.47136594843111,-1.34846713542859,
9.85339506328992));
#97461=CARTESIAN_POINT('Ctrl Pts',(0.335792850651442,-1.96736556142493,
9.9645814831211));
#97462=CARTESIAN_POINT('Ctrl Pts',(1.83535233538869,-0.784070240605622,
10.0757679029522));
#97463=CARTESIAN_POINT('Ctrl Pts',(1.65364659137136,1.11746450372967,10.1869543227834));
#97464=CARTESIAN_POINT('Ctrl Pts',(-0.0428657180698079,1.99535886614283,
10.2981407426146));
#97465=CARTESIAN_POINT('Ctrl Pts',(-1.70012155281541,1.04540731136874,10.4093271624457));
#97466=CARTESIAN_POINT('Ctrl Pts',(-1.79997252133044,-0.862162458906591,
10.5205135822769));
#97467=CARTESIAN_POINT('Ctrl Pts',(-0.251008199743871,-1.97999253599851,
10.6317000021081));
#97468=CARTESIAN_POINT('Ctrl Pts',(1.52796215902707,-1.28399021223231,10.7428864219392));
#97469=CARTESIAN_POINT('Ctrl Pts',(1.90711651044001,0.588063231359589,10.8540728417704));
#97470=CARTESIAN_POINT('Ctrl Pts',(0.539529066393858,1.92169106390877,10.9652592616015));
#97471=CARTESIAN_POINT('Ctrl Pts',(-1.32278503412967,1.49446025304978,11.0764456814327));
#97472=CARTESIAN_POINT('Ctrl Pts',(-1.97242652143987,-0.300795429882017,
11.1876321012639));
#97473=CARTESIAN_POINT('Ctrl Pts',(-0.817058724297523,-1.82236293883171,
11.2988185210951));
#97474=CARTESIAN_POINT('Ctrl Pts',(1.09041866382002,-1.67090592797485,11.4100049409262));
#97475=CARTESIAN_POINT('Ctrl Pts',(1.69055718360052,-0.554926552610627,
11.4841292208136));
#97476=CARTESIAN_POINT('Ctrl Pts',(1.6883199391646,0.00672513670271936,
11.5211913607574));
#97477=CARTESIAN_POINT('Ctrl Pts',(-0.802959149489932,1.63459616787394,
-0.0766913607573554));
#97478=CARTESIAN_POINT('Ctrl Pts',(-1.34673860605774,1.36747655843322,-0.0396292208136346));
#97479=CARTESIAN_POINT('Ctrl Pts',(-2.13734155664247,0.252529773779836,
0.0344950590738073));
#97480=CARTESIAN_POINT('Ctrl Pts',(-1.36915832429422,-1.66322257224481,
0.14568147890497));
#97481=CARTESIAN_POINT('Ctrl Pts',(0.655021664869751,-2.05011034068591,
0.256867898736133));
#97482=CARTESIAN_POINT('Ctrl Pts',(2.0782545237117,-0.561654367873057,0.368054318567295));
#97483=CARTESIAN_POINT('Ctrl Pts',(1.59819640148463,1.44267659192936,0.479240738398458));
#97484=CARTESIAN_POINT('Ctrl Pts',(-0.346130996849898,2.12473254047885,
0.590427158229621));
#97485=CARTESIAN_POINT('Ctrl Pts',(-1.97325502634714,0.860819657174806,
0.701613578060782));
#97486=CARTESIAN_POINT('Ctrl Pts',(-1.79286136672128,-1.19184009808233,
0.812799997891947));
#97487=CARTESIAN_POINT('Ctrl Pts',(0.0299076046828686,-2.15261823504807,
0.923986417723108));
#97488=CARTESIAN_POINT('Ctrl Pts',(1.82526073013706,-1.14155950949091,1.03517283755427));
#97489=CARTESIAN_POINT('Ctrl Pts',(1.94860591616173,0.915246053141843,1.14635925738543));
#97490=CARTESIAN_POINT('Ctrl Pts',(0.286938251999433,2.13363139543668,1.2575456772166));
#97491=CARTESIAN_POINT('Ctrl Pts',(-1.63757451921909,1.39752576117334,1.36873209704776));
#97492=CARTESIAN_POINT('Ctrl Pts',(-2.0619994469249,-0.618778274775138,
1.47991851687892));
#97493=CARTESIAN_POINT('Ctrl Pts',(-0.597542656570052,-2.06825237330522,
1.59110493671008));
#97494=CARTESIAN_POINT('Ctrl Pts',(1.41428872795678,-1.62311872087351,1.70229135654125));
#97495=CARTESIAN_POINT('Ctrl Pts',(2.13057049201279,0.308862702088754,1.81347777637241));
#97496=CARTESIAN_POINT('Ctrl Pts',(0.895157141781652,1.95791217246742,1.92466419620357));
#97497=CARTESIAN_POINT('Ctrl Pts',(-1.16025892730732,1.81342931797682,2.03585061603473));
#97498=CARTESIAN_POINT('Ctrl Pts',(-2.15282751312695,0.00776644692787891,
2.1470370358659));
#97499=CARTESIAN_POINT('Ctrl Pts',(-1.173312682795,-1.80501078038335,2.25822345569706));
#97500=CARTESIAN_POINT('Ctrl Pts',(0.881007459369614,-1.96431984868673,
2.36940987552822));
#97501=CARTESIAN_POINT('Ctrl Pts',(2.12828655167567,-0.324226703065412,
2.48059629535939));
#97502=CARTESIAN_POINT('Ctrl Pts',(1.42596282698117,1.6128721621003,2.59178271519055));
#97503=CARTESIAN_POINT('Ctrl Pts',(-0.582604709802392,2.07251015763547,
2.70296913502171));
#97504=CARTESIAN_POINT('Ctrl Pts',(-2.05748105739819,0.633638933400953,
2.81415555485287));
#97505=CARTESIAN_POINT('Ctrl Pts',(-1.6476154945659,-1.38567304257714,2.92534197468403));
#97506=CARTESIAN_POINT('Ctrl Pts',(0.271537341065049,-2.13564839618882,
3.0365283945152));
#97507=CARTESIAN_POINT('Ctrl Pts',(1.9419501920302,-0.92927716590924,3.14771481434636));
#97508=CARTESIAN_POINT('Ctrl Pts',(1.83345241771109,1.12835226385271,3.25890123417753));
#97509=CARTESIAN_POINT('Ctrl Pts',(0.045432686513366,2.15236206769919,3.37008765400868));
#97510=CARTESIAN_POINT('Ctrl Pts',(-1.78420535659039,1.20471483967528,3.48127407383985));
#97511=CARTESIAN_POINT('Ctrl Pts',(-1.97943388729784,-0.8465034466758,3.59246049367101));
#97512=CARTESIAN_POINT('Ctrl Pts',(-0.361415101720502,-2.12228785127793,
3.70364691350217));
#97513=CARTESIAN_POINT('Ctrl Pts',(1.58767559662444,-1.45396451102085,3.81483333333334));
#97514=CARTESIAN_POINT('Ctrl Pts',(2.08238656893164,0.546253399951339,3.9260197531645));
#97515=CARTESIAN_POINT('Ctrl Pts',(0.669541102087431,2.04607949797729,4.03720617299566));
#97516=CARTESIAN_POINT('Ctrl Pts',(-1.35663306156047,1.67160800898631,4.14839259282683));
#97517=CARTESIAN_POINT('Ctrl Pts',(-2.14007248481188,-0.234128937078206,
4.25957901265799));
#97518=CARTESIAN_POINT('Ctrl Pts',(-0.963112667326238,-1.92539361935742,
4.37076543248915));
#97519=CARTESIAN_POINT('Ctrl Pts',(1.09610013699538,-1.85291421525797,4.48195185232032));
#97520=CARTESIAN_POINT('Ctrl Pts',(2.15123766275159,-0.0830850033729405,
4.59313827215147));
#97521=CARTESIAN_POINT('Ctrl Pts',(1.23574816038915,1.76285367615161,4.70432469198265));
#97522=CARTESIAN_POINT('Ctrl Pts',(-0.811740268440561,1.99394190888763,
4.8155111118138));
#97523=CARTESIAN_POINT('Ctrl Pts',(-2.11563939493572,0.398492848144611,
4.92669753164497));
#97524=CARTESIAN_POINT('Ctrl Pts',(-1.48152105102257,-1.56199294966507,
5.03788395147612));
#97525=CARTESIAN_POINT('Ctrl Pts',(0.509734849759847,-2.0916254402657,5.1490703713073));
#97526=CARTESIAN_POINT('Ctrl Pts',(2.03405151388631,-0.705238284754304,
5.26025679113844));
#97527=CARTESIAN_POINT('Ctrl Pts',(1.69508874624462,1.32717773556567,5.37144321096963));
#97528=CARTESIAN_POINT('Ctrl Pts',(-0.19664885248515,2.1438413719869,5.48262963080077));
#97529=CARTESIAN_POINT('Ctrl Pts',(-1.90824757094816,0.996653303509719,
5.59381605063195));
#97530=CARTESIAN_POINT('Ctrl Pts',(-1.87180872723762,-1.06351242967042,
5.70500247046309));
#97531=CARTESIAN_POINT('Ctrl Pts',(-0.12071188305083,-2.14945463797604,
5.81618889029427));
#97532=CARTESIAN_POINT('Ctrl Pts',(1.74096228296046,-1.26640314621194,5.92737531012542));
#97533=CARTESIAN_POINT('Ctrl Pts',(2.00783946807991,0.776728568965356,6.0385617299566));
#97534=CARTESIAN_POINT('Ctrl Pts',(0.435448592570146,2.10834321747079,6.14974814978775));
#97535=CARTESIAN_POINT('Ctrl Pts',(-1.53583208518367,1.50862401066228,6.26093456961893));
#97536=CARTESIAN_POINT('Ctrl Pts',(-2.10022394255324,-0.473060239877022,
6.37212098945007));
#97537=CARTESIAN_POINT('Ctrl Pts',(-0.74071955267899,-2.02140078749996,
6.48330740928124));
#97538=CARTESIAN_POINT('Ctrl Pts',(1.29731608273796,-1.71805051756223,6.5944938291124));
#97539=CARTESIAN_POINT('Ctrl Pts',(2.14695390376071,0.15910856216126,6.70568024894357));
#97540=CARTESIAN_POINT('Ctrl Pts',(1.02988880574655,1.89051729619815,6.81686666877473));
#97541=CARTESIAN_POINT('Ctrl Pts',(-1.03059911890458,1.89013016894061,6.92805308860589));
#97542=CARTESIAN_POINT('Ctrl Pts',(-2.14701353924984,0.158301805751674,
7.03923950843705));
#97543=CARTESIAN_POINT('Ctrl Pts',(-1.29667041186295,-1.71853787925252,
7.15042592826822));
#97544=CARTESIAN_POINT('Ctrl Pts',(0.741479067384996,-2.0211223100189,7.26161234809938));
#97545=CARTESIAN_POINT('Ctrl Pts',(2.10040155266868,-0.472271020678894,
7.37279876793055));
#97546=CARTESIAN_POINT('Ctrl Pts',(1.53526509213771,1.50920101255294,7.48398518776171));
#97547=CARTESIAN_POINT('Ctrl Pts',(-0.436240798549652,2.10817944328893,
7.59517160759286));
#97548=CARTESIAN_POINT('Ctrl Pts',(-2.00813119194563,0.775974042967894,
7.70635802742404));
#97549=CARTESIAN_POINT('Ctrl Pts',(-1.74048629299744,-1.26705724547931,
7.81754444725519));
#97550=CARTESIAN_POINT('Ctrl Pts',(0.121519559390324,-2.14940912720278,
7.92873086708636));
#97551=CARTESIAN_POINT('Ctrl Pts',(1.87220822337856,-1.06280899870737,8.03991728691751));
#97552=CARTESIAN_POINT('Ctrl Pts',(1.90787293110882,0.997370281398245,8.15110370674869));
#97553=CARTESIAN_POINT('Ctrl Pts',(0.195843262983046,2.1439151139204,8.26229012657984));
#97554=CARTESIAN_POINT('Ctrl Pts',(-1.69558733042143,1.32654069078969,8.37347654641101));
#97555=CARTESIAN_POINT('Ctrl Pts',(-2.03378636810517,-0.706002555693802,
8.48466296624217));
#97556=CARTESIAN_POINT('Ctrl Pts',(-0.508948858861673,-2.09181683182873,
8.59584938607333));
#97557=CARTESIAN_POINT('Ctrl Pts',(1.48210788489943,-1.56143613926181,8.70703580590451));
#97558=CARTESIAN_POINT('Ctrl Pts',(2.11548950721726,0.399287798761521,8.81822222573564));
#97559=CARTESIAN_POINT('Ctrl Pts',(0.810990961415923,1.99424678906897,8.92940864556684));
#97560=CARTESIAN_POINT('Ctrl Pts',(-1.23641048638147,1.76238920508216,9.04059506539797));
#97561=CARTESIAN_POINT('Ctrl Pts',(-2.15120629331062,-0.0838933551026959,
9.15178148522916));
#97562=CARTESIAN_POINT('Ctrl Pts',(-1.09540379848118,-1.85332595276186,
9.26296790506031));
#97563=CARTESIAN_POINT('Ctrl Pts',(0.963836080712942,-1.9250315915564,9.37415432489147));
#97564=CARTESIAN_POINT('Ctrl Pts',(2.14016032912378,-0.233324742234878,
9.48534074472264));
#97565=CARTESIAN_POINT('Ctrl Pts',(1.35600480268067,1.67211762704833,9.5965271645538));
#97566=CARTESIAN_POINT('Ctrl Pts',(-0.67030982818557,2.04582783352242,9.70771358438496));
#97567=CARTESIAN_POINT('Ctrl Pts',(-2.08259181106143,0.545470747680921,
9.81890000421612));
#97568=CARTESIAN_POINT('Ctrl Pts',(-1.58712889620009,-1.45456074914393,
9.93008642404728));
#97569=CARTESIAN_POINT('Ctrl Pts',(0.362212090727357,-2.12215236818265,
10.0412728438785));
#97570=CARTESIAN_POINT('Ctrl Pts',(1.97975271162804,-0.845758688953388,
10.1524592637096));
#97571=CARTESIAN_POINT('Ctrl Pts',(1.78375086909329,1.20538347801125,10.2636456835408));
#97572=CARTESIAN_POINT('Ctrl Pts',(-0.0462382725911752,2.15234810763501,
10.3748321033719));
#97573=CARTESIAN_POINT('Ctrl Pts',(-1.83388235020868,1.12765702777161,10.4860185232031));
#97574=CARTESIAN_POINT('Ctrl Pts',(-1.94158931298892,-0.929994984054507,
10.5972049430343));
#97575=CARTESIAN_POINT('Ctrl Pts',(-0.270756821184746,-2.13577279771527,
10.7083913628654));
#97576=CARTESIAN_POINT('Ctrl Pts',(1.64817793797518,-1.38501096239512,10.8195777826966));
#97577=CARTESIAN_POINT('Ctrl Pts',(2.0571630907777,0.634330397736036,10.9307642025277));
#97578=CARTESIAN_POINT('Ctrl Pts',(0.58197770073898,2.07288432925282,11.0419506223589));
#97579=CARTESIAN_POINT('Ctrl Pts',(-1.42685805211597,1.61204019596003,11.1531370421901));
#97580=CARTESIAN_POINT('Ctrl Pts',(-2.12761151034289,-0.324461171008946,
11.2643234620212));
#97581=CARTESIAN_POINT('Ctrl Pts',(-0.881342614057178,-1.96574134576644,
11.3755098818524));
#97582=CARTESIAN_POINT('Ctrl Pts',(1.17620974724197,-1.80236812191326,11.4866963016836));
#97583=CARTESIAN_POINT('Ctrl Pts',(1.82356548323819,-0.598586618003602,
11.560820581571));
#97584=CARTESIAN_POINT('Ctrl Pts',(1.82115221868229,0.00725425160419088,
11.5978827215147));
#97585=CARTESIAN_POINT('Ctrl Pts',(-0.861525859670525,1.75382131162755,
-1.38777878078145E-16));
#97586=CARTESIAN_POINT('Ctrl Pts',(-1.44496782441849,1.46721837385112,0.0370621399437207));
#97587=CARTESIAN_POINT('Ctrl Pts',(-2.29323624142731,0.270948940037977,
0.111186419831162));
#97588=CARTESIAN_POINT('Ctrl Pts',(-1.4690228053469,-1.78453568564088,0.222372839662325));
#97589=CARTESIAN_POINT('Ctrl Pts',(0.702798023147504,-2.19964250335881,
0.333559259493488));
#97590=CARTESIAN_POINT('Ctrl Pts',(2.22983948348091,-0.602620646924488,
0.44474567932465));
#97591=CARTESIAN_POINT('Ctrl Pts',(1.71476659751129,1.54790339194469,0.555932099155814));
#97592=CARTESIAN_POINT('Ctrl Pts',(-0.371377304572895,2.2797075413722,0.667118518986976));
#97593=CARTESIAN_POINT('Ctrl Pts',(-2.11718147056775,0.923606631345987,
0.778304938818138));
#97594=CARTESIAN_POINT('Ctrl Pts',(-1.92363015131696,-1.2787712372945,0.889491358649302));
#97595=CARTESIAN_POINT('Ctrl Pts',(0.0320890232727887,-2.30962717925356,
1.00067777848046));
#97596=CARTESIAN_POINT('Ctrl Pts',(1.95839267869742,-1.22482325334233,1.11186419831163));
#97597=CARTESIAN_POINT('Ctrl Pts',(2.09073448897961,0.982002812028443,1.22305061814279));
#97598=CARTESIAN_POINT('Ctrl Pts',(0.3078671242282,2.28925546628532,1.33423703797395));
#97599=CARTESIAN_POINT('Ctrl Pts',(-1.75701689972769,1.49945932314417,1.44542345780511));
#97600=CARTESIAN_POINT('Ctrl Pts',(-2.21239878427269,-0.663911091192784,
1.55660987763628));
#97601=CARTESIAN_POINT('Ctrl Pts',(-0.641126576885465,-2.21910779030204,
1.66779629746744));
#97602=CARTESIAN_POINT('Ctrl Pts',(1.51744495713052,-1.74150671579767,1.7789827172986));
#97603=CARTESIAN_POINT('Ctrl Pts',(2.28597130487397,0.331390712847842,1.89016913712977));
#97604=CARTESIAN_POINT('Ctrl Pts',(0.960448643749269,2.10071953052146,2.00135555696093));
#97605=CARTESIAN_POINT('Ctrl Pts',(-1.24488658037438,1.94569829998722,2.11254197679209));
#97606=CARTESIAN_POINT('Ctrl Pts',(-2.30985172178094,0.00833292063536468,
2.22372839662325));
#97607=CARTESIAN_POINT('Ctrl Pts',(-1.2588924584139,-1.93666572611094,2.33491481645442));
#97608=CARTESIAN_POINT('Ctrl Pts',(0.945266903418065,-2.10759457362527,
2.44610123628558));
#97609=CARTESIAN_POINT('Ctrl Pts',(2.28352077714336,-0.347875342430591,
2.55728765611674));
#97610=CARTESIAN_POINT('Ctrl Pts',(1.52997054850621,1.73051278744978,2.6684740759479));
#97611=CARTESIAN_POINT('Ctrl Pts',(-0.625099077306038,2.22367613142842,
2.77966049577907));
#97612=CARTESIAN_POINT('Ctrl Pts',(-2.20755082977362,0.679855665342084,
2.89084691561023));
#97613=CARTESIAN_POINT('Ctrl Pts',(-1.76779024968342,-1.48674208393651,
3.00203333544139));
#97614=CARTESIAN_POINT('Ctrl Pts',(0.291342892527361,-2.29141958423335,
3.11321975527256));
#97615=CARTESIAN_POINT('Ctrl Pts',(2.08359330569799,-0.997057334412016,
3.22440617510372));
#97616=CARTESIAN_POINT('Ctrl Pts',(1.96718185643314,1.21065268979674,3.33559259493488));
#97617=CARTESIAN_POINT('Ctrl Pts',(0.0487464827201324,2.30935232741881,
3.44677901476604));
#97618=CARTESIAN_POINT('Ctrl Pts',(-1.91434278399063,1.29258504441778,3.55796543459721));
#97619=CARTESIAN_POINT('Ctrl Pts',(-2.12381100893932,-0.908246216603541,
3.66915185442837));
#97620=CARTESIAN_POINT('Ctrl Pts',(-0.38777621054007,-2.27708453998192,
3.78033827425954));
#97621=CARTESIAN_POINT('Ctrl Pts',(1.70347841995286,-1.56001463596674,3.89152469409069));
#97622=CARTESIAN_POINT('Ctrl Pts',(2.23427291426326,0.58609635407974,4.00271111392186));
#97623=CARTESIAN_POINT('Ctrl Pts',(0.718376487679439,2.19531765665651,4.11389753375301));
#97624=CARTESIAN_POINT('Ctrl Pts',(-1.45558396757891,1.79353274433565,4.22508395358419));
#97625=CARTESIAN_POINT('Ctrl Pts',(-2.29616635965357,-0.251205972206891,
4.33627037341534));
#97626=CARTESIAN_POINT('Ctrl Pts',(-1.03336074967814,-2.06582911991821,
4.44745679324651));
#97627=CARTESIAN_POINT('Ctrl Pts',(1.17604813820203,-1.98806317010017,4.55864321307767));
#97628=CARTESIAN_POINT('Ctrl Pts',(2.30814590995695,-0.0891451065749571,
4.66982963290884));
#97629=CARTESIAN_POINT('Ctrl Pts',(1.32588189186442,1.89143374203362,4.78101605273999));
#97630=CARTESIAN_POINT('Ctrl Pts',(-0.870947461077787,2.1393772252035,4.89220247257116));
#97631=CARTESIAN_POINT('Ctrl Pts',(-2.26995115459196,0.427558355600586,
5.00338889240232));
#97632=CARTESIAN_POINT('Ctrl Pts',(-1.58958111120973,-1.67592251687317,
5.11457531223348));
#97633=CARTESIAN_POINT('Ctrl Pts',(0.546914192237968,-2.24418565586851,
5.22576173206465));
#97634=CARTESIAN_POINT('Ctrl Pts',(2.1824123683356,-0.756677372605439,5.33694815189581));
#97635=CARTESIAN_POINT('Ctrl Pts',(1.81872613351991,1.4239802115651,5.44813457172697));
#97636=CARTESIAN_POINT('Ctrl Pts',(-0.210992142997687,2.30021014415434,
5.55932099155813));
#97637=CARTESIAN_POINT('Ctrl Pts',(-2.04743246287144,1.06934779265563,5.67050741138931));
#97638=CARTESIAN_POINT('Ctrl Pts',(-2.00833582118916,-1.14108352937273,
5.78169383122044));
#97639=CARTESIAN_POINT('Ctrl Pts',(-0.129516437895867,-2.30623283386393,
5.89288025105164));
#97640=CARTESIAN_POINT('Ctrl Pts',(1.86794562143574,-1.35877280920554,6.00406667088277));
#97641=CARTESIAN_POINT('Ctrl Pts',(2.15428845280213,0.83338205752262,6.11525309071395));
#97642=CARTESIAN_POINT('Ctrl Pts',(0.467209600008474,2.26212280421227,6.22643951054511));
#97643=CARTESIAN_POINT('Ctrl Pts',(-1.64785351575852,1.61866092257753,6.33762593037627));
#97644=CARTESIAN_POINT('Ctrl Pts',(-2.25341132081031,-0.507564587930634,
6.44881235020743));
#97645=CARTESIAN_POINT('Ctrl Pts',(-0.794746594271866,-2.1688389157728,
6.55999877003859));
#97646=CARTESIAN_POINT('Ctrl Pts',(1.39194049181108,-1.84336270411821,6.67118518986976));
#97647=CARTESIAN_POINT('Ctrl Pts',(2.30354969961477,0.170713716736379,6.78237160970093));
#97648=CARTESIAN_POINT('Ctrl Pts',(1.1050074456459,2.02840896683692,6.89355802953208));
#97649=CARTESIAN_POINT('Ctrl Pts',(-1.10576956804586,2.02799360306213,7.00474444936325));
#97650=CARTESIAN_POINT('Ctrl Pts',(-2.30361368483253,0.169848116649841,
7.11593086919441));
#97651=CARTESIAN_POINT('Ctrl Pts',(-1.39124772661127,-1.84388561328419,
7.22711728902557));
#97652=CARTESIAN_POINT('Ctrl Pts',(0.795561506911461,-2.16854012653626,
7.33830370885674));
#97653=CARTESIAN_POINT('Ctrl Pts',(2.25360188555757,-0.506717804195071,
7.44949012868789));
#97654=CARTESIAN_POINT('Ctrl Pts',(1.64724516703786,1.61928001017393,7.56067654851907));
#97655=CARTESIAN_POINT('Ctrl Pts',(-0.468059588377044,2.26194708457211,
7.67186296835021));
#97656=CARTESIAN_POINT('Ctrl Pts',(-2.154601454596,0.832572497460946,7.78304938818139));
#97657=CARTESIAN_POINT('Ctrl Pts',(-1.8674349134348,-1.35947461755279,7.89423580801255));
#97658=CARTESIAN_POINT('Ctrl Pts',(0.130383025010703,-2.30618400359892,
8.00542222784371));
#97659=CARTESIAN_POINT('Ctrl Pts',(2.00876445601631,-1.14032879114536,8.11660864767487));
#97660=CARTESIAN_POINT('Ctrl Pts',(2.04703049732954,1.07011706590215,8.22779506750604));
#97661=CARTESIAN_POINT('Ctrl Pts',(0.210127794931219,2.30028926472067,8.3389814873372));
#97662=CARTESIAN_POINT('Ctrl Pts',(-1.81926108372479,1.42329670163983,8.45016790716836));
#97663=CARTESIAN_POINT('Ctrl Pts',(-2.18212788319439,-0.757497388391501,
8.56135432699953));
#97664=CARTESIAN_POINT('Ctrl Pts',(-0.546070872270014,-2.24439100726275,
8.67254074683069));
#97665=CARTESIAN_POINT('Ctrl Pts',(1.59021074792356,-1.67532509350284,8.78372716666185));
#97666=CARTESIAN_POINT('Ctrl Pts',(2.26979033427429,0.428411288796547,8.89491358649301));
#97667=CARTESIAN_POINT('Ctrl Pts',(0.870143500653468,2.13970434291613,9.00610000632417));
#97668=CARTESIAN_POINT('Ctrl Pts',(-1.32659252698235,1.89093539309814,9.11728642615534));
#97669=CARTESIAN_POINT('Ctrl Pts',(-2.30811225247311,-0.0900124183420705,
9.2284728459865));
#97670=CARTESIAN_POINT('Ctrl Pts',(-1.17530100973675,-1.98850493915805,
9.33965926581767));
#97671=CARTESIAN_POINT('Ctrl Pts',(1.03413692781901,-2.06544068631896,9.45084568564882));
#97672=CARTESIAN_POINT('Ctrl Pts',(2.29626061120593,-0.250343120523647,
9.56203210547999));
#97673=CARTESIAN_POINT('Ctrl Pts',(1.45490988438074,1.79407953322179,9.67321852531115));
#97674=CARTESIAN_POINT('Ctrl Pts',(-0.719201283577143,2.19504763615053,
9.78440494514231));
#97675=CARTESIAN_POINT('Ctrl Pts',(-2.2344931264651,0.585256616254353,9.89559136497349));
#97676=CARTESIAN_POINT('Ctrl Pts',(-1.70289184396906,-1.56065436285928,
10.0067777848046));
#97677=CARTESIAN_POINT('Ctrl Pts',(0.388631330803272,-2.27693917494037,
10.1179642046358));
#97678=CARTESIAN_POINT('Ctrl Pts',(2.1241530878674,-0.907447137301155,10.229150624467));
#97679=CARTESIAN_POINT('Ctrl Pts',(1.91385514681521,1.29330245229283,10.3403370442981));
#97680=CARTESIAN_POINT('Ctrl Pts',(-0.0496108271125438,2.30933734912719,
10.4515234641293));
#97681=CARTESIAN_POINT('Ctrl Pts',(-1.96764314760194,1.20990674417448,10.5627098839605));
#97682=CARTESIAN_POINT('Ctrl Pts',(-2.08320610464741,-0.997827509202423,
10.6738963037916));
#97683=CARTESIAN_POINT('Ctrl Pts',(-0.290505442625618,-2.29155305943203,
10.7850827236228));
#97684=CARTESIAN_POINT('Ctrl Pts',(1.7683937169233,-1.48603171255794,10.8962691434539));
#97685=CARTESIAN_POINT('Ctrl Pts',(2.20720967111538,0.680597564112484,11.0074555632851));
#97686=CARTESIAN_POINT('Ctrl Pts',(0.624426335084105,2.22407759459687,11.1186419831163));
#97687=CARTESIAN_POINT('Ctrl Pts',(-1.53093107010227,1.72962013887028,11.2298284029474));
#97688=CARTESIAN_POINT('Ctrl Pts',(-2.28279649924591,-0.348126912135875,
11.3410148227786));
#97689=CARTESIAN_POINT('Ctrl Pts',(-0.945626503816835,-2.10911975270116,
11.4522012426097));
#97690=CARTESIAN_POINT('Ctrl Pts',(1.26200083066393,-1.93383031585166,11.5633876624409));
#97691=CARTESIAN_POINT('Ctrl Pts',(1.95657378287586,-0.642246683396576,
11.6375119423284));
#97692=CARTESIAN_POINT('Ctrl Pts',(1.95398449819998,0.0077833665056624,
11.6745740822721));
#97693=CARTESIAN_POINT('Ctrl Pts',(-1.95093054978418,-0.000550606481354719,
10.6241303078758));
#97694=CARTESIAN_POINT('Ctrl Pts',(-1.95166977968097,-0.292567552961119,
10.640718973181));
#97695=CARTESIAN_POINT('Ctrl Pts',(-1.89027401228485,-0.584289311968449,
10.6573076384863));
#97696=CARTESIAN_POINT('Ctrl Pts',(-1.7651621681362,-0.845492725344543,
10.6738963037916));
#97697=CARTESIAN_POINT('Ctrl Pts',(-1.48563921730681,-1.42906935927896,
10.7109584437353));
#97698=CARTESIAN_POINT('Ctrl Pts',(-0.888072329966215,-1.8603112093555,
10.7480205836791));
#97699=CARTESIAN_POINT('Ctrl Pts',(-0.246139026371096,-1.94167857658142,
10.7850827236228));
#97700=CARTESIAN_POINT('Ctrl Pts',(0.395794277224022,-2.02304594380734,
10.8221448635665));
#97701=CARTESIAN_POINT('Ctrl Pts',(1.08209399707366,-1.75453882818264,10.8592070035102));
#97702=CARTESIAN_POINT('Ctrl Pts',(1.49837984936383,-1.25918039092522,10.8962691434539));
#97703=CARTESIAN_POINT('Ctrl Pts',(1.91466570165399,-0.763821953667804,
10.9333312833977));
#97704=CARTESIAN_POINT('Ctrl Pts',(2.06093768638468,-0.041612194777677,
10.9703934233414));
#97705=CARTESIAN_POINT('Ctrl Pts',(1.87027645607817,0.576739356414784,11.0074555632851));
#97706=CARTESIAN_POINT('Ctrl Pts',(1.80418088670294,0.791100177355746,11.0203037088567));
#97707=CARTESIAN_POINT('Ctrl Pts',(1.69759382901609,0.992979671982257,11.0331518544284));
#97708=CARTESIAN_POINT('Ctrl Pts',(1.56057659382855,1.17255425406022,11.046));
#97709=CARTESIAN_POINT('Ctrl Pts',(-0.9055496143049,-1.2679201530598,4.59701721133854E-17));
#97710=CARTESIAN_POINT('Ctrl Pts',(-0.937460871048188,-1.25085822491965,
4.11134559556874E-17));
#97711=CARTESIAN_POINT('Ctrl Pts',(-0.968677330061127,-1.23263760516135,
2.44937731663795E-16));
#97712=CARTESIAN_POINT('Ctrl Pts',(-0.999128467894991,-1.21327242330634,
1.95156391047391E-16));
#97713=CARTESIAN_POINT('Ctrl Pts',(-1.04916478169554,-1.18145218981002,
1.19833509668E-16));
#97714=CARTESIAN_POINT('Ctrl Pts',(-1.09713600671012,-1.14654455097205,
1.20483738925504E-16));
#97715=CARTESIAN_POINT('Ctrl Pts',(-1.14296368523792,-1.10887020140839,
3.46944695195361E-17));
#97716=CARTESIAN_POINT('Ctrl Pts',(-1.1691715546085,-1.08732504652154,-1.4366579135275E-17));
#97717=CARTESIAN_POINT('Ctrl Pts',(-1.19467812556179,-1.06487409533188,
1.54611493479508E-16));
#97718=CARTESIAN_POINT('Ctrl Pts',(-1.21946596262297,-1.04157045589269,
1.28369537222284E-16));
#97719=CARTESIAN_POINT('Ctrl Pts',(-1.23288807387334,-1.02895200756582,
1.14160049906282E-16));
#97720=CARTESIAN_POINT('Ctrl Pts',(-1.24610308792281,-1.01607950194371,
2.35779340588765E-16));
#97721=CARTESIAN_POINT('Ctrl Pts',(-1.25908578368524,-1.0029839550804,2.28983498828939E-16));
#97722=CARTESIAN_POINT('Ctrl Pts',(-1.30296735026586,-0.95872095130156,
2.06013524941215E-16));
#97723=CARTESIAN_POINT('Ctrl Pts',(-1.34424080059494,-0.911874911049719,
3.41092537496216E-16));
#97724=CARTESIAN_POINT('Ctrl Pts',(-1.3828175432908,-0.862794893107178,
2.15105711021124E-16));
#97725=CARTESIAN_POINT('Ctrl Pts',(-1.41246270387874,-0.825078255778903,
1.18288316865636E-16));
#97726=CARTESIAN_POINT('Ctrl Pts',(-1.44051505756546,-0.786041114269597,
-3.41744083773187E-17));
#97727=CARTESIAN_POINT('Ctrl Pts',(-1.46692433972057,-0.745823635123971,
-2.77555756156289E-17));
#97728=CARTESIAN_POINT('Ctrl Pts',(-1.479951210132,-0.725985614308893,-2.45893667770833E-17));
#97729=CARTESIAN_POINT('Ctrl Pts',(-1.49257814628919,-0.705860181165347,
1.12314029669873E-16));
#97730=CARTESIAN_POINT('Ctrl Pts',(-1.50479813274716,-0.685463000140721,
1.31838984174237E-16));
#97731=CARTESIAN_POINT('Ctrl Pts',(-1.51107691151866,-0.674982678607113,
1.41871145034493E-16));
#97732=CARTESIAN_POINT('Ctrl Pts',(-1.51724344631134,-0.664438579506566,
2.39743182585592E-16));
#97733=CARTESIAN_POINT('Ctrl Pts',(-1.52329612440982,-0.653835068968427,
2.42861286636753E-16));
#97734=CARTESIAN_POINT('Ctrl Pts',(-1.55541704658302,-0.597563360607725,
2.59408734877987E-16));
#97735=CARTESIAN_POINT('Ctrl Pts',(-1.58434358367058,-0.539605423501723,
2.32306933354682E-17));
#97736=CARTESIAN_POINT('Ctrl Pts',(-1.60998194797531,-0.480314579840224,
1.38777878078145E-17));
#97737=CARTESIAN_POINT('Ctrl Pts',(-1.63611695660561,-0.419875204988797,
4.34370584461709E-18));
#97738=CARTESIAN_POINT('Ctrl Pts',(-1.65883591999594,-0.358049987819819,
-3.99522282745635E-16));
#97739=CARTESIAN_POINT('Ctrl Pts',(-1.67800508733892,-0.295172269836945,
-4.02455846426619E-16));
#97740=CARTESIAN_POINT('Ctrl Pts',(-1.69036857863681,-0.254618180804147,
-4.04347899868101E-16));
#97741=CARTESIAN_POINT('Ctrl Pts',(-1.70125468815875,-0.21362546632645,
2.10692284276142E-16));
#97742=CARTESIAN_POINT('Ctrl Pts',(-1.71061789501208,-0.172277279535232,
2.22044604925031E-16));
#97743=CARTESIAN_POINT('Ctrl Pts',(-1.71585060492304,-0.149169484288187,
2.28388948449886E-16));
#97744=CARTESIAN_POINT('Ctrl Pts',(-1.72060753217063,-0.125950592727189,
-7.81124113857471E-17));
#97745=CARTESIAN_POINT('Ctrl Pts',(-1.72487954070067,-0.102634681883505,
-6.93889390390723E-17));
#97746=CARTESIAN_POINT('Ctrl Pts',(-1.72700542719079,-0.0910319475914671,
-6.50478634353357E-17));
#97747=CARTESIAN_POINT('Ctrl Pts',(-1.7290114810898,-0.0794035343790101,
3.2530658909822E-16));
#97748=CARTESIAN_POINT('Ctrl Pts',(-1.73089565945358,-0.0677563287869385,
3.05311331771918E-16));
#97749=CARTESIAN_POINT('Ctrl Pts',(-1.74172479313661,-0.000815136373784872,
1.90390516006322E-16));
#97750=CARTESIAN_POINT('Ctrl Pts',(-1.74848828323664,0.0664709663887247,
1.66332759660732E-17));
#97751=CARTESIAN_POINT('Ctrl Pts',(-1.75106678678907,0.133744024330042,
0.));
#97752=CARTESIAN_POINT('Ctrl Pts',(-1.75197767455289,0.157509050853062,
-5.87590718476407E-18));
#97753=CARTESIAN_POINT('Ctrl Pts',(-1.75236592486458,0.181272742240003,
-1.43574718418596E-16));
#97754=CARTESIAN_POINT('Ctrl Pts',(-1.75222496230419,0.20502014676713,-1.52655665885959E-16));
#97755=CARTESIAN_POINT('Ctrl Pts',(-1.75184009030703,0.269858008556557,
-1.89868827307373E-16));
#97756=CARTESIAN_POINT('Ctrl Pts',(-1.74751402866387,0.334573792851957,
-3.30194805135327E-16));
#97757=CARTESIAN_POINT('Ctrl Pts',(-1.7394637798186,0.398932034828451,-3.60822483003176E-16));
#97758=CARTESIAN_POINT('Ctrl Pts',(-1.73512917103287,0.433585348839861,
-3.77313774654407E-16));
#97759=CARTESIAN_POINT('Ctrl Pts',(-1.72971393872322,0.468135193807322,
-2.30290250750647E-16));
#97760=CARTESIAN_POINT('Ctrl Pts',(-1.72324590502527,0.502545438383202,
-2.22044604925031E-16));
#97761=CARTESIAN_POINT('Ctrl Pts',(-1.71875224847293,0.526451903350239,
-2.16315955056648E-16));
#97762=CARTESIAN_POINT('Ctrl Pts',(-1.71375034317529,0.550290993458765,
-1.09112752506388E-16));
#97763=CARTESIAN_POINT('Ctrl Pts',(-1.70824837476028,0.574050543226345,
-1.11022302462516E-16));
#97764=CARTESIAN_POINT('Ctrl Pts',(-1.70556019910987,0.585659087356796,
-1.11955278682682E-16));
#97765=CARTESIAN_POINT('Ctrl Pts',(-1.70275214211861,0.597250589985584,
-1.86923780482983E-17));
#97766=CARTESIAN_POINT('Ctrl Pts',(-1.69982665236451,0.608817432227434,
-2.77555756156289E-17));
#97767=CARTESIAN_POINT('Ctrl Pts',(-1.68323412399998,0.674421202576402,
-7.91594003935956E-17));
#97768=CARTESIAN_POINT('Ctrl Pts',(-1.6629277813761,0.739001412074313,-4.05964646411352E-16));
#97769=CARTESIAN_POINT('Ctrl Pts',(-1.63916833994428,0.802303176749866,
-3.88578058618805E-16));
#97770=CARTESIAN_POINT('Ctrl Pts',(-1.61488642929252,0.866996944840365,
-3.70809140417215E-16));
#97771=CARTESIAN_POINT('Ctrl Pts',(-1.58699772603761,0.930356288581554,
-4.09457680297508E-17));
#97772=CARTESIAN_POINT('Ctrl Pts',(-1.55572518982035,0.992113582996803,
0.));
#97773=CARTESIAN_POINT('Ctrl Pts',(-1.52416508821539,1.05443876420538,4.13222832434933E-17));
#97774=CARTESIAN_POINT('Ctrl Pts',(-1.48915832892389,1.11513327578217,-2.91589739144645E-16));
#97775=CARTESIAN_POINT('Ctrl Pts',(-1.45088203376165,1.17391247934435,-2.77555756156289E-16));
#97776=CARTESIAN_POINT('Ctrl Pts',(-1.43586030613212,1.19698067814596,-2.72048047818399E-16));
#97777=CARTESIAN_POINT('Ctrl Pts',(-1.42033446520901,1.21975369583959,-2.46829292445535E-16));
#97778=CARTESIAN_POINT('Ctrl Pts',(-1.40431321996707,1.24221341255695,-2.22044604925031E-16));
#97779=CARTESIAN_POINT('Ctrl Pts',(-1.39827097600966,1.25068385824148,-2.12697320981403E-16));
#97780=CARTESIAN_POINT('Ctrl Pts',(-1.39215941512485,1.25910802930607,-2.5395452896005E-16));
#97781=CARTESIAN_POINT('Ctrl Pts',(-1.38598454691313,1.26747777400967,-2.4980018054066E-16));
#97782=CARTESIAN_POINT('Ctrl Pts',(-1.3431243018081,1.32557282918544,-2.20964521964367E-16));
#97783=CARTESIAN_POINT('Ctrl Pts',(-1.29714727100707,1.38114651172693,8.67497813555755E-17));
#97784=CARTESIAN_POINT('Ctrl Pts',(-1.24829449348075,1.43391808714502,5.55111512312578E-17));
#97785=CARTESIAN_POINT('Ctrl Pts',(-1.19933005104754,1.48681028483588,2.42011176187261E-17));
#97786=CARTESIAN_POINT('Ctrl Pts',(-1.14747626839011,1.53688856046327,-1.29713890200027E-16));
#97787=CARTESIAN_POINT('Ctrl Pts',(-1.09292624810297,1.58385401467225,-2.77555756156289E-17));
#97788=CARTESIAN_POINT('Ctrl Pts',(-1.03954323648884,1.62981471962349,7.20215071969156E-17));
#97789=CARTESIAN_POINT('Ctrl Pts',(-0.983577547054738,1.67279522220595,
1.33536308196711E-16));
#97790=CARTESIAN_POINT('Ctrl Pts',(-0.92517040004714,1.71248622994896,1.66533453693773E-16));
#97791=CARTESIAN_POINT('Ctrl Pts',(-0.904266808925204,1.72669141954621,
1.78342947445829E-16));
#97792=CARTESIAN_POINT('Ctrl Pts',(-0.883050159709791,1.74047492561567,
-1.31748417511445E-16));
#97793=CARTESIAN_POINT('Ctrl Pts',(-0.861525859670525,1.75382131162755,
-1.38777878078145E-16));
#97794=CARTESIAN_POINT('Origin',(0.,0.,0.));
#97795=CARTESIAN_POINT('Origin',(-0.866025403784439,-1.5,-4.));
#97796=CARTESIAN_POINT('',(-0.866025403784439,-1.5,-4.));
#97797=CARTESIAN_POINT('',(0.866025403784439,-1.5,-4.));
#97798=CARTESIAN_POINT('',(-0.43301270189222,-1.5,-4.));
#97799=CARTESIAN_POINT('',(-0.866025403784439,-1.5,-2.));
#97800=CARTESIAN_POINT('',(-0.866025403784439,-1.5,-4.));
#97801=CARTESIAN_POINT('',(0.866025403784439,-1.5,-2.));
#97802=CARTESIAN_POINT('',(-0.866025403784439,-1.5,-2.));
#97803=CARTESIAN_POINT('',(0.866025403784439,-1.5,-4.));
#97804=CARTESIAN_POINT('Origin',(-1.73205080756888,2.12115047744981E-16,
-4.));
#97805=CARTESIAN_POINT('',(-1.73205080756888,2.12115047744981E-16,-4.));
#97806=CARTESIAN_POINT('',(-1.51554445662277,-0.375,-4.));
#97807=CARTESIAN_POINT('',(-1.73205080756888,2.77555756156289E-16,-2.));
#97808=CARTESIAN_POINT('',(-1.73205080756888,2.12115047744981E-16,-4.));
#97809=CARTESIAN_POINT('',(-1.73205080756888,2.12115047744981E-16,-2.));
#97810=CARTESIAN_POINT('Origin',(-0.866025403784438,1.5,-4.));
#97811=CARTESIAN_POINT('',(-0.866025403784438,1.5,-4.));
#97812=CARTESIAN_POINT('',(-1.08253175473055,1.125,-4.));
#97813=CARTESIAN_POINT('',(-0.866025403784438,1.5,-2.));
#97814=CARTESIAN_POINT('',(-0.866025403784438,1.5,-4.));
#97815=CARTESIAN_POINT('',(-0.866025403784438,1.5,-2.));
#97816=CARTESIAN_POINT('Origin',(0.866025403784439,1.5,-4.));
#97817=CARTESIAN_POINT('',(0.866025403784439,1.5,-4.));
#97818=CARTESIAN_POINT('',(0.43301270189222,1.5,-4.));
#97819=CARTESIAN_POINT('',(0.866025403784439,1.5,-2.));
#97820=CARTESIAN_POINT('',(0.866025403784439,1.5,-4.));
#97821=CARTESIAN_POINT('',(0.866025403784439,1.5,-2.));
#97822=CARTESIAN_POINT('Origin',(1.73205080756888,0.,-4.));
#97823=CARTESIAN_POINT('',(1.73205080756888,0.,-4.));
#97824=CARTESIAN_POINT('',(1.51554445662277,0.375,-4.));
#97825=CARTESIAN_POINT('',(1.73205080756888,0.,-2.));
#97826=CARTESIAN_POINT('',(1.73205080756888,0.,-4.));
#97827=CARTESIAN_POINT('',(1.73205080756888,0.,-2.));
#97828=CARTESIAN_POINT('Origin',(0.866025403784439,-1.5,-4.));
#97829=CARTESIAN_POINT('',(1.08253175473055,-1.125,-4.));
#97830=CARTESIAN_POINT('',(0.866025403784439,-1.5,-2.));
#97831=CARTESIAN_POINT('Origin',(0.,2.77555756156289E-16,-2.));
#97832=CARTESIAN_POINT('Origin',(0.,0.,0.));
#97833=CARTESIAN_POINT('',(-3.5,-4.28626379701574E-16,0.));
#97834=CARTESIAN_POINT('Origin',(0.,0.,0.));
#97835=CARTESIAN_POINT('Origin',(0.,0.,-4.));
#97836=CARTESIAN_POINT('',(-3.5,-4.28626379701574E-16,-4.));
#97837=CARTESIAN_POINT('',(-3.5,-4.28626379701574E-16,-4.));
#97838=CARTESIAN_POINT('Origin',(0.,0.,-4.));
#97839=CARTESIAN_POINT('Origin',(0.,0.,-4.));
#97840=CARTESIAN_POINT('Origin',(0.,0.,12.));
#99506=UNCERTAINTY_MEASURE_WITH_UNIT(LENGTH_MEASURE(0.01),#99527,
'DISTANCE_ACCURACY_VALUE',
'Maximum model space distance between geometric entities at asserted c
onnectivities');
#99508=UNCERTAINTY_MEASURE_WITH_UNIT(LENGTH_MEASURE(0.01),#99527,
'DISTANCE_ACCURACY_VALUE',
'Maximum model space distance between geometric entities at asserted c
onnectivities');
#99524=(
GEOMETRIC_REPRESENTATION_CONTEXT(3)
GLOBAL_UNCERTAINTY_ASSIGNED_CONTEXT((#99506))
GLOBAL_UNIT_ASSIGNED_CONTEXT((#99527,#99529,#99530))
REPRESENTATION_CONTEXT('','3D')
);
#99526=(
GEOMETRIC_REPRESENTATION_CONTEXT(3)
GLOBAL_UNCERTAINTY_ASSIGNED_CONTEXT((#99508))
GLOBAL_UNIT_ASSIGNED_CONTEXT((#99527,#99529,#99530))
REPRESENTATION_CONTEXT('','3D')
);
#99527=(
LENGTH_UNIT()
NAMED_UNIT(*)
SI_UNIT(.MILLI.,.METRE.)
);
#99529=(
NAMED_UNIT(*)
PLANE_ANGLE_UNIT()
SI_UNIT($,.RADIAN.)
);
#99530=(
NAMED_UNIT(*)
SI_UNIT($,.STERADIAN.)
SOLID_ANGLE_UNIT()
);
#99546=SHAPE_DEFINITION_REPRESENTATION(#99563,#99639);
#99563=PRODUCT_DEFINITION_SHAPE('',$,#99657);
#99639=SHAPE_REPRESENTATION('',(#19647),#99524);
#99641=PRODUCT_DEFINITION_CONTEXT('part definition',#99694,'design');
#99657=PRODUCT_DEFINITION('Socket head cap screw M4x12',
'Socket head cap screw M4x12',#99674,#99641);
#99674=PRODUCT_DEFINITION_FORMATION('',$,#99711);
#99694=APPLICATION_CONTEXT(
'Core Data for Automotive Mechanical Design Process');
#99695=PRODUCT_CONTEXT('part definition',#99694,'mechanical');
#99711=PRODUCT('Socket head cap screw M4x12',
'Socket head cap screw M4x12',$,(#99695));
#99722=PRESENTATION_STYLE_ASSIGNMENT((#99735));
#99735=SURFACE_STYLE_USAGE(.BOTH.,#99748);
#99748=SURFACE_SIDE_STYLE('',(#99761));
#99761=SURFACE_STYLE_FILL_AREA(#99774);
#99774=FILL_AREA_STYLE('Dark gray',(#99787));
#99787=FILL_AREA_STYLE_COLOUR('Dark gray',#99800);
#99800=COLOUR_RGB('Dark gray',0.250980392156863,0.282352941176471,0.32156862745098);
ENDSEC;
END-ISO-10303-21;
